ISO-10303-21;
HEADER;
FILE_DESCRIPTION (('STEP AP214'),
    '1' );
FILE_NAME ('7. Anchor.step',
    '2026-10-09T14:04:53',
    ( '' ),
    ( '' ),
    'SwSTEP 2.0',
    'SolidWorks 2021',
    '' );
FILE_SCHEMA (( 'AUTOMOTIVE_DESIGN' ));
ENDSEC;

DATA;
#41=CARTESIAN_POINT ( 'NONE',  ( 5.082755093536325930, -14.84375000204838457, -5.082755093536325042 ) ) ;
#44=CARTESIAN_POINT ( 'NONE',  ( 6.653282514704100592, -30.00000000000001066, 2.730950945157442966 ) ) ;
#48=CARTESIAN_POINT ( 'NONE',  ( -1.320432766682874540E-15, -21.40625000204838457, 7.188101187500000044 ) ) ;
#65=EDGE_LOOP ( 'NONE', ( #73939, #52655, #97069, #25713 ) ) ;
#66=CARTESIAN_POINT ( 'NONE',  ( -7.934883677559675164, 88.86839177937550005, 1.051380792122690311 ) ) ;
#94=CARTESIAN_POINT ( 'NONE',  ( -1.320432766682874540E-15, -24.40625000204838813, 7.188101187500000044 ) ) ;
#107=CARTESIAN_POINT ( 'NONE',  ( -7.188101187500002709, -10.81250000204838457, 2.977408999572647819 ) ) ;
#108=CARTESIAN_POINT ( 'NONE',  ( 7.344505440741524005, 27.55381072701297285, -3.175463080953007999 ) ) ;
#121=CARTESIAN_POINT ( 'NONE',  ( -5.082755093536326818, -28.71875000204838813, 5.082755093536325042 ) ) ;
#129=AXIS2_PLACEMENT_3D ( 'NONE', #36140, #18887, #77080 ) ;
#181=CARTESIAN_POINT ( 'NONE',  ( 7.188101187500000044, -19.15625000204838457, 0.000000000000000000 ) ) ;
#183=CARTESIAN_POINT ( 'NONE',  ( 9.333892298909262308, 83.21724268374964595, -3.590295303293451923 ) ) ;
#235=CARTESIAN_POINT ( 'NONE',  ( 7.188101187500000933, -29.56250000204838813, -2.977408999572650483 ) ) ;
#243=LINE ( 'NONE', #66079, #65315 ) ;
#244=CARTESIAN_POINT ( 'NONE',  ( -5.656854249492379694, -21.12500000409676915, -5.656854249492380582 ) ) ;
#278=CARTESIAN_POINT ( 'NONE',  ( -7.211357414135266986, 32.01146539934441648, 3.467230644691326802 ) ) ;
#297=CARTESIAN_POINT ( 'NONE',  ( -3.313708498984817119, -22.53124999999998934, -7.999999999999941380 ) ) ;
#335=CARTESIAN_POINT ( 'NONE',  ( 7.999912353029506207, 101.0001752939690647, -0.2691822806795024503 ) ) ;
#366=CARTESIAN_POINT ( 'NONE',  ( -5.656854249492381470, -10.06249999999999112, 5.656854249492379694 ) ) ;
#378=( BOUNDED_CURVE ( )  B_SPLINE_CURVE ( 2, ( #76091, #61000, #11891, #101964, #28124, #35141, #100895, #50737, #44819 ),
 .UNSPECIFIED., .F., .F. ) 
 B_SPLINE_CURVE_WITH_KNOTS ( ( 3, 2, 2, 2, 3 ),
 ( 0.5735294117647058432, 0.5808823529411765163, 0.5882352941176470784, 0.5955882352941176405, 0.6029411764705882026 ),
 .UNSPECIFIED. ) 
 CURVE ( )  GEOMETRIC_REPRESENTATION_ITEM ( )  RATIONAL_B_SPLINE_CURVE ( ( 1.000000000000000000, 0.9238795325112867385, 1.000000000000000000, 0.9238795325112867385, 1.000000000000000000, 0.9238795325112867385, 1.000000000000000000, 0.9238795325112867385, 1.000000000000000000 ) ) 
 REPRESENTATION_ITEM ( '' )  );
#398=CARTESIAN_POINT ( 'NONE',  ( -6.928203230275510549, 29.99999999999999645, -4.000000000000000000 ) ) ;
#418=MECHANICAL_DESIGN_GEOMETRIC_PRESENTATION_REPRESENTATION('',(#43583),#41807);
#431=CARTESIAN_POINT ( 'NONE',  ( 7.188101187500001821, -34.06250000204839523, -2.977408999572650483 ) ) ;
#466=ORIENTED_EDGE ( 'NONE', *, *, #57229, .F. ) ;
#488=CARTESIAN_POINT ( 'NONE',  ( 8.000000000000000000, -28.90624999999999645, -3.313708498984761608 ) ) ;
#514=CARTESIAN_POINT ( 'NONE',  ( -1.320432766682874540E-15, -16.53125000204838813, 7.188101187500000044 ) ) ;
#567=CARTESIAN_POINT ( 'NONE',  ( -1.320432766682874540E-15, -12.40625000204838635, 7.188101187500000044 ) ) ;
#577=CARTESIAN_POINT ( 'NONE',  ( 7.188101187500001821, -17.93750000204838457, -2.977408999572650483 ) ) ;
#602=FACE_BOUND ( 'NONE', #43188, .T. ) ;
#618=CARTESIAN_POINT ( 'NONE',  ( 10.00005432054556920, 25.99986419862086962, 0.2621623937322681286 ) ) ;
#619=CARTESIAN_POINT ( 'NONE',  ( 7.188101187500001821, -16.43750000204838457, -2.977408999572650483 ) ) ;
#630=CARTESIAN_POINT ( 'NONE',  ( -5.082755093536325042, -9.593750002048384573, -5.082755093536325930 ) ) ;
#644=CARTESIAN_POINT ( 'NONE',  ( -5.082755093536325042, -33.59375000204838813, -5.082755093536325930 ) ) ;
#646=VECTOR ( 'NONE', #4565, 1000.000000000000000 ) ;
#699=VERTEX_POINT ( 'NONE', #90019 ) ;
#703=CARTESIAN_POINT ( 'NONE',  ( 7.188101187499999156, -10.25000000204838813, 2.977408999572654924 ) ) ;
#739=ORIENTED_EDGE ( 'NONE', *, *, #66044, .F. ) ;
#760=CARTESIAN_POINT ( 'NONE',  ( -7.188101187500002709, -22.81250000204838813, 2.977408999572647819 ) ) ;
#765=ORIENTED_EDGE ( 'NONE', *, *, #69858, .F. ) ;
#770=CARTESIAN_POINT ( 'NONE',  ( -10.00000000000000178, 15.00000000000000000, 1.734723475976807489E-15 ) ) ;
#771=CARTESIAN_POINT ( 'NONE',  ( 5.656854249492380582, -23.00000000409677270, -5.656854249492379694 ) ) ;
#775=CARTESIAN_POINT ( 'NONE',  ( 9.646032546913145822, 33.01280328474367565, 2.644051433538245011 ) ) ;
#778=CARTESIAN_POINT ( 'NONE',  ( -3.420980250011399715, -30.00000000000000355, -7.222355033959453330 ) ) ;
#802=CARTESIAN_POINT ( 'NONE',  ( 3.313708498984762496, -12.78124999999999467, 7.999999999999998224 ) ) ;
#813=CARTESIAN_POINT ( 'NONE',  ( -6.943482370013978944, 30.52848370260725019, 3.973876482044365499 ) ) ;
#819=EDGE_LOOP ( 'NONE', ( #7919, #30918, #47841, #33303 ) ) ;
#822=CARTESIAN_POINT ( 'NONE',  ( -3.313708498984726969, -20.65625000409677625, 8.000000000000039080 ) ) ;
#846=DIRECTION ( 'NONE',  ( -0.000000000000000000, -1.000000000000000000, -0.000000000000000000 ) ) ;
#864=CARTESIAN_POINT ( 'NONE',  ( 7.343637806710344051, 102.5563687809938074, 3.177475076494674866 ) ) ;
#896=CARTESIAN_POINT ( 'NONE',  ( 4.898587196589412829E-16, -10.62499999999999289, -8.000000000000000000 ) ) ;
#902=DIRECTION ( 'NONE',  ( -0.000000000000000000, 1.000000000000000000, -0.000000000000000000 ) ) ;
#912=CARTESIAN_POINT ( 'NONE',  ( -3.313708498984774042, -29.65625000409676559, 7.999999999999988454 ) ) ;
#926=SURFACE_STYLE_FILL_AREA ( #48971 ) ;
#927=CARTESIAN_POINT ( 'NONE',  ( -7.212994264445058867, 82.98288655659960966, 3.463766307298584035 ) ) ;
#934=B_SPLINE_CURVE_WITH_KNOTS ( 'NONE', 3,
 ( #24452, #57285, #25512, #81035, #90207, #31991, #16307, #49199, #58367, #82099, #49739, #41127, #83174, #82648, #74011, #74541, #72940, #618, #15251, #91288, #9272, #64866, #72427, #56212, #64357, #7151, #59997, #100950, #27645, #42179, #43254, #34665, #17930, #44318 ),
 .UNSPECIFIED., .F., .F.,
 ( 4, 2, 2, 2, 2, 2, 2, 2, 2, 2, 2, 2, 2, 2, 2, 2, 4 ),
 ( 0.000000000000000000, 0.0007899309203816044745, 0.001579861840763208949, 0.002369792761144813315, 0.003159723681526417898, 0.003949654601908022047, 0.004739585522289626630, 0.005529516442671232081, 0.006319447363052837531, 0.007109378283434441247, 0.007899309203816045830, 0.008689240124197651280, 0.009479171044579254995, 0.01026910196496085871, 0.01105903288534246416, 0.01184896380572406788, 0.01263889472610567159 ),
 .UNSPECIFIED. ) ;
#940=CIRCLE ( 'NONE', #85382, 8.000000000000000000 ) ;
#956=CARTESIAN_POINT ( 'NONE',  ( -1.469576158976823947E-15, -27.87499999999999645, 8.000000000000000000 ) ) ;
#963=CARTESIAN_POINT ( 'NONE',  ( 2.977408999572650927, -30.87500000204838813, -7.188101187500001821 ) ) ;
#975=ORIENTED_EDGE ( 'NONE', *, *, #52449, .T. ) ;
#1009=( BOUNDED_CURVE ( )  B_SPLINE_CURVE ( 2, ( #65512, #39132, #73042, #72532, #104921, #15893, #105953, #40692, #72010 ),
 .UNSPECIFIED., .F., .F. ) 
 B_SPLINE_CURVE_WITH_KNOTS ( ( 3, 2, 2, 2, 3 ),
 ( 0.5441176470588234837, 0.5514705882352941568, 0.5588235294117647189, 0.5661764705882352811, 0.5735294117647058432 ),
 .UNSPECIFIED. ) 
 CURVE ( )  GEOMETRIC_REPRESENTATION_ITEM ( )  RATIONAL_B_SPLINE_CURVE ( ( 1.000000000000000000, 0.9238795325112867385, 1.000000000000000000, 0.9238795325112867385, 1.000000000000000000, 0.9238795325112867385, 1.000000000000000000, 0.9238795325112867385, 1.000000000000000000 ) ) 
 REPRESENTATION_ITEM ( '' )  );
#1024=CARTESIAN_POINT ( 'NONE',  ( 4.898587196589412829E-16, -28.62499999999999289, -8.000000000000000000 ) ) ;
#1041=DIRECTION ( 'NONE',  ( -0.000000000000000000, 1.000000000000000000, -0.000000000000000000 ) ) ;
#1053=CARTESIAN_POINT ( 'NONE',  ( -3.999995229665001428, -8.688226215992830959, 6.928205984420947594 ) ) ;
#1054=CARTESIAN_POINT ( 'NONE',  ( -2.977408999572654480, -10.62500000204838813, 7.188101187499999156 ) ) ;
#1057=ORIENTED_EDGE ( 'NONE', *, *, #67703, .T. ) ;
#1063=EDGE_CURVE ( 'NONE', #63010, #81483, #29576, .T. ) ;
#1111=CARTESIAN_POINT ( 'NONE',  ( -1.320432766682874540E-15, -15.40625000204838635, 7.188101187500000044 ) ) ;
#1121=CARTESIAN_POINT ( 'NONE',  ( 2.977408999572651815, -18.31250000204838457, 7.188101187500000933 ) ) ;
#1135=ORIENTED_EDGE ( 'NONE', *, *, #16738, .T. ) ;
#1137=CARTESIAN_POINT ( 'NONE',  ( -7.151217271224854066, 86.78749400445715878, -3.587901469523282927 ) ) ;
#1159=DIRECTION ( 'NONE',  ( -0.000000000000000000, 1.000000000000000000, -0.000000000000000000 ) ) ;
#1160=CARTESIAN_POINT ( 'NONE',  ( -5.082755093536326818, -21.59375000204838457, 5.082755093536325042 ) ) ;
#1185=CARTESIAN_POINT ( 'NONE',  ( -2.977408999572650039, -30.68750000204839168, -7.188101187500001821 ) ) ;
#1189=DIRECTION ( 'NONE',  ( -0.000000000000000000, 1.000000000000000000, -0.000000000000000000 ) ) ;
#1237=DIRECTION ( 'NONE',  ( 1.734723475976807094E-16, 0.000000000000000000, 1.000000000000000000 ) ) ;
#1247=CARTESIAN_POINT ( 'NONE',  ( 2.977408999572650927, -12.87500000204838280, -7.188101187500001821 ) ) ;
#1261=ORIENTED_EDGE ( 'NONE', *, *, #74125, .F. ) ;
#1287=VERTEX_POINT ( 'NONE', #53687 ) ;
#1308=CARTESIAN_POINT ( 'NONE',  ( 2.977408999572650927, -27.87500000204838457, -7.188101187500000933 ) ) ;
#1311=PRESENTATION_STYLE_ASSIGNMENT (( #82794 ) ) ;
#1319=CARTESIAN_POINT ( 'NONE',  ( -5.656854249492379694, -25.62500000409677270, -5.656854249492380582 ) ) ;
#1341=ADVANCED_FACE ( 'NONE', ( #26797 ), #44552, .F. ) ;
#1371=CARTESIAN_POINT ( 'NONE',  ( 10.00000000000000000, 0.000000000000000000, 10.00000000000000000 ) ) ;
#1374=LINE ( 'NONE', #95210, #95947 ) ;
#1400=ORIENTED_EDGE ( 'NONE', *, *, #19466, .F. ) ;
#1426=CARTESIAN_POINT ( 'NONE',  ( 7.999999999999998224, -15.59374999999999289, 3.313708498984766049 ) ) ;
#1452=CARTESIAN_POINT ( 'NONE',  ( -8.000000000000000000, -10.34374999999999289, -3.313708498984762496 ) ) ;
#1471=CARTESIAN_POINT ( 'NONE',  ( -5.656854249492381470, -29.75000000409677270, 5.656854249492379694 ) ) ;
#1487=CARTESIAN_POINT ( 'NONE',  ( -7.619135598915499408, 81.82694632215323338, 2.449260492474793161 ) ) ;
#1506=ORIENTED_EDGE ( 'NONE', *, *, #47518, .F. ) ;
#1575=CARTESIAN_POINT ( 'NONE',  ( 3.313708498984762496, -26.28124999999999645, 7.999999999999998224 ) ) ;
#1584=CARTESIAN_POINT ( 'NONE',  ( -3.313708498984722528, -9.218750004096770923, -8.000000000000040856 ) ) ;
#1596=CARTESIAN_POINT ( 'NONE',  ( 7.896254658894418021, 108.7892918275420016, 1.307282859663298158 ) ) ;
#1601=CARTESIAN_POINT ( 'NONE',  ( -9.798380800342664898, 88.46800654315505597, -2.010350564680321472 ) ) ;
#1669=CARTESIAN_POINT ( 'NONE',  ( 7.188101187499999156, -19.62500000204838457, 2.977408999572654924 ) ) ;
#1685=CARTESIAN_POINT ( 'NONE',  ( 8.000000000000000000, -13.90624999999999289, -3.313708498984761164 ) ) ;
#1713=CARTESIAN_POINT ( 'NONE',  ( -7.188101187500001821, -18.87500000204838457, -2.977408999572651371 ) ) ;
#1739=CARTESIAN_POINT ( 'NONE',  ( -8.000000000000001776, -8.843750004096769146, 3.313708498984758943 ) ) ;
#1788=CARTESIAN_POINT ( 'NONE',  ( -1.320432766682874540E-15, -25.90625000204838813, 7.188101187500000044 ) ) ;
#1796=CARTESIAN_POINT ( 'NONE',  ( -1.320432766682874540E-15, -15.03125000204838457, 7.188101187500000044 ) ) ;
#1800=CARTESIAN_POINT ( 'NONE',  ( 4.898587196589412829E-16, -15.12499999999999289, -8.000000000000000000 ) ) ;
#1831=CARTESIAN_POINT ( 'NONE',  ( 7.046289519167722837, 83.69408180055623347, -3.789821819998813623 ) ) ;
#1839=VERTEX_POINT ( 'NONE', #53941 ) ;
#1852=CARTESIAN_POINT ( 'NONE',  ( -2.977408999572654480, -25.62500000204838813, 7.188101187499999156 ) ) ;
#1863=CARTESIAN_POINT ( 'NONE',  ( 8.000000000000000000, -26.18750000409677270, 0.000000000000000000 ) ) ;
#1913=CYLINDRICAL_SURFACE ( 'NONE', #24062, 8.000000000000000000 ) ;
#1926=CARTESIAN_POINT ( 'NONE',  ( 0.000000000000000000, 15.00000000000000000, 9.999999999999998224 ) ) ;
#1949=ORIENTED_EDGE ( 'NONE', *, *, #16553, .T. ) ;
#2018=DIRECTION ( 'NONE',  ( 0.000000000000000000, 0.000000000000000000, -1.000000000000000000 ) ) ;
#2027=CARTESIAN_POINT ( 'NONE',  ( -9.699016383038308931, 108.1763817144834121, 2.444973590251038775 ) ) ;
#2048=ORIENTED_EDGE ( 'NONE', *, *, #96195, .T. ) ;
#2054=ORIENTED_EDGE ( 'NONE', *, *, #72475, .F. ) ;
#2110=CARTESIAN_POINT ( 'NONE',  ( 5.656854249492378806, -24.68749999999999289, 5.656854249492381470 ) ) ;
#2113=DIRECTION ( 'NONE',  ( -0.9090909090909092827, 0.000000000000000000, -0.4165977904505306917 ) ) ;
#2133=CARTESIAN_POINT ( 'NONE',  ( 4.898587196589412829E-16, -16.62499999999999289, -8.000000000000000000 ) ) ;
#2146=EDGE_CURVE ( 'NONE', #13028, #60867, #101289, .T. ) ;
#2171=AXIS2_PLACEMENT_3D ( 'NONE', #72189, #104547, #31231 ) ;
#2199=CARTESIAN_POINT ( 'NONE',  ( -7.188101187500002709, -18.68750000204838102, 2.977408999572648707 ) ) ;
#2239=CARTESIAN_POINT ( 'NONE',  ( 4.401442555609581635E-16, -22.15625000204838457, -7.188101187500000044 ) ) ;
#2242=CARTESIAN_POINT ( 'NONE',  ( -1.469576158976823947E-15, -11.56250000409677092, 8.000000000000000000 ) ) ;
#2247=CARTESIAN_POINT ( 'NONE',  ( 9.482993638194542996, 87.44348720253677243, -3.177441187500463560 ) ) ;
#2265=CARTESIAN_POINT ( 'NONE',  ( 7.188101187500000044, -26.65625000204838813, 0.000000000000000000 ) ) ;
#2277=ORIENTED_EDGE ( 'NONE', *, *, #96460, .F. ) ;
#2278=CARTESIAN_POINT ( 'NONE',  ( 3.313708498984800688, -17.28124999999999645, 7.999999999999960032 ) ) ;
#2322=CARTESIAN_POINT ( 'NONE',  ( -7.188101187500000933, -24.87500000204838813, -2.977408999572651371 ) ) ;
#2332=CARTESIAN_POINT ( 'NONE',  ( -2.977408999572654480, -12.12500000204838990, 7.188101187499999156 ) ) ;
#2338=CARTESIAN_POINT ( 'NONE',  ( -3.313708498984726969, -14.46874999999999112, 8.000000000000039080 ) ) ;
#2370=CARTESIAN_POINT ( 'NONE',  ( 7.986452802927059835, 81.02690242308116808, 0.5332468218996382348 ) ) ;
#2393=CARTESIAN_POINT ( 'NONE',  ( 4.401442555609581635E-16, -27.78125000204838457, -7.188101187500000044 ) ) ;
#2397=FILL_AREA_STYLE_COLOUR ( '', #74565 ) ;
#2404=CARTESIAN_POINT ( 'NONE',  ( 8.000000000000000000, -15.68750000409677092, 0.000000000000000000 ) ) ;
#2419=VECTOR ( 'NONE', #1159, 1000.000000000000000 ) ;
#2506=EDGE_CURVE ( 'NONE', #79080, #28854, #19010, .T. ) ;
#2510=CARTESIAN_POINT ( 'NONE',  ( -2.797224791467303184, 15.83450757143047305, -9.607634652978001455 ) ) ;
#2548=CARTESIAN_POINT ( 'NONE',  ( -9.090909090909093493, 16.00000000000000000, 4.165977904505304252 ) ) ;
#2558=CARTESIAN_POINT ( 'NONE',  ( -9.221249107921748234, 106.0482137149848683, 3.869340886054259521 ) ) ;
#2590=LINE ( 'NONE', #35540, #78896 ) ;
#2621=ORIENTED_EDGE ( 'NONE', *, *, #105168, .T. ) ;
#2645=ORIENTED_EDGE ( 'NONE', *, *, #53175, .T. ) ;
#2650=CARTESIAN_POINT ( 'NONE',  ( 8.000000000000000000, -18.49999999999999289, 0.000000000000000000 ) ) ;
#2652=CARTESIAN_POINT ( 'NONE',  ( 9.797174393178825657E-16, 115.0000000000000000, 8.000000000000000000 ) ) ;
#2669=CARTESIAN_POINT ( 'NONE',  ( 7.999885325681426629, 108.9997706512993858, 0.2682325777720065418 ) ) ;
#2723=CARTESIAN_POINT ( 'NONE',  ( -9.699189539447123920, 101.8230777175328541, -2.444343703917210675 ) ) ;
#2738=CARTESIAN_POINT ( 'NONE',  ( 5.082755093536324154, -12.21875000204838635, 5.082755093536326818 ) ) ;
#2745=CARTESIAN_POINT ( 'NONE',  ( -3.313708498984765161, -14.65625000409677092, 7.999999999999998224 ) ) ;
#2750=UNCERTAINTY_MEASURE_WITH_UNIT (LENGTH_MEASURE( 1.000000000000000082E-05 ), #102451, 'distance_accuracy_value', 'NONE');
#2771=DIRECTION ( 'NONE',  ( 0.000000000000000000, -1.000000000000000000, 0.000000000000000000 ) ) ;
#2782=CARTESIAN_POINT ( 'NONE',  ( 7.188101187499999156, -18.12500000204838457, 2.977408999572654924 ) ) ;
#2793=CARTESIAN_POINT ( 'NONE',  ( 9.843481099141458301, 88.59204556153383692, -1.779148000612192693 ) ) ;
#2803=ORIENTED_EDGE ( 'NONE', *, *, #49663, .F. ) ;
#2808=CARTESIAN_POINT ( 'NONE',  ( -5.082755093536326818, -22.71875000204838457, 5.082755093536325042 ) ) ;
#2821=CARTESIAN_POINT ( 'NONE',  ( 8.000000000000000000, -16.90624999999999289, -3.313708498984761164 ) ) ;
#2835=VECTOR ( 'NONE', #86940, 1000.000000000000000 ) ;
#2838=CARTESIAN_POINT ( 'NONE',  ( 8.000000000000000000, -25.90624999999999645, -3.313708498984761164 ) ) ;
#2856=CARTESIAN_POINT ( 'NONE',  ( -7.188101187500000044, -24.78125000204838813, -8.802885111219163269E-16 ) ) ;
#2866=CARTESIAN_POINT ( 'NONE',  ( 4.401442555609581635E-16, -12.78125000204838280, -7.188101187500000044 ) ) ;
#2881=CYLINDRICAL_SURFACE ( 'NONE', #76744, 8.000000000000000000 ) ;
#2897=CARTESIAN_POINT ( 'NONE',  ( 7.999999999999998224, -11.09374999999999289, 3.313708498984766049 ) ) ;
#2914=VECTOR ( 'NONE', #29107, 1000.000000000000000 ) ;
#2925=CARTESIAN_POINT ( 'NONE',  ( -1.320432766682874540E-15, -24.03125000204838457, 7.188101187500000044 ) ) ;
#2929=FACE_OUTER_BOUND ( 'NONE', #102349, .T. ) ;
#2934=CARTESIAN_POINT ( 'NONE',  ( -8.000000000000000000, -18.03125000409677625, -3.313708498984762496 ) ) ;
#2962=VECTOR ( 'NONE', #33069, 1000.000000000000000 ) ;
#3001=CARTESIAN_POINT ( 'NONE',  ( 4.401442555609581635E-16, -30.78125000204838813, -7.188101187500000044 ) ) ;
#3043=CARTESIAN_POINT ( 'NONE',  ( 3.313708498984722972, -15.21874999999999112, -8.000000000000040856 ) ) ;
#3054=CARTESIAN_POINT ( 'NONE',  ( 8.000000000000000000, -11.09375000409677092, -3.313708498984761164 ) ) ;
#3075=AXIS2_PLACEMENT_3D ( 'NONE', #29172, #80838, #63083 ) ;
#3098=CARTESIAN_POINT ( 'NONE',  ( -9.151133496029540737, 15.07443463110275417, 4.034557488804506598 ) ) ;
#3199=CARTESIAN_POINT ( 'NONE',  ( -8.000000000000000000, -22.34374999999999289, -3.313708498984762496 ) ) ;
#3251=CARTESIAN_POINT ( 'NONE',  ( 4.898587196589412829E-16, -12.12499999999999289, -8.000000000000000000 ) ) ;
#3287=CARTESIAN_POINT ( 'NONE',  ( -5.082755093536326818, -15.59375000204838635, 5.082755093536325042 ) ) ;
#3293=CARTESIAN_POINT ( 'NONE',  ( -5.656854249492381470, -14.75000000409677092, 5.656854249492379694 ) ) ;
#3325=CARTESIAN_POINT ( 'NONE',  ( -1.320432766682874540E-15, -10.90625000204838457, 7.188101187500000044 ) ) ;
#3327=EDGE_CURVE ( 'NONE', #81483, #89014, #70580, .T. ) ;
#3340=FACE_OUTER_BOUND ( 'NONE', #26445, .T. ) ;
#3358=CARTESIAN_POINT ( 'NONE',  ( 2.977408999572651815, -23.93750000204838457, 7.188101187500000933 ) ) ;
#3407=CARTESIAN_POINT ( 'NONE',  ( 5.082755093536325930, -23.84375000204838457, -5.082755093536325042 ) ) ;
#3418=CARTESIAN_POINT ( 'NONE',  ( -7.188101187500000044, -9.406250002048384573, -8.802885111219163269E-16 ) ) ;
#3427=CARTESIAN_POINT ( 'NONE',  ( -6.928203230275507885, 105.0000000000000000, -4.000000000000001776 ) ) ;
#3457=CARTESIAN_POINT ( 'NONE',  ( -5.082755093536326818, -29.09375000204838813, 5.082755093536325042 ) ) ;
#3472=CARTESIAN_POINT ( 'NONE',  ( -2.977408999572654480, -18.12500000204838457, 7.188101187499999156 ) ) ;
#3485=CARTESIAN_POINT ( 'NONE',  ( -1.469576158976823947E-15, -19.06250000409677270, 8.000000000000000000 ) ) ;
#3492=CARTESIAN_POINT ( 'NONE',  ( 1.754457302166835930, -30.00000000000002132, -7.493468971370472076 ) ) ;
#3495=FILL_AREA_STYLE_COLOUR ( '', #45710 ) ;
#3521=ORIENTED_EDGE ( 'NONE', *, *, #96460, .T. ) ;
#3536=CARTESIAN_POINT ( 'NONE',  ( 9.797174393178825657E-16, -30.00000000000000000, -8.000000000000000000 ) ) ;
#3543=VERTEX_POINT ( 'NONE', #59101 ) ;
#3546=CARTESIAN_POINT ( 'NONE',  ( -5.082755093536326818, -24.21875000204838813, 5.082755093536325042 ) ) ;
#3593=VECTOR ( 'NONE', #85180, 1000.000000000000000 ) ;
#3603=VERTEX_POINT ( 'NONE', #38043 ) ;
#3605=ADVANCED_FACE ( 'NONE', ( #45053 ), #52581, .T. ) ;
#3647=CARTESIAN_POINT ( 'NONE',  ( -9.842473135306409660, 108.5893181711358721, 1.785129593756277222 ) ) ;
#3711=VERTEX_POINT ( 'NONE', #24368 ) ;
#3731=CARTESIAN_POINT ( 'NONE',  ( -9.852211596319794040, 15.56091200510340755, -1.749942564367551912 ) ) ;
#3739=CARTESIAN_POINT ( 'NONE',  ( -5.656854249492381470, -23.56249999999999289, 5.656854249492379694 ) ) ;
#3765=SURFACE_STYLE_FILL_AREA ( #93303 ) ;
#3803=CARTESIAN_POINT ( 'NONE',  ( -9.989113211954167681, 101.0270072645100754, 0.5334031035449037228 ) ) ;
#3805=CARTESIAN_POINT ( 'NONE',  ( -4.582575694955840717, 15.00000000000000000, -10.00000000000000000 ) ) ;
#3821=CARTESIAN_POINT ( 'NONE',  ( 2.977408999572650927, -16.25000000204838813, -7.188101187500001821 ) ) ;
#3856=CARTESIAN_POINT ( 'NONE',  ( 7.619753052866895970, 33.17451502807172403, -2.447276542590444137 ) ) ;
#3863=CARTESIAN_POINT ( 'NONE',  ( 2.977408999572651815, -15.31250000204838457, 7.188101187500000933 ) ) ;
#3889=CARTESIAN_POINT ( 'NONE',  ( 5.082755093536325930, -26.46875000204838813, -5.082755093536325042 ) ) ;
#3908=CARTESIAN_POINT ( 'NONE',  ( 9.645512969475854348, 101.9889684932427514, -2.645801731561389758 ) ) ;
#3938=CARTESIAN_POINT ( 'NONE',  ( 2.977408999572652260, -22.81250000204838813, 7.188101187500000044 ) ) ;
#3941=ORIENTED_EDGE ( 'NONE', *, *, #87900, .F. ) ;
#3948=CARTESIAN_POINT ( 'NONE',  ( -1.320432766682874540E-15, -31.90625000204838813, 7.188101187500000044 ) ) ;
#3954=CARTESIAN_POINT ( 'NONE',  ( -7.619701877737479201, 108.1744215953277006, -2.447562251315980486 ) ) ;
#3962=ORIENTED_EDGE ( 'NONE', *, *, #29073, .F. ) ;
#3992=CARTESIAN_POINT ( 'NONE',  ( 7.188101187499999156, -28.62500000204838457, 2.977408999572654924 ) ) ;
#4004=CARTESIAN_POINT ( 'NONE',  ( -7.188101187500000933, -20.00000000204838457, -2.977408999572651371 ) ) ;
#4008=CARTESIAN_POINT ( 'NONE',  ( -9.948688207305195874, 81.12976850509815563, -1.044946705213431137 ) ) ;
#4011=CARTESIAN_POINT ( 'NONE',  ( 7.999999999999998224, -17.28125000409677270, 3.313708498984766493 ) ) ;
#4049=ADVANCED_FACE ( 'NONE', ( #87893 ), #21073, .T. ) ;
#4075=CARTESIAN_POINT ( 'NONE',  ( -1.320432766682874540E-15, -24.03125000204838457, 7.188101187500000044 ) ) ;
#4101=EDGE_LOOP ( 'NONE', ( #11753, #78760, #16712, #101804 ) ) ;
#4117=CARTESIAN_POINT ( 'NONE',  ( 9.999999999999998224, 15.00000000000000000, 4.582575694955846934 ) ) ;
#4126=CARTESIAN_POINT ( 'NONE',  ( 5.656854249492378806, -11.37500000409677092, 5.656854249492381470 ) ) ;
#4154=CARTESIAN_POINT ( 'NONE',  ( -10.00000000000000355, 30.00000000000000000, 0.000000000000000000 ) ) ;
#4188=ORIENTED_EDGE ( 'NONE', *, *, #2146, .T. ) ;
#4189=AXIS2_PLACEMENT_3D ( 'NONE', #26872, #85071, #11154 ) ;
#4263=CARTESIAN_POINT ( 'NONE',  ( 5.656854249492380582, -19.81249999999999289, -5.656854249492379694 ) ) ;
#4309=CARTESIAN_POINT ( 'NONE',  ( -9.537291425704607306, 27.35595622667227289, 3.012810007365996245 ) ) ;
#4310=CARTESIAN_POINT ( 'NONE',  ( -3.313708498984741180, -27.03124999999998934, -8.000000000000019540 ) ) ;
#4323=VERTEX_POINT ( 'NONE', #27445 ) ;
#4345=CARTESIAN_POINT ( 'NONE',  ( -5.082755093536325042, -14.46875000204838457, -5.082755093536325930 ) ) ;
#4348=STYLED_ITEM ( 'NONE', ( #38521 ), #99162 ) ;
#4367=CARTESIAN_POINT ( 'NONE',  ( 3.313708498984780260, -25.90625000409676915, -7.999999999999981348 ) ) ;
#4375=AXIS2_PLACEMENT_3D ( 'NONE', #36784, #2771, #68598 ) ;
#4383=CARTESIAN_POINT ( 'NONE',  ( 5.082755093536325930, -14.84375000204838457, -5.082755093536325042 ) ) ;
#4411=CARTESIAN_POINT ( 'NONE',  ( -2.977408999572650039, -20.18750000204838457, -7.188101187500001821 ) ) ;
#4429=CARTESIAN_POINT ( 'NONE',  ( 9.989285784994811124, 101.0265757255430117, 0.5301777604595964144 ) ) ;
#4445=COLOUR_RGB ( '', 0.72549020, 0.75294118, 0.79215686) ;
#4463=CARTESIAN_POINT ( 'NONE',  ( -5.082755093536325042, -21.96875000204838457, -5.082755093536325930 ) ) ;
#4474=CARTESIAN_POINT ( 'NONE',  ( -7.188101187500001821, -33.87500000204838813, -2.977408999572651371 ) ) ;
#4495=CARTESIAN_POINT ( 'NONE',  ( 5.656854249492380582, -23.00000000409677270, -5.656854249492379694 ) ) ;
#4513=CARTESIAN_POINT ( 'NONE',  ( -7.188101187500002709, -33.68750000204839523, 2.977408999572648707 ) ) ;
#4519=EDGE_LOOP ( 'NONE', ( #32835, #72333, #11848, #25311 ) ) ;
#4525=CARTESIAN_POINT ( 'NONE',  ( -1.320432766682874540E-15, -19.53125000204838457, 7.188101187500000044 ) ) ;
#4538=CARTESIAN_POINT ( 'NONE',  ( 3.313708498984762052, -18.40625000409676915, -8.000000000000000000 ) ) ;
#4565=DIRECTION ( 'NONE',  ( 1.000000000000000000, -0.000000000000000000, -0.000000000000000000 ) ) ;
#4597=FACE_OUTER_BOUND ( 'NONE', #96513, .T. ) ;
#4609=CARTESIAN_POINT ( 'NONE',  ( -7.188101187500000044, -22.90625000204838457, -8.802885111219163269E-16 ) ) ;
#4610=DIRECTION ( 'NONE',  ( 0.000000000000000000, -1.000000000000000000, 0.000000000000000000 ) ) ;
#4632=AXIS2_PLACEMENT_3D ( 'NONE', #12934, #20034, #70127 ) ;
#4674=CARTESIAN_POINT ( 'NONE',  ( 7.002641335706727865, 28.94912737319167917, 3.868676264653293284 ) ) ;
#4703=( BOUNDED_CURVE ( )  B_SPLINE_CURVE ( 2, ( #46827, #21014, #12856, #95923, #45774, #102417, #103473, #54359, #97485 ),
 .UNSPECIFIED., .F., .F. ) 
 B_SPLINE_CURVE_WITH_KNOTS ( ( 3, 2, 2, 2, 3 ),
 ( 0.8970588235294117974, 0.9044117647058823595, 0.9117647058823529216, 0.9191176470588234837, 0.9264705882352941568 ),
 .UNSPECIFIED. ) 
 CURVE ( )  GEOMETRIC_REPRESENTATION_ITEM ( )  RATIONAL_B_SPLINE_CURVE ( ( 1.000000000000000000, 0.9238795325112867385, 1.000000000000000000, 0.9238795325112867385, 1.000000000000000000, 0.9238795325112867385, 1.000000000000000000, 0.9238795325112867385, 1.000000000000000000 ) ) 
 REPRESENTATION_ITEM ( '' )  );
#4730=CARTESIAN_POINT ( 'NONE',  ( 4.898587196589412829E-16, -13.81250000409676915, -8.000000000000000000 ) ) ;
#4781=CARTESIAN_POINT ( 'NONE',  ( 3.313708498984780260, -24.40625000409677270, -7.999999999999981348 ) ) ;
#4794=CARTESIAN_POINT ( 'NONE',  ( -1.469576158976823947E-15, -18.87499999999999289, 8.000000000000000000 ) ) ;
#4824=EDGE_LOOP ( 'NONE', ( #60598, #22828, #73724, #90867, #73752, #21383, #92292, #65076, #88661 ) ) ;
#4845=CARTESIAN_POINT ( 'NONE',  ( -9.482993638194541219, 27.55651279746323823, -3.177441187500465336 ) ) ;
#4865=CARTESIAN_POINT ( 'NONE',  ( -9.165151389911681434, 104.7328921871708474, -4.000000000000000888 ) ) ;
#4881=CARTESIAN_POINT ( 'NONE',  ( 7.188101187500000044, -13.53125000204838457, 0.000000000000000000 ) ) ;
#4907=CARTESIAN_POINT ( 'NONE',  ( 5.656854249492378806, -26.37500000409677270, 5.656854249492381470 ) ) ;
#4908=CARTESIAN_POINT ( 'NONE',  ( 8.000000000000000000, -17.18750000409676915, 0.000000000000000000 ) ) ;
#4912=EDGE_CURVE ( 'NONE', #3603, #106390, #1374, .T. ) ;
#4918=EDGE_LOOP ( 'NONE', ( #23708, #66932, #53884 ) ) ;
#4924=CARTESIAN_POINT ( 'NONE',  ( -5.082755093536326818, -15.59375000204838635, 5.082755093536325042 ) ) ;
#4952=CARTESIAN_POINT ( 'NONE',  ( 4.401442555609581635E-16, -20.28125000204838813, -7.188101187500000044 ) ) ;
#5001=CARTESIAN_POINT ( 'NONE',  ( 7.188101187499999156, -18.12500000204838457, 2.977408999572654924 ) ) ;
#5005=ORIENTED_EDGE ( 'NONE', *, *, #35494, .F. ) ;
#5010=CARTESIAN_POINT ( 'NONE',  ( -7.188101187500001821, -30.87500000204838813, -2.977408999572651371 ) ) ;
#5036=STYLED_ITEM ( 'NONE', ( #58042 ), #31536 ) ;
#5049=DIRECTION ( 'NONE',  ( -0.000000000000000000, 1.000000000000000000, -0.000000000000000000 ) ) ;
#5051=CARTESIAN_POINT ( 'NONE',  ( 4.401442555609581635E-16, -29.65625000204838813, -7.188101187500000044 ) ) ;
#5064=CARTESIAN_POINT ( 'NONE',  ( 5.082755093536325930, -21.96875000204838457, -5.082755093536325042 ) ) ;
#5072=CARTESIAN_POINT ( 'NONE',  ( -9.537927238823506570, 82.35373142881822162, -3.010735687602428268 ) ) ;
#5074=CARTESIAN_POINT ( 'NONE',  ( 5.656854249492380582, -9.500000004096769146, -5.656854249492379694 ) ) ;
#5077=CARTESIAN_POINT ( 'NONE',  ( 9.999999999999996447, 15.00000000000000000, 3.082707893549208045 ) ) ;
#5081=( LENGTH_UNIT ( ) NAMED_UNIT ( * ) SI_UNIT ( .MILLI., .METRE. ) );
#5083=CARTESIAN_POINT ( 'NONE',  ( -9.165151389911681434, 30.00000000000000000, -4.000000000000000000 ) ) ;
#5138=CARTESIAN_POINT ( 'NONE',  ( -2.977408999572650039, -23.18750000204838813, -7.188101187500001821 ) ) ;
#5153=DIRECTION ( 'NONE',  ( 1.000000000000000000, -0.000000000000000000, -0.000000000000000000 ) ) ;
#5171=( BOUNDED_CURVE ( )  B_SPLINE_CURVE ( 2, ( #18513, #52986, #60043, #11980, #100463, #85352, #27154, #102599, #19604 ),
 .UNSPECIFIED., .F., .F. ) 
 B_SPLINE_CURVE_WITH_KNOTS ( ( 3, 2, 2, 2, 3 ),
 ( 0.4264705882352941568, 0.4338235294117647745, 0.4411764705882353366, 0.4485294117647059542, 0.4558823529411765163 ),
 .UNSPECIFIED. ) 
 CURVE ( )  GEOMETRIC_REPRESENTATION_ITEM ( )  RATIONAL_B_SPLINE_CURVE ( ( 0.9999999999999994449, 0.9238795325112872936, 1.000000000000000000, 0.9238795325112867385, 1.000000000000000000, 0.9238795325112867385, 1.000000000000000000, 0.9238795325112861834, 1.000000000000000666 ) ) 
 REPRESENTATION_ITEM ( '' )  );
#5180=CARTESIAN_POINT ( 'NONE',  ( -8.000000000000001776, -16.34375000409677270, 3.313708498984759387 ) ) ;
#5199=CARTESIAN_POINT ( 'NONE',  ( -6.928203230275510549, 85.00000000000000000, 4.000000000000000000 ) ) ;
#5208=CARTESIAN_POINT ( 'NONE',  ( 8.000000000000000000, -30.68750000409677625, 0.000000000000000000 ) ) ;
#5229=CARTESIAN_POINT ( 'NONE',  ( -9.999999999999998224, 15.00000000000000000, 1.785846837348918736E-15 ) ) ;
#5258=ORIENTED_EDGE ( 'NONE', *, *, #11734, .F. ) ;
#5263=CARTESIAN_POINT ( 'NONE',  ( 3.313708498984762496, -12.96875000409676915, 7.999999999999998224 ) ) ;
#5280=DIRECTION ( 'NONE',  ( 0.000000000000000000, -0.000000000000000000, -1.000000000000000000 ) ) ;
#5328=CARTESIAN_POINT ( 'NONE',  ( 5.656854249492378806, -12.68749999999999467, 5.656854249492381470 ) ) ;
#5330=( BOUNDED_SURFACE ( )  B_SPLINE_SURFACE ( 3, 2, ( 
 ( #28114, #21091, #60989 ),
 ( #37800, #102500, #45336 ),
 ( #93876, #20035, #28643 ),
 ( #70129, #70661, #103555 ),
 ( #103035, #61528, #13463 ),
 ( #20582, #53928, #86859 ),
 ( #14515, #49010, #24782 ),
 ( #15062, #30759, #40404 ),
 ( #15594, #105145, #57630 ),
 ( #90021, #55502, #105667 ) ),
 .UNSPECIFIED., .F., .F., .F. ) 
 B_SPLINE_SURFACE_WITH_KNOTS ( ( 4, 2, 2, 2, 4 ),
 ( 3, 3 ),
 ( 0.002450517525418905579, 0.003060732775749475110, 0.003670948026080045074, 0.004891378526741184569, 0.007332239528063463560 ),
 ( 0.000000000000000000, 1.000000000000000000 ),
 .UNSPECIFIED. ) 
 GEOMETRIC_REPRESENTATION_ITEM ( )  RATIONAL_B_SPLINE_SURFACE ( (
 ( 1.000000000000000000, 0.7071067811865475727, 1.000000000000000000),
 ( 1.000000000000000000, 0.7344063550101432858, 1.000000000000000000),
 ( 1.000000000000000000, 0.7590375248711684897, 1.000000000000000000),
 ( 1.000000000000000000, 0.8038331608703419562, 1.000000000000000000),
 ( 1.000000000000000000, 0.8240352460866020579, 1.000000000000000000),
 ( 1.000000000000000000, 0.8791017378333015886, 1.000000000000000000),
 ( 1.000000000000000000, 0.9085032776981116776, 1.000000000000000000),
 ( 1.000000000000000000, 0.9784170511696360650, 1.000000000000000000),
 ( 1.000000000000000000, 0.9996598051696939935, 1.000000000000000000),
 ( 1.000000000000000000, 1.000000000000000000, 1.000000000000000000) ) ) 
 REPRESENTATION_ITEM ( '' )  SURFACE ( )  );
#5359=EDGE_CURVE ( 'NONE', #15011, #90051, #85941, .T. ) ;
#5379=CARTESIAN_POINT ( 'NONE',  ( -10.00004721872059754, 25.99988195318847772, -0.2617599822266526433 ) ) ;
#5396=FACE_OUTER_BOUND ( 'NONE', #80591, .T. ) ;
#5410=CARTESIAN_POINT ( 'NONE',  ( -2.977408999572650039, -10.06250000204838280, -7.188101187500001821 ) ) ;
#5419=ORIENTED_EDGE ( 'NONE', *, *, #88252, .F. ) ;
#5427=ORIENTED_EDGE ( 'NONE', *, *, #56694, .T. ) ;
#5439=ORIENTED_EDGE ( 'NONE', *, *, #56234, .T. ) ;
#5442=CARTESIAN_POINT ( 'NONE',  ( 8.000113193197767814, 34.00022638645860695, -0.2613481123984610077 ) ) ;
#5450=CARTESIAN_POINT ( 'NONE',  ( -5.082755093536325042, -11.46875000204838635, -5.082755093536325930 ) ) ;
#5473=CARTESIAN_POINT ( 'NONE',  ( -5.082755093536326818, -18.21875000204838457, 5.082755093536325042 ) ) ;
#5492=ORIENTED_EDGE ( 'NONE', *, *, #68893, .T. ) ;
#5523=CARTESIAN_POINT ( 'NONE',  ( 2.977408999572652260, -21.31250000204838813, 7.188101187500000044 ) ) ;
#5530=CARTESIAN_POINT ( 'NONE',  ( -5.082755093536326818, -9.218750002048382797, 5.082755093536325042 ) ) ;
#5569=CARTESIAN_POINT ( 'NONE',  ( 5.082755093536325930, -31.34375000204838457, -5.082755093536325042 ) ) ;
#5573=ORIENTED_EDGE ( 'NONE', *, *, #69858, .T. ) ;
#5583=CARTESIAN_POINT ( 'NONE',  ( 2.977408999572652260, -17.93750000204838457, 7.188101187500000044 ) ) ;
#5596=CARTESIAN_POINT ( 'NONE',  ( 4.898587196589412829E-16, -9.312500004096769146, -8.000000000000000000 ) ) ;
#5598=SURFACE_STYLE_FILL_AREA ( #102170 ) ;
#5600=EDGE_CURVE ( 'NONE', #37759, #50908, #13545, .T. ) ;
#5658=CARTESIAN_POINT ( 'NONE',  ( 5.082755093536324154, -22.34375000204838457, 5.082755093536326818 ) ) ;
#5659=CARTESIAN_POINT ( 'NONE',  ( 5.656854249492380582, -20.00000000409677270, -5.656854249492379694 ) ) ;
#5677=DIRECTION ( 'NONE',  ( 0.4165977904505313578, 0.000000000000000000, 0.9090909090909089496 ) ) ;
#5678=CARTESIAN_POINT ( 'NONE',  ( 9.797174393178825657E-16, 0.000000000000000000, -8.000000000000000000 ) ) ;
#5706=AXIS2_PLACEMENT_3D ( 'NONE', #28518, #79153, #5280 ) ;
#5723=CARTESIAN_POINT ( 'NONE',  ( -5.656854249492379694, -31.62500000409677270, -5.656854249492380582 ) ) ;
#5776=ORIENTED_EDGE ( 'NONE', *, *, #53760, .F. ) ;
#5801=ORIENTED_EDGE ( 'NONE', *, *, #75590, .T. ) ;
#5840=CARTESIAN_POINT ( 'NONE',  ( -8.000000000000001776, -16.15624999999999289, 3.313708498984758943 ) ) ;
#5862=CARTESIAN_POINT ( 'NONE',  ( 9.168149550320974228, 15.99999999372935022, -3.997425403568101387 ) ) ;
#5896=CARTESIAN_POINT ( 'NONE',  ( -10.00000000000000000, 15.00000000000000178, -3.648665620917535435 ) ) ;
#5907=ORIENTED_EDGE ( 'NONE', *, *, #61015, .F. ) ;
#5920=CARTESIAN_POINT ( 'NONE',  ( -5.082755093536326818, -9.593750002048384573, 5.082755093536325042 ) ) ;
#5942=CARTESIAN_POINT ( 'NONE',  ( 4.898587196589412829E-16, -25.81250000409677270, -8.000000000000000000 ) ) ;
#5944=CARTESIAN_POINT ( 'NONE',  ( -1.469576158976823947E-15, -17.56250000409676915, 8.000000000000000000 ) ) ;
#5956=VECTOR ( 'NONE', #51193, 1000.000000000000000 ) ;
#5963=CARTESIAN_POINT ( 'NONE',  ( -5.082755093536325042, -9.968750002048384573, -5.082755093536325930 ) ) ;
#5988=CARTESIAN_POINT ( 'NONE',  ( 7.188101187500001821, -20.56250000204838457, -2.977408999572650483 ) ) ;
#6038=CARTESIAN_POINT ( 'NONE',  ( 2.977408999572652260, -18.31250000204838457, 7.188101187500000044 ) ) ;
#6044=VECTOR ( 'NONE', #66090, 1000.000000000000000 ) ;
#6045=CARTESIAN_POINT ( 'NONE',  ( -7.188101187500002709, -29.18750000204839523, 2.977408999572647819 ) ) ;
#6048=CARTESIAN_POINT ( 'NONE',  ( -5.082755093536326818, -27.59375000204838813, 5.082755093536325042 ) ) ;
#6053=CARTESIAN_POINT ( 'NONE',  ( -7.151217271224854954, 106.7874940044571872, -3.587901469523285591 ) ) ;
#6095=CARTESIAN_POINT ( 'NONE',  ( -5.082755093536326818, -23.09375000204838457, 5.082755093536325042 ) ) ;
#6105=CARTESIAN_POINT ( 'NONE',  ( -7.188101187500000933, -15.50000000204838635, -2.977408999572651371 ) ) ;
#6113=CARTESIAN_POINT ( 'NONE',  ( -9.482945380845297478, 82.55666941221069521, 3.177595346755244243 ) ) ;
#6116=CARTESIAN_POINT ( 'NONE',  ( 7.999999999999998224, -11.28125000409677092, 3.313708498984766493 ) ) ;
#6121=CARTESIAN_POINT ( 'NONE',  ( 4.898587196589412829E-16, -19.62499999999999289, -8.000000000000000000 ) ) ;
#6176=CARTESIAN_POINT ( 'NONE',  ( -7.188101187500001821, -20.00000000204838813, -2.977408999572651371 ) ) ;
#6177=CARTESIAN_POINT ( 'NONE',  ( 8.000000000000000000, -20.18750000409677270, 0.000000000000000000 ) ) ;
#6205=VERTEX_POINT ( 'NONE', #2548 ) ;
#6232=CARTESIAN_POINT ( 'NONE',  ( -2.977408999572654480, -28.62500000204838813, 7.188101187499999156 ) ) ;
#6237=CARTESIAN_POINT ( 'NONE',  ( 7.999999999999998224, -30.78125000409677625, 3.313708498984766493 ) ) ;
#6259=CARTESIAN_POINT ( 'NONE',  ( -9.373884331924891455, 15.95332971149351842, 3.487646406148589229 ) ) ;
#6297=ADVANCED_FACE ( 'NONE', ( #53235 ), #43546, .F. ) ;
#6302=DIRECTION ( 'NONE',  ( 1.000000000000000000, -0.000000000000000000, -0.000000000000000000 ) ) ;
#6358=CARTESIAN_POINT ( 'NONE',  ( 3.313708498984762052, -15.21874999999999289, -8.000000000000000000 ) ) ;
#6379=( BOUNDED_CURVE ( )  B_SPLINE_CURVE ( 2, ( #43883, #19133, #84883, #10970, #86508, #88078, #4495, #22832, #95113 ),
 .UNSPECIFIED., .F., .F. ) 
 B_SPLINE_CURVE_WITH_KNOTS ( ( 3, 2, 2, 2, 3 ),
 ( 0.3970588235294117418, 0.4044117647058823595, 0.4117647058823529216, 0.4191176470588235947, 0.4264705882352941568 ),
 .UNSPECIFIED. ) 
 CURVE ( )  GEOMETRIC_REPRESENTATION_ITEM ( )  RATIONAL_B_SPLINE_CURVE ( ( 1.000000000000000000, 0.9238795325112867385, 1.000000000000000000, 0.9238795325112867385, 1.000000000000000000, 0.9238795325112867385, 1.000000000000000000, 0.9238795325112861834, 1.000000000000000666 ) ) 
 REPRESENTATION_ITEM ( '' )  );
#6397=AXIS2_PLACEMENT_3D ( 'NONE', #77350, #9942, #68189 ) ;
#6486=CARTESIAN_POINT ( 'NONE',  ( -7.213352437320217803, 27.98163526992318495, -3.463014597543478068 ) ) ;
#6493=CARTESIAN_POINT ( 'NONE',  ( -3.313708498984760720, -34.53125000000000000, -8.000000000000000000 ) ) ;
#6516=CARTESIAN_POINT ( 'NONE',  ( 7.188101187499999156, -22.25000000204839168, 2.977408999572654924 ) ) ;
#6564=ORIENTED_EDGE ( 'NONE', *, *, #25322, .T. ) ;
#6566=CARTESIAN_POINT ( 'NONE',  ( 5.082755093536325930, -19.34375000204838457, -5.082755093536325042 ) ) ;
#6571=CARTESIAN_POINT ( 'NONE',  ( 4.898587196589412829E-16, -27.31250000409677270, -8.000000000000000000 ) ) ;
#6577=CARTESIAN_POINT ( 'NONE',  ( -7.188101187500001821, -26.37500000204838457, -2.977408999572651371 ) ) ;
#6603=DIRECTION ( 'NONE',  ( -0.000000000000000000, -1.000000000000000000, -0.000000000000000000 ) ) ;
#6607=CARTESIAN_POINT ( 'NONE',  ( 0.000000000000000000, 115.0000000000000000, 0.000000000000000000 ) ) ;
#6625=CARTESIAN_POINT ( 'NONE',  ( 7.188101187499999156, -22.62500000204838813, 2.977408999572654924 ) ) ;
#6640=CARTESIAN_POINT ( 'NONE',  ( 7.188101187500000044, -10.15625000204838457, 0.000000000000000000 ) ) ;
#6641=CARTESIAN_POINT ( 'NONE',  ( 7.151217271224853178, 28.21250599554285543, -3.587901469523288700 ) ) ;
#6652=CARTESIAN_POINT ( 'NONE',  ( 5.656854249492378806, -12.87500000409676915, 5.656854249492381470 ) ) ;
#6654=CARTESIAN_POINT ( 'NONE',  ( 9.999999999999953815, 15.00000000000004974, 1.544939622598893836 ) ) ;
#6658=CARTESIAN_POINT ( 'NONE',  ( -8.000000000000001776, -16.15624999999999289, 3.313708498984759387 ) ) ;
#6662=ORIENTED_EDGE ( 'NONE', *, *, #100036, .T. ) ;
#6664=SURFACE_STYLE_USAGE ( .BOTH. , #102717 ) ;
#6717=CARTESIAN_POINT ( 'NONE',  ( 2.977408999572650927, -20.37500000204838457, -7.188101187500001821 ) ) ;
#6720=CARTESIAN_POINT ( 'NONE',  ( 9.176645556628256983, 84.47260967593273051, 3.973966573947710135 ) ) ;
#6775=EDGE_LOOP ( 'NONE', ( #89563, #104379, #6662 ) ) ;
#6781=EDGE_CURVE ( 'NONE', #1839, #56748, #93987, .T. ) ;
#6782=CARTESIAN_POINT ( 'NONE',  ( 5.656854249492378806, -30.87500000409677625, 5.656854249492381470 ) ) ;
#6831=ADVANCED_FACE ( 'NONE', ( #96227 ), #95918, .F. ) ;
#6851=VECTOR ( 'NONE', #101786, 1000.000000000000000 ) ;
#6902=CARTESIAN_POINT ( 'NONE',  ( 8.000000000000000000, -15.40624999999999467, -3.313708498984761608 ) ) ;
#6928=CARTESIAN_POINT ( 'NONE',  ( 9.090909090909086387, 16.00000000000000000, -4.165977904505313134 ) ) ;
#6949=CARTESIAN_POINT ( 'NONE',  ( -10.00000000000000178, 15.00000000000000000, 1.734723475976807489E-15 ) ) ;
#7011=( BOUNDED_CURVE ( )  B_SPLINE_CURVE ( 2, ( #14731, #49223, #41677, #65427, #97253, #32015, #106394, #64891, #81574 ),
 .UNSPECIFIED., .F., .F. ) 
 B_SPLINE_CURVE_WITH_KNOTS ( ( 3, 2, 2, 2, 3 ),
 ( 0.6029411764705883137, 0.6102941176470589868, 0.6176470588235295489, 0.6250000000000001110, 0.6323529411764706731 ),
 .UNSPECIFIED. ) 
 CURVE ( )  GEOMETRIC_REPRESENTATION_ITEM ( )  RATIONAL_B_SPLINE_CURVE ( ( 0.9999999999999988898, 0.9238795325112878487, 1.000000000000000000, 0.9238795325112867385, 1.000000000000000000, 0.9238795325112867385, 1.000000000000000000, 0.9238795325112856283, 1.000000000000001110 ) ) 
 REPRESENTATION_ITEM ( '' )  );
#7019=CARTESIAN_POINT ( 'NONE',  ( -7.619135598915494967, 26.82694632215321207, 2.449260492474797157 ) ) ;
#7027=CARTESIAN_POINT ( 'NONE',  ( -8.000000000000001776, -34.15624999999999289, 3.313708498984758943 ) ) ;
#7046=CIRCLE ( 'NONE', #105225, 1.000000000000000444 ) ;
#7051=CARTESIAN_POINT ( 'NONE',  ( -7.188101187500001821, -14.00000000204838457, -2.977408999572651371 ) ) ;
#7102=CARTESIAN_POINT ( 'NONE',  ( 7.188101187500000933, -11.93750000204838635, -2.977408999572650483 ) ) ;
#7111=CARTESIAN_POINT ( 'NONE',  ( 7.188101187500001821, -26.93750000204838457, -2.977408999572650483 ) ) ;
#7151=CARTESIAN_POINT ( 'NONE',  ( 9.536842176398144133, 27.35764630116009855, 3.014135744008177298 ) ) ;
#7152=CARTESIAN_POINT ( 'NONE',  ( 2.977408999572650927, -28.25000000204838813, -7.188101187500001821 ) ) ;
#7158=ORIENTED_EDGE ( 'NONE', *, *, #85792, .T. ) ;
#7165=CARTESIAN_POINT ( 'NONE',  ( -5.082755093536325042, -14.09375000204838457, -5.082755093536325930 ) ) ;
#7166=CARTESIAN_POINT ( 'NONE',  ( 7.800703710507055355, 26.41404307342058644, 1.791736796405272170 ) ) ;
#7178=CARTESIAN_POINT ( 'NONE',  ( 8.000000000000000000, -14.18750000409677092, 0.000000000000000000 ) ) ;
#7188=CARTESIAN_POINT ( 'NONE',  ( -3.836411046841926797, 15.00000000000001066, 9.999999999999959144 ) ) ;
#7234=LINE ( 'NONE', #29961, #16499 ) ;
#7237=FACE_BOUND ( 'NONE', #63202, .T. ) ;
#7238=CARTESIAN_POINT ( 'NONE',  ( -5.082755093536326818, -21.21875000204838457, 5.082755093536325042 ) ) ;
#7240=CARTESIAN_POINT ( 'NONE',  ( 9.536842176398147686, 82.35764630116013052, 3.014135744008184847 ) ) ;
#7269=EDGE_LOOP ( 'NONE', ( #58893, #51042 ) ) ;
#7298=CARTESIAN_POINT ( 'NONE',  ( -3.313708498984765161, -29.65625000409676915, 7.999999999999998224 ) ) ;
#7302=CARTESIAN_POINT ( 'NONE',  ( 9.918512371096300129, 33.79282992270550068, -1.297150762882706143 ) ) ;
#7305=( LENGTH_UNIT ( ) NAMED_UNIT ( * ) SI_UNIT ( .MILLI., .METRE. ) );
#7309=MECHANICAL_DESIGN_GEOMETRIC_PRESENTATION_REPRESENTATION('',(#81364),#93502);
#7321=CARTESIAN_POINT ( 'NONE',  ( -9.341953373613074874, 15.21714514899110071, 3.572352985695586902 ) ) ;
#7322=UNCERTAINTY_MEASURE_WITH_UNIT (LENGTH_MEASURE( 1.000000000000000082E-05 ), #97941, 'distance_accuracy_value', 'NONE');
#7329=CARTESIAN_POINT ( 'NONE',  ( 4.898587196589412829E-16, -12.12499999999999289, -8.000000000000000000 ) ) ;
#7331=ADVANCED_FACE ( 'NONE', ( #28473 ), #56802, .F. ) ;
#7350=CARTESIAN_POINT ( 'NONE',  ( -3.888805312026751615, -29.99999999999997868, 6.385547335617978604 ) ) ;
#7394=CARTESIAN_POINT ( 'NONE',  ( 7.934914944860278041, 101.1315435279989003, -1.051261972695691771 ) ) ;
#7395=EDGE_LOOP ( 'NONE', ( #81045, #96428 ) ) ;
#7403=CARTESIAN_POINT ( 'NONE',  ( 9.999952458099484076, 108.9998811452386462, 0.2653554233229081238 ) ) ;
#7422=CARTESIAN_POINT ( 'NONE',  ( -3.313708498984760720, -13.53124999999999289, -8.000000000000000000 ) ) ;
#7445=CARTESIAN_POINT ( 'NONE',  ( 9.999999999999998224, 15.00000000000000000, -2.283746462400398747E-15 ) ) ;
#7449=VERTEX_POINT ( 'NONE', #40233 ) ;
#7483=CARTESIAN_POINT ( 'NONE',  ( -9.373884331924879021, 15.95332971149351842, -3.487646406148622980 ) ) ;
#7485=CARTESIAN_POINT ( 'NONE',  ( 5.082755093536325930, -32.46875000204838813, -5.082755093536325042 ) ) ;
#7517=ORIENTED_EDGE ( 'NONE', *, *, #60368, .F. ) ;
#7547=CARTESIAN_POINT ( 'NONE',  ( 3.313708498984762496, -30.78124999999999289, 7.999999999999998224 ) ) ;
#7570=CARTESIAN_POINT ( 'NONE',  ( -2.977408999572650039, -15.68750000204838457, -7.188101187500001821 ) ) ;
#7621=CARTESIAN_POINT ( 'NONE',  ( 5.082755093536325930, -11.84375000204838635, -5.082755093536325042 ) ) ;
#7625=ORIENTED_EDGE ( 'NONE', *, *, #84601, .F. ) ;
#7630=CARTESIAN_POINT ( 'NONE',  ( 4.401442555609581635E-16, -28.15625000204838813, -7.188101187500000044 ) ) ;
#7633=( BOUNDED_CURVE ( )  B_SPLINE_CURVE ( 1, ( #18672, #33780 ),
 .UNSPECIFIED., .F., .T. ) 
 B_SPLINE_CURVE_WITH_KNOTS ( ( 2, 2 ),
 ( 0.000000000000000000, 1.000000000000000000 ),
 .UNSPECIFIED. ) 
 CURVE ( )  GEOMETRIC_REPRESENTATION_ITEM ( )  RATIONAL_B_SPLINE_CURVE ( ( 0.9660719911230173373, 0.9660719911230173373 ) ) 
 REPRESENTATION_ITEM ( '' )  );
#7648=CARTESIAN_POINT ( 'NONE',  ( -7.896165657598944065, 88.78911131371972942, -1.307894402814553825 ) ) ;
#7672=CARTESIAN_POINT ( 'NONE',  ( 5.082755093536325930, -23.84375000204838457, -5.082755093536325042 ) ) ;
#7692=CARTESIAN_POINT ( 'NONE',  ( 4.401442555609581635E-16, -12.78125000204838280, -7.188101187500000044 ) ) ;
#7693=CARTESIAN_POINT ( 'NONE',  ( 7.619701877737481865, 26.82557840467232424, -2.447562251315978266 ) ) ;
#7704=CARTESIAN_POINT ( 'NONE',  ( 5.082755093536324154, -29.84375000204838813, 5.082755093536326818 ) ) ;
#7714=CARTESIAN_POINT ( 'NONE',  ( -4.582575694955839829, 15.00000000000000000, 9.999999999999998224 ) ) ;
#7724=CARTESIAN_POINT ( 'NONE',  ( 9.999999999999996447, 15.00000000000000000, -10.00000000000000000 ) ) ;
#7756=CARTESIAN_POINT ( 'NONE',  ( 7.413471587080149305, 87.64352159168325329, -3.013058070223553209 ) ) ;
#7758=AXIS2_PLACEMENT_3D ( 'NONE', #51567, #846, #93100 ) ;
#7768=CYLINDRICAL_SURFACE ( 'NONE', #100058, 8.000000000000000000 ) ;
#7769=CARTESIAN_POINT ( 'NONE',  ( 5.082755093536325930, -20.46875000204838813, -5.082755093536325042 ) ) ;
#7771=CARTESIAN_POINT ( 'NONE',  ( 9.253583916535173870, 83.70196091994968413, 3.792462592445555725 ) ) ;
#7774=CARTESIAN_POINT ( 'NONE',  ( -5.656854249492381470, -13.25000000409676915, 5.656854249492379694 ) ) ;
#7791=CARTESIAN_POINT ( 'NONE',  ( -1.469576158976823947E-15, -13.06250000409676915, 8.000000000000000000 ) ) ;
#7799=ORIENTED_EDGE ( 'NONE', *, *, #71051, .T. ) ;
#7820=EDGE_CURVE ( 'NONE', #1287, #103615, #5171, .T. ) ;
#7831=CARTESIAN_POINT ( 'NONE',  ( 7.999999999999998224, -24.78125000409677270, 3.313708498984766493 ) ) ;
#7840=CARTESIAN_POINT ( 'NONE',  ( -3.487646406147736133, 15.95332971149351842, -9.373884331925221858 ) ) ;
#7847=B_SPLINE_CURVE_WITH_KNOTS ( 'NONE', 3,
 ( #6949, #30740, #89480, #96515, #48989, #80299, #39867, #63080, #98088, #72739 ),
 .UNSPECIFIED., .F., .F.,
 ( 4, 2, 2, 2, 4 ),
 ( -2.000195913693996610E-05, 0.001085800244612921545, 0.002191602448362782625, 0.003297404652112645440, 0.004403206855862508255 ),
 .UNSPECIFIED. ) ;
#7879=CARTESIAN_POINT ( 'NONE',  ( -6.638433539294970487, -30.00000000000000711, 3.894772332383715785 ) ) ;
#7911=SURFACE_STYLE_FILL_AREA ( #81787 ) ;
#7919=ORIENTED_EDGE ( 'NONE', *, *, #26509, .F. ) ;
#7928=CARTESIAN_POINT ( 'NONE',  ( 7.002619243997876275, 103.9499268198618154, -3.868708944013000028 ) ) ;
#7936=ORIENTED_EDGE ( 'NONE', *, *, #29499, .T. ) ;
#7939=VERTEX_POINT ( 'NONE', #57204 ) ;
#7946=CARTESIAN_POINT ( 'NONE',  ( -10.00000000000000000, 15.00000000000000000, 10.00000000000000000 ) ) ;
#7959=CARTESIAN_POINT ( 'NONE',  ( -3.313708498984765161, -11.46874999999999289, 7.999999999999998224 ) ) ;
#7961=CARTESIAN_POINT ( 'NONE',  ( -6.944031699373470090, 104.4653934544386971, 3.972913591453824278 ) ) ;
#7972=( BOUNDED_CURVE ( )  B_SPLINE_CURVE ( 2, ( #35728, #20631, #78788, #52933, #53975, #68605, #103606, #53471, #29757 ),
 .UNSPECIFIED., .F., .F. ) 
 B_SPLINE_CURVE_WITH_KNOTS ( ( 3, 2, 2, 2, 3 ),
 ( 0.5147058823529413463, 0.5220588235294120194, 0.5294117647058824705, 0.5367647058823530326, 0.5441176470588235947 ),
 .UNSPECIFIED. ) 
 CURVE ( )  GEOMETRIC_REPRESENTATION_ITEM ( )  RATIONAL_B_SPLINE_CURVE ( ( 0.9999999999999976685, 0.9238795325112890700, 1.000000000000000000, 0.9238795325112867385, 1.000000000000000000, 0.9238795325112867385, 1.000000000000000000, 0.9238795325112856283, 1.000000000000001110 ) ) 
 REPRESENTATION_ITEM ( '' )  );
#8003=CARTESIAN_POINT ( 'NONE',  ( -8.000000000000000000, -29.74999999999999645, -9.797174393178825657E-16 ) ) ;
#8024=CARTESIAN_POINT ( 'NONE',  ( 2.977408999572650927, -32.37500000204838813, -7.188101187500001821 ) ) ;
#8033=PRODUCT_DEFINITION ( 'UNKNOWN', '', #50753, #33814 ) ;
#8085=CARTESIAN_POINT ( 'NONE',  ( 4.898587196589412829E-16, -15.31250000409677092, -8.000000000000000000 ) ) ;
#8091=CARTESIAN_POINT ( 'NONE',  ( 8.000000000000000000, -34.90625000000000000, -3.313708498984761608 ) ) ;
#8111=CARTESIAN_POINT ( 'NONE',  ( -5.082755093536326818, -13.71875000204838457, 5.082755093536325042 ) ) ;
#8150=STYLED_ITEM ( 'NONE', ( #88848 ), #8942 ) ;
#8170=CARTESIAN_POINT ( 'NONE',  ( -5.082755093536326818, -14.09375000204838457, 5.082755093536325042 ) ) ;
#8179=CARTESIAN_POINT ( 'NONE',  ( 2.977408999572650927, -25.25000000204839523, -7.188101187500001821 ) ) ;
#8196=ORIENTED_EDGE ( 'NONE', *, *, #5359, .T. ) ;
#8220=CARTESIAN_POINT ( 'NONE',  ( 2.977408999572651815, -27.31250000204838457, 7.188101187500000933 ) ) ;
#8233=CARTESIAN_POINT ( 'NONE',  ( 2.977408999572650927, -11.37500000204838635, -7.188101187500000933 ) ) ;
#8234=CARTESIAN_POINT ( 'NONE',  ( 7.002619243997879828, 28.94992681986182248, -3.868708944012997808 ) ) ;
#8244=CARTESIAN_POINT ( 'NONE',  ( 7.188101187499999156, -31.25000000204838813, 2.977408999572654924 ) ) ;
#8283=ORIENTED_EDGE ( 'NONE', *, *, #52147, .F. ) ;
#8294=CARTESIAN_POINT ( 'NONE',  ( 7.619135598915500296, 88.17305367784679504, 2.449260492474792716 ) ) ;
#8305=CARTESIAN_POINT ( 'NONE',  ( -1.320432766682874540E-15, -19.53125000204838457, 7.188101187500000044 ) ) ;
#8339=B_SPLINE_CURVE_WITH_KNOTS ( 'NONE', 3,
 ( #23621, #56474, #74258, #7928, #99053, #90999, #72667, #97464, #89403, #31707, #106085, #105568, #74785, #81277, #7394, #81801, #335, #98534, #33842, #73178, #32233, #98008, #17110, #25220, #58074, #24162, #864, #82892, #57007, #89922, #66715, #8990, #23087, #55922 ),
 .UNSPECIFIED., .F., .F.,
 ( 4, 2, 2, 2, 2, 2, 2, 2, 2, 2, 2, 2, 2, 2, 2, 2, 4 ),
 ( 0.000000000000000000, 0.0007951492273476391814, 0.001590298454695278363, 0.002385447682042917544, 0.003180596909390556726, 0.003975746136738195907, 0.004770895364085835089, 0.005566044591433473403, 0.006361193818781111717, 0.007156343046128750031, 0.007951492273476388345, 0.008746641500824025792, 0.009541790728171663238, 0.01033693995551930069, 0.01113208918286693987, 0.01192723841021457558, 0.01272238763756221476 ),
 .UNSPECIFIED. ) ;
#8365=ADVANCED_FACE ( 'NONE', ( #13437 ), #21576, .F. ) ;
#8371=CARTESIAN_POINT ( 'NONE',  ( -3.313708498984760720, -22.71875000409677270, -8.000000000000000000 ) ) ;
#8377=CARTESIAN_POINT ( 'NONE',  ( -1.005505455502474499, -29.99999999999999645, -7.776392279229293436 ) ) ;
#8400=ORIENTED_EDGE ( 'NONE', *, *, #53247, .T. ) ;
#8420=CARTESIAN_POINT ( 'NONE',  ( -4.160433058848811427, -29.99999999999997513, 6.232720532359338428 ) ) ;
#8429=CARTESIAN_POINT ( 'NONE',  ( -5.656854249492381470, -22.06249999999999289, 5.656854249492379694 ) ) ;
#8476=CARTESIAN_POINT ( 'NONE',  ( 9.381394091586567896, 107.0134960558160628, 3.465950112474264433 ) ) ;
#8488=EDGE_CURVE ( 'NONE', #18153, #57343, #96834, .T. ) ;
#8496=CARTESIAN_POINT ( 'NONE',  ( -8.000000000000000000, -10.24999999999999112, -9.797174393178825657E-16 ) ) ;
#8561=CARTESIAN_POINT ( 'NONE',  ( 2.977408999572651815, -28.43750000204839168, 7.188101187500000933 ) ) ;
#8580=LINE ( 'NONE', #32890, #66288 ) ;
#8621=CARTESIAN_POINT ( 'NONE',  ( 7.999999999999998224, -24.59374999999999289, 3.313708498984766493 ) ) ;
#8647=CARTESIAN_POINT ( 'NONE',  ( 7.188101187500001821, -16.06250000204838457, -2.977408999572650483 ) ) ;
#8683=CARTESIAN_POINT ( 'NONE',  ( -10.00000000000000355, 85.00000000000000000, -4.000000000000000000 ) ) ;
#8701=CARTESIAN_POINT ( 'NONE',  ( 7.188101187500000044, -10.53125000204838457, 0.000000000000000000 ) ) ;
#8709=CARTESIAN_POINT ( 'NONE',  ( -5.082755093536326818, -21.59375000204838457, 5.082755093536325042 ) ) ;
#8741=ORIENTED_EDGE ( 'NONE', *, *, #16783, .F. ) ;
#8749=CARTESIAN_POINT ( 'NONE',  ( 5.082755093536325930, -19.34375000204838457, -5.082755093536325042 ) ) ;
#8760=CARTESIAN_POINT ( 'NONE',  ( 9.221216839714873714, 86.04759748168980593, 3.869414262756989853 ) ) ;
#8777=CARTESIAN_POINT ( 'NONE',  ( -7.188101187500000044, -30.40625000204838813, -8.802885111219163269E-16 ) ) ;
#8807=EDGE_CURVE ( 'NONE', #50100, #53546, #67223, .T. ) ;
#8822=AXIS2_PLACEMENT_3D ( 'NONE', #39201, #54273, #79109 ) ;
#8826=CARTESIAN_POINT ( 'NONE',  ( 7.896254658894418021, 88.78929182754201577, 1.307282859663297936 ) ) ;
#8834=CARTESIAN_POINT ( 'NONE',  ( -1.320432766682874540E-15, -10.53125000204838457, 7.188101187500000044 ) ) ;
#8870=CARTESIAN_POINT ( 'NONE',  ( 4.898587196589412829E-16, -10.62499999999999289, -8.000000000000000000 ) ) ;
#8890=CARTESIAN_POINT ( 'NONE',  ( -5.082755093536326818, -22.71875000204838457, 5.082755093536325042 ) ) ;
#8899=CARTESIAN_POINT ( 'NONE',  ( -8.000000000000000000, -23.93750000409677270, -9.797174393178825657E-16 ) ) ;
#8904=CARTESIAN_POINT ( 'NONE',  ( 9.333555687487613994, 31.78102696608970490, 3.591168747312691423 ) ) ;
#8916=CARTESIAN_POINT ( 'NONE',  ( 5.656854249492378806, -15.87500000409677092, 5.656854249492381470 ) ) ;
#8928=CARTESIAN_POINT ( 'NONE',  ( -1.469576158976823947E-15, -12.87499999999999467, 8.000000000000000000 ) ) ;
#8942=ADVANCED_FACE ( 'NONE', ( #48372 ), #70151, .F. ) ;
#8948=FACE_OUTER_BOUND ( 'NONE', #65687, .T. ) ;
#8990=CARTESIAN_POINT ( 'NONE',  ( 6.943482370013978944, 104.4715162973927534, 3.973876482044368164 ) ) ;
#9003=CARTESIAN_POINT ( 'NONE',  ( 9.646032546913144046, 108.0128032847436401, 2.644051433538247231 ) ) ;
#9031=FACE_OUTER_BOUND ( 'NONE', #58296, .T. ) ;
#9033=CARTESIAN_POINT ( 'NONE',  ( 8.000000000000000000, -18.40624999999999289, -3.313708498984761164 ) ) ;
#9054=CARTESIAN_POINT ( 'NONE',  ( -8.000113193197767814, 80.99977361354139305, -0.2613481123984612853 ) ) ;
#9072=CARTESIAN_POINT ( 'NONE',  ( 0.000000000000000000, 15.00000000000000000, 0.000000000000000000 ) ) ;
#9075=ORIENTED_EDGE ( 'NONE', *, *, #30298, .T. ) ;
#9086=CARTESIAN_POINT ( 'NONE',  ( -7.188101187500001821, -32.00000000204838813, -2.977408999572651371 ) ) ;
#9142=DIRECTION ( 'NONE',  ( -1.000000000000000000, -0.000000000000000000, -0.000000000000000000 ) ) ;
#9143=CARTESIAN_POINT ( 'NONE',  ( -8.000000000000001776, -26.65624999999999645, 3.313708498984758943 ) ) ;
#9151=CARTESIAN_POINT ( 'NONE',  ( -5.656854249492379694, -9.125000004096769146, -5.656854249492380582 ) ) ;
#9164=CARTESIAN_POINT ( 'NONE',  ( -9.698972129396508990, 88.17629712741940295, -2.445345647270319667 ) ) ;
#9165=CARTESIAN_POINT ( 'NONE',  ( -7.188101187500002709, -10.81250000204838457, 2.977408999572648707 ) ) ;
#9222=CARTESIAN_POINT ( 'NONE',  ( -7.188101187500002709, -15.68750000204838635, 2.977408999572647819 ) ) ;
#9232=CARTESIAN_POINT ( 'NONE',  ( -2.977408999572654480, -20.00000000204838813, 7.188101187499999156 ) ) ;
#9247=CARTESIAN_POINT ( 'NONE',  ( -7.046289519167721060, 86.30591819944379495, -3.789821819998813623 ) ) ;
#9266=VECTOR ( 'NONE', #31864, 1000.000000000000000 ) ;
#9272=CARTESIAN_POINT ( 'NONE',  ( 9.918579450955565591, 26.20696087031312160, 1.297207292923859834 ) ) ;
#9274=CARTESIAN_POINT ( 'NONE',  ( 7.188101187500000044, -16.53125000204838813, 0.000000000000000000 ) ) ;
#9291=UNCERTAINTY_MEASURE_WITH_UNIT (LENGTH_MEASURE( 1.000000000000000082E-05 ), #43931, 'distance_accuracy_value', 'NONE');
#9296=CARTESIAN_POINT ( 'NONE',  ( 7.188101187500001821, -32.56250000204838813, -2.977408999572650483 ) ) ;
#9307=ORIENTED_EDGE ( 'NONE', *, *, #91001, .F. ) ;
#9351=CARTESIAN_POINT ( 'NONE',  ( 5.082755093536324154, -13.34375000204838457, 5.082755093536326818 ) ) ;
#9384=CARTESIAN_POINT ( 'NONE',  ( -1.469576158976823947E-15, -11.37499999999999289, 8.000000000000000000 ) ) ;
#9404=CARTESIAN_POINT ( 'NONE',  ( -7.188101187500000044, -27.40625000204838813, -8.802885111219163269E-16 ) ) ;
#9415=CARTESIAN_POINT ( 'NONE',  ( 8.000000000000000000, -23.09375000409676915, -3.313708498984761608 ) ) ;
#9423=CARTESIAN_POINT ( 'NONE',  ( -1.404490565848831141, 15.46725112412266512, -9.926810856659471938 ) ) ;
#9441=VECTOR ( 'NONE', #17095, 1000.000000000000000 ) ;
#9463=CARTESIAN_POINT ( 'NONE',  ( -7.551437640244099470, 33.00872462522908535, -2.648272645923380519 ) ) ;
#9482=CARTESIAN_POINT ( 'NONE',  ( 1.404490565848997230, 15.46725112412266512, 9.926810856659436411 ) ) ;
#9603=ORIENTED_EDGE ( 'NONE', *, *, #27926, .F. ) ;
#9625=CARTESIAN_POINT ( 'NONE',  ( -5.656854249492379694, -13.43749999999999112, -5.656854249492380582 ) ) ;
#9628=ORIENTED_EDGE ( 'NONE', *, *, #88665, .T. ) ;
#9661=ADVANCED_FACE ( 'NONE', ( #43756 ), #68588, .F. ) ;
#9669=CARTESIAN_POINT ( 'NONE',  ( -5.656854249492381470, -29.56249999999999645, 5.656854249492379694 ) ) ;
#9680=CARTESIAN_POINT ( 'NONE',  ( -4.912113277822308000, -8.720202683089764761, 6.401595221162452276 ) ) ;
#9682=CARTESIAN_POINT ( 'NONE',  ( -8.000000000000000000, -32.93750000409677625, -9.797174393178825657E-16 ) ) ;
#9686=CARTESIAN_POINT ( 'NONE',  ( 0.000000000000000000, -30.00000000000000000, 0.000000000000000000 ) ) ;
#9699=CARTESIAN_POINT ( 'NONE',  ( -5.082755093536326818, -9.218750002048382797, 5.082755093536325042 ) ) ;
#9761=CARTESIAN_POINT ( 'NONE',  ( -2.977408999572650039, -20.56250000204838457, -7.188101187500001821 ) ) ;
#9777=CARTESIAN_POINT ( 'NONE',  ( -6.928203230275510549, 85.26930929695539874, -4.000000000000000000 ) ) ;
#9785=CARTESIAN_POINT ( 'NONE',  ( 9.907647895771711788, 15.45478884909084094, -1.400734872026643929 ) ) ;
#9794=VERTEX_POINT ( 'NONE', #89926 ) ;
#9801=CARTESIAN_POINT ( 'NONE',  ( -2.977408999572654480, -20.00000000204838813, 7.188101187499999156 ) ) ;
#9805=DIRECTION ( 'NONE',  ( 0.000000000000000000, -0.000000000000000000, 1.000000000000000000 ) ) ;
#9829=CARTESIAN_POINT ( 'NONE',  ( -1.320432766682874540E-15, -31.53125000204838457, 7.188101187500000044 ) ) ;
#9841=MECHANICAL_DESIGN_GEOMETRIC_PRESENTATION_REPRESENTATION('',(#8150),#104628);
#9894=CARTESIAN_POINT ( 'NONE',  ( 2.977408999572651815, -14.93750000204838457, 7.188101187500000933 ) ) ;
#9921=ORIENTED_EDGE ( 'NONE', *, *, #72350, .F. ) ;
#9942=DIRECTION ( 'NONE',  ( 1.000000000000000000, 0.000000000000000000, -1.734723475976807094E-16 ) ) ;
#9956=CARTESIAN_POINT ( 'NONE',  ( -2.977408999572654480, -27.12500000204838457, 7.188101187499999156 ) ) ;
#9967=CARTESIAN_POINT ( 'NONE',  ( -8.000000000000001776, -22.34375000409677625, 3.313708498984758943 ) ) ;
#9976=CARTESIAN_POINT ( 'NONE',  ( -3.316968746323984085, 15.92795519102023860, -9.435590127033053776 ) ) ;
#9997=B_SPLINE_CURVE_WITH_KNOTS ( 'NONE', 3,
 ( #95614, #54064, #61132, #54592, #70809, #6053, #46528, #53563, #69751, #69235, #3954, #94023, #13080, #71328, #53035, #61686, #102104, #62216, #95100, #20184, #21235, #85956, #12029, #44959, #77841, #78888, #105816, #72905, #81002, #82067, #23336, #64319, #71853, #48100 ),
 .UNSPECIFIED., .F., .F.,
 ( 4, 2, 2, 2, 2, 2, 2, 2, 2, 2, 2, 2, 2, 2, 2, 2, 4 ),
 ( 0.000000000000000000, 0.0007951492273476395067, 0.001590298454695279013, 0.002385447682042918845, 0.003180596909390558027, 0.003975746136738197642, 0.004770895364085837691, 0.005566044591433476005, 0.006361193818781115186, 0.007156343046128753500, 0.007951492273476390080, 0.008746641500824029261, 0.009541790728171666708, 0.01033693995551930589, 0.01113208918286694334, 0.01192723841021458078, 0.01272238763756221823 ),
 .UNSPECIFIED. ) ;
#10097=AXIS2_PLACEMENT_3D ( 'NONE', #28330, #68229, #75780 ) ;
#10129=CARTESIAN_POINT ( 'NONE',  ( -9.989435848181784650, 108.9738029252842466, -0.5278651953176012324 ) ) ;
#10213=CARTESIAN_POINT ( 'NONE',  ( -5.656854249492379694, -26.93749999999999645, -5.656854249492380582 ) ) ;
#10223=ORIENTED_EDGE ( 'NONE', *, *, #68061, .F. ) ;
#10226=CYLINDRICAL_SURFACE ( 'NONE', #83079, 8.000000000000000000 ) ;
#10234=CARTESIAN_POINT ( 'NONE',  ( 7.986711519608433285, 108.9736190362343535, -0.5300249774147602899 ) ) ;
#10256=FACE_OUTER_BOUND ( 'NONE', #64104, .T. ) ;
#10276=ADVANCED_FACE ( 'NONE', ( #105966 ), #90869, .F. ) ;
#10293=CARTESIAN_POINT ( 'NONE',  ( 5.082755093536325930, -10.34375000204838457, -5.082755093536325042 ) ) ;
#10300=CARTESIAN_POINT ( 'NONE',  ( -5.082755093536326818, -20.09375000204838457, 5.082755093536325042 ) ) ;
#10312=CARTESIAN_POINT ( 'NONE',  ( 5.656854249492380582, -13.81249999999999112, -5.656854249492379694 ) ) ;
#10317=ORIENTED_EDGE ( 'NONE', *, *, #56340, .T. ) ;
#10332=ADVANCED_FACE ( 'NONE', ( #66586 ), #25640, .T. ) ;
#10340=CARTESIAN_POINT ( 'NONE',  ( 7.188101187500001821, -17.93750000204838457, -2.977408999572650483 ) ) ;
#10344=CARTESIAN_POINT ( 'NONE',  ( -5.656854249492379694, -12.12500000409676915, -5.656854249492380582 ) ) ;
#10358=EDGE_CURVE ( 'NONE', #101925, #28968, #97934, .T. ) ;
#10366=CARTESIAN_POINT ( 'NONE',  ( 7.188101187499999156, -28.25000000204838813, 2.977408999572654924 ) ) ;
#10371=EDGE_CURVE ( 'NONE', #3543, #32331, #16172, .T. ) ;
#10383=CARTESIAN_POINT ( 'NONE',  ( 9.999945253488242258, 101.0001368662946675, -0.2662901834230885223 ) ) ;
#10420=CARTESIAN_POINT ( 'NONE',  ( 7.188101187500000044, -27.03125000204838813, 0.000000000000000000 ) ) ;
#10427=CARTESIAN_POINT ( 'NONE',  ( -1.320432766682874540E-15, -13.53125000204838457, 7.188101187500000044 ) ) ;
#10462=CARTESIAN_POINT ( 'NONE',  ( 7.743982712349854580, 81.53786985239264595, 2.020119794285907044 ) ) ;
#10482=CARTESIAN_POINT ( 'NONE',  ( -5.082755093536326818, -24.21875000204838813, 5.082755093536325042 ) ) ;
#10489=FILL_AREA_STYLE ('',( #2397 ) ) ;
#10497=CARTESIAN_POINT ( 'NONE',  ( -5.656854249492379694, -15.12500000409677092, -5.656854249492380582 ) ) ;
#10598=ORIENTED_EDGE ( 'NONE', *, *, #100053, .F. ) ;
#10632=FACE_OUTER_BOUND ( 'NONE', #53528, .T. ) ;
#10646=CARTESIAN_POINT ( 'NONE',  ( -9.380894568449075877, 107.0113063311094237, -3.467341429141166831 ) ) ;
#10653=VERTEX_POINT ( 'NONE', #80499 ) ;
#10728=AXIS2_PLACEMENT_3D ( 'NONE', #14983, #57033, #47878 ) ;
#10735=CARTESIAN_POINT ( 'NONE',  ( -8.000000000000001776, -28.15625000000000000, 3.313708498984758943 ) ) ;
#10738=LINE ( 'NONE', #2652, #3593 ) ;
#10758=CARTESIAN_POINT ( 'NONE',  ( 5.082755093536324154, -10.34375000204838457, 5.082755093536326818 ) ) ;
#10818=CARTESIAN_POINT ( 'NONE',  ( -1.320432766682874540E-15, -12.40625000204838635, 7.188101187500000044 ) ) ;
#10861=CARTESIAN_POINT ( 'NONE',  ( 7.188101187500001821, -19.43750000204838457, -2.977408999572650483 ) ) ;
#10874=LINE ( 'NONE', #84792, #53755 ) ;
#10887=CARTESIAN_POINT ( 'NONE',  ( 5.082755093536325930, -27.96875000204838457, -5.082755093536325042 ) ) ;
#10896=EDGE_CURVE ( 'NONE', #97744, #80543, #37319, .T. ) ;
#10935=CARTESIAN_POINT ( 'NONE',  ( 7.188101187500000044, -25.53125000204838813, 0.000000000000000000 ) ) ;
#10945=CARTESIAN_POINT ( 'NONE',  ( 5.082755093536324154, -14.84375000204838457, 5.082755093536326818 ) ) ;
#10962=ORIENTED_EDGE ( 'NONE', *, *, #16553, .F. ) ;
#10970=CARTESIAN_POINT ( 'NONE',  ( 7.999999999999998224, -23.28125000409677270, 3.313708498984766049 ) ) ;
#10993=CARTESIAN_POINT ( 'NONE',  ( 7.188101187500000044, -34.53125000204838813, 0.000000000000000000 ) ) ;
#11005=ORIENTED_EDGE ( 'NONE', *, *, #67729, .F. ) ;
#11009=CARTESIAN_POINT ( 'NONE',  ( -7.188101187500002709, -24.31250000204838813, 2.977408999572647819 ) ) ;
#11019=CARTESIAN_POINT ( 'NONE',  ( -5.656854249492379694, -18.12500000409676915, -5.656854249492380582 ) ) ;
#11074=CARTESIAN_POINT ( 'NONE',  ( -7.188101187500001821, -30.50000000204838813, -2.977408999572651371 ) ) ;
#11077=CARTESIAN_POINT ( 'NONE',  ( 2.455962139888425710, 15.75268258782372754, 9.700350089084274430 ) ) ;
#11132=CARTESIAN_POINT ( 'NONE',  ( 9.797174393178825657E-16, -30.00000000000000000, -8.000000000000000000 ) ) ;
#11148=LINE ( 'NONE', #44077, #46336 ) ;
#11154=DIRECTION ( 'NONE',  ( 0.000000000000000000, 0.000000000000000000, -1.000000000000000000 ) ) ;
#11184=CARTESIAN_POINT ( 'NONE',  ( -8.000000000000000000, -23.93750000409677270, -9.797174393178825657E-16 ) ) ;
#11220=CARTESIAN_POINT ( 'NONE',  ( 9.165151389911679658, 85.00000000000000000, 4.000000000000000000 ) ) ;
#11237=VERTEX_POINT ( 'NONE', #103998 ) ;
#11263=CARTESIAN_POINT ( 'NONE',  ( -8.000000000000000000, -19.24999999999999289, -9.797174393178825657E-16 ) ) ;
#11285=EDGE_CURVE ( 'NONE', #35576, #70143, #105081, .T. ) ;
#11287=CARTESIAN_POINT ( 'NONE',  ( -7.188101187500000044, -9.406250002048384573, -8.802885111219163269E-16 ) ) ;
#11349=CARTESIAN_POINT ( 'NONE',  ( 4.401442555609581635E-16, -13.15625000204838280, -7.188101187500000044 ) ) ;
#11361=UNCERTAINTY_MEASURE_WITH_UNIT (LENGTH_MEASURE( 1.000000000000000082E-05 ), #68845, 'distance_accuracy_value', 'NONE');
#11366=CARTESIAN_POINT ( 'NONE',  ( -7.343637806710344051, 87.44363121900617841, 3.177475076494672201 ) ) ;
#11394=CARTESIAN_POINT ( 'NONE',  ( -7.188101187500000044, -12.78125000204838635, -8.802885111219163269E-16 ) ) ;
#11420=CARTESIAN_POINT ( 'NONE',  ( -7.188101187500002709, -25.81250000204838457, 2.977408999572648707 ) ) ;
#11439=CARTESIAN_POINT ( 'NONE',  ( 9.797537890442933772, 101.5344220233380810, 2.014215961808881072 ) ) ;
#11471=CARTESIAN_POINT ( 'NONE',  ( -7.188101187500000044, -23.28125000204838457, -8.802885111219163269E-16 ) ) ;
#11481=CARTESIAN_POINT ( 'NONE',  ( 7.188101187500001821, -29.93750000204839523, -2.977408999572650483 ) ) ;
#11541=CARTESIAN_POINT ( 'NONE',  ( 2.977408999572650927, -21.87500000204838813, -7.188101187500000933 ) ) ;
#11548=CARTESIAN_POINT ( 'NONE',  ( -9.253500431420428995, 83.70228450082292682, 3.792688295761951434 ) ) ;
#11550=CARTESIAN_POINT ( 'NONE',  ( -8.000000000000000000, -19.43750000409677270, -9.797174393178825657E-16 ) ) ;
#11612=CARTESIAN_POINT ( 'NONE',  ( -2.977408999572654480, -24.12500000204838457, 7.188101187499999156 ) ) ;
#11616=CARTESIAN_POINT ( 'NONE',  ( 3.082707893549380351, 15.00000000000000000, 9.999999999999998224 ) ) ;
#11644=CARTESIAN_POINT ( 'NONE',  ( 0.3498606326581470416, 15.11603512203462962, 10.00000000000000000 ) ) ;
#11682=CARTESIAN_POINT ( 'NONE',  ( 9.981531048852463783, 15.23280014800325688, 0.7018335428337066917 ) ) ;
#11692=ADVANCED_FACE ( 'NONE', ( #15485 ), #14941, .T. ) ;
#11734=EDGE_CURVE ( 'NONE', #94312, #93124, #81966, .T. ) ;
#11753=ORIENTED_EDGE ( 'NONE', *, *, #61575, .T. ) ;
#11802=CARTESIAN_POINT ( 'NONE',  ( -8.000000000000000000, -22.24999999999999289, -9.797174393178825657E-16 ) ) ;
#11818=ADVANCED_FACE ( 'NONE', ( #74770 ), #62979, .F. ) ;
#11830=CARTESIAN_POINT ( 'NONE',  ( 7.188101187500001821, -10.06250000204838280, -2.977408999572650483 ) ) ;
#11848=ORIENTED_EDGE ( 'NONE', *, *, #6781, .F. ) ;
#11858=CARTESIAN_POINT ( 'NONE',  ( -9.165151389911679658, 29.73704489083662494, 3.999999999999999112 ) ) ;
#11873=FILL_AREA_STYLE ('',( #27583 ) ) ;
#11878=CARTESIAN_POINT ( 'NONE',  ( -9.221346651730840449, 103.9516597993166158, -3.869102247876032852 ) ) ;
#11891=CARTESIAN_POINT ( 'NONE',  ( 5.656854249492378806, -18.87500000409677270, 5.656854249492381470 ) ) ;
#11897=CARTESIAN_POINT ( 'NONE',  ( -2.977408999572654480, -15.50000000204838635, 7.188101187499999156 ) ) ;
#11935=CARTESIAN_POINT ( 'NONE',  ( -2.977408999572654480, -12.50000000204838990, 7.188101187499999156 ) ) ;
#11940=CARTESIAN_POINT ( 'NONE',  ( 4.165977904505311358, 16.00000000000000000, -9.090909090909089940 ) ) ;
#11944=CARTESIAN_POINT ( 'NONE',  ( 9.797936955406315818, 88.46671689770482772, -2.012343231877592675 ) ) ;
#11960=ADVANCED_FACE ( 'NONE', ( #22434 ), #45627, .T. ) ;
#11962=CARTESIAN_POINT ( 'NONE',  ( 7.188101187500001821, -28.06250000204838813, -2.977408999572650483 ) ) ;
#11980=CARTESIAN_POINT ( 'NONE',  ( -8.000000000000000000, -22.53125000409677625, -3.313708498984762496 ) ) ;
#11981=CARTESIAN_POINT ( 'NONE',  ( 9.253583916535172094, 103.7019609199496557, 3.792462592445557945 ) ) ;
#12012=CARTESIAN_POINT ( 'NONE',  ( -2.977408999572654480, -26.00000000204839168, 7.188101187499999156 ) ) ;
#12022=CARTESIAN_POINT ( 'NONE',  ( 7.188101187500000044, -31.53125000204838457, 0.000000000000000000 ) ) ;
#12029=CARTESIAN_POINT ( 'NONE',  ( -7.743982712349853692, 108.4621301476073683, 2.020119794285910153 ) ) ;
#12064=CARTESIAN_POINT ( 'NONE',  ( -5.082755093536326818, -33.59375000204838813, 5.082755093536325042 ) ) ;
#12078=CARTESIAN_POINT ( 'NONE',  ( 2.977408999572650927, -17.37500000204838457, -7.188101187500000933 ) ) ;
#12083=B_SPLINE_CURVE_WITH_KNOTS ( 'NONE', 3,
 ( #47621, #80523, #82114, #8234, #97767, #6641, #57833, #108, #56776, #98825, #7693, #97244, #56227, #89165, #16325, #90760, #65945, #48680, #48153, #81052, #49756, #7166, #16876, #73487, #32007, #89699, #32547, #81564, #37606, #65419, #4674, #98314, #71913, #34144 ),
 .UNSPECIFIED., .F., .F.,
 ( 4, 2, 2, 2, 2, 2, 2, 2, 2, 2, 2, 2, 2, 2, 2, 2, 4 ),
 ( 3.576224061345498009E-18, 0.0007951492273476420004, 0.001590298454695280314, 0.002385447682042918845, 0.003180596909390557159, 0.003975746136738195040, 0.004770895364085834221, 0.005566044591433472535, 0.006361193818781110849, 0.007156343046128749164, 0.007951492273476386610, 0.008746641500824025792, 0.009541790728171664973, 0.01033693995551930242, 0.01113208918286694160, 0.01192723841021457905, 0.01272238763756221476 ),
 .UNSPECIFIED. ) ;
#12086=CARTESIAN_POINT ( 'NONE',  ( -9.699121749566360862, 81.82331239724180705, 2.444499528233564423 ) ) ;
#12088=CARTESIAN_POINT ( 'NONE',  ( 4.898587196589412829E-16, -18.31250000409676915, -8.000000000000000000 ) ) ;
#12090=CARTESIAN_POINT ( 'NONE',  ( 9.168149550321063046, 15.99999999372935022, 3.997425403567909541 ) ) ;
#12092=CARTESIAN_POINT ( 'NONE',  ( -9.537909130738276176, 87.64614830963394354, -3.010726932293856350 ) ) ;
#12106=ORIENTED_EDGE ( 'NONE', *, *, #82464, .T. ) ;
#12149=CARTESIAN_POINT ( 'NONE',  ( 5.082755093536324154, -26.84375000204838813, 5.082755093536326818 ) ) ;
#12159=ORIENTED_EDGE ( 'NONE', *, *, #85079, .F. ) ;
#12219=CARTESIAN_POINT ( 'NONE',  ( 9.999999999999998224, 15.00000000000000000, -1.734723475976806897E-15 ) ) ;
#12229=EDGE_CURVE ( 'NONE', #89525, #33789, #1009, .T. ) ;
#12248=CARTESIAN_POINT ( 'NONE',  ( -9.989285784994814676, 108.9734242744570025, 0.5301777604595967475 ) ) ;
#12262=CARTESIAN_POINT ( 'NONE',  ( -5.656854249492381470, -23.75000000409677270, 5.656854249492379694 ) ) ;
#12330=CARTESIAN_POINT ( 'NONE',  ( -10.00000000000000178, 15.00000000000000000, 1.734723475976807489E-15 ) ) ;
#12331=CARTESIAN_POINT ( 'NONE',  ( 6.928203230275510549, 85.00000000000000000, -4.000000000000000000 ) ) ;
#12338=CARTESIAN_POINT ( 'NONE',  ( 5.656854249492380582, -22.81249999999999289, -5.656854249492379694 ) ) ;
#12342=ORIENTED_EDGE ( 'NONE', *, *, #21437, .F. ) ;
#12395=B_SPLINE_CURVE_WITH_KNOTS ( 'NONE', 3,
 ( #103601, #38879, #29752, #78262, #14042, #62625, #53466, #29234, #95512, #54491, #87962, #88491, #87436, #63695, #46433, #79322, #96583, #5442, #38364, #30266, #22181, #46947, #47475, #3856, #71748, #79848, #22716, #102544, #20624, #28695, #86385, #12453, #15112, #57682 ),
 .UNSPECIFIED., .F., .F.,
 ( 4, 2, 2, 2, 2, 2, 2, 2, 2, 2, 2, 2, 2, 2, 2, 2, 4 ),
 ( 0.01272238763756221476, 0.01351613129786391303, 0.01430987495816561129, 0.01510361861846732691, 0.01589736227876904426, 0.01669110593907075987, 0.01748484959937247549, 0.01827859325967419457, 0.01907233691997591019, 0.01986608058027762580, 0.02065982424057934141, 0.02145356790088105703, 0.02224731156118277264, 0.02304105522148449173, 0.02383479888178620734, 0.02462854254208794377, 0.02542228620238968020 ),
 .UNSPECIFIED. ) ;
#12402=CARTESIAN_POINT ( 'NONE',  ( -9.537291425704607306, 102.3559562266722907, 3.012810007366001130 ) ) ;
#12403=CYLINDRICAL_SURFACE ( 'NONE', #4632, 8.000000000000000000 ) ;
#12404=FILL_AREA_STYLE_COLOUR ( '', #14043 ) ;
#12407=AXIS2_PLACEMENT_3D ( 'NONE', #76972, #58128, #59746 ) ;
#12420=CARTESIAN_POINT ( 'NONE',  ( 7.188101187500001821, -16.43750000204838457, -2.977408999572650483 ) ) ;
#12453=CARTESIAN_POINT ( 'NONE',  ( 6.944371705245972137, 30.53899691424550511, -3.972324460300560744 ) ) ;
#12461=CARTESIAN_POINT ( 'NONE',  ( 7.188101187500000044, -10.53125000204838457, 0.000000000000000000 ) ) ;
#12487=CARTESIAN_POINT ( 'NONE',  ( 5.082755093536325930, -23.46875000204838457, -5.082755093536325042 ) ) ;
#12516=VERTEX_POINT ( 'NONE', #94036 ) ;
#12517=CARTESIAN_POINT ( 'NONE',  ( 7.999999999999998224, -26.09374999999999645, 3.313708498984766049 ) ) ;
#12535=CARTESIAN_POINT ( 'NONE',  ( 4.401442555609581635E-16, -20.65625000204838813, -7.188101187500000044 ) ) ;
#12546=CARTESIAN_POINT ( 'NONE',  ( -5.082755093536326818, -33.59375000204838813, 5.082755093536325042 ) ) ;
#12590=CARTESIAN_POINT ( 'NONE',  ( -1.320432766682874540E-15, -33.40625000204838813, 7.188101187500000044 ) ) ;
#12599=ORIENTED_EDGE ( 'NONE', *, *, #37721, .T. ) ;
#12601=CARTESIAN_POINT ( 'NONE',  ( 2.977408999572652260, -16.43750000204838813, 7.188101187500000044 ) ) ;
#12605=DIRECTION ( 'NONE',  ( 0.000000000000000000, 1.000000000000000000, 0.000000000000000000 ) ) ;
#12606=CARTESIAN_POINT ( 'NONE',  ( -9.165151389911681434, 84.99999999999998579, -4.000000000000000000 ) ) ;
#12609=CARTESIAN_POINT ( 'NONE',  ( 3.313708498984762052, -15.40625000409677092, -8.000000000000000000 ) ) ;
#12618=CARTESIAN_POINT ( 'NONE',  ( 2.048435453982682120, -30.00000000000000355, -7.401063805010598351 ) ) ;
#12675=CARTESIAN_POINT ( 'NONE',  ( -7.188101187500000044, -25.90625000204838813, -8.802885111219163269E-16 ) ) ;
#12705=CARTESIAN_POINT ( 'NONE',  ( 1.749814335632528417, 15.56087475005694643, 9.852235012526419311 ) ) ;
#12748=CARTESIAN_POINT ( 'NONE',  ( 0.000000000000000000, -30.00000000000000000, 8.000000000000000000 ) ) ;
#12769=EDGE_CURVE ( 'NONE', #40311, #31698, #49236, .T. ) ;
#12795=EDGE_CURVE ( 'NONE', #63010, #43496, #22053, .T. ) ;
#12856=CARTESIAN_POINT ( 'NONE',  ( -5.656854249492379694, -10.62500000409677092, -5.656854249492380582 ) ) ;
#12863=CARTESIAN_POINT ( 'NONE',  ( 8.000000000000000000, -21.40624999999999289, -3.313708498984761608 ) ) ;
#12865=( BOUNDED_CURVE ( )  B_SPLINE_CURVE ( 2, ( #2133, #99785, #56248, #48696, #89183, #6658, #81583, #72456, #74961 ),
 .UNSPECIFIED., .F., .F. ) 
 B_SPLINE_CURVE_WITH_KNOTS ( ( 3, 2, 2, 2, 3 ),
 ( 0.7205882352941177516, 0.7279411764705883137, 0.7352941176470589868, 0.7426470588235295489, 0.7500000000000001110 ),
 .UNSPECIFIED. ) 
 CURVE ( )  GEOMETRIC_REPRESENTATION_ITEM ( )  RATIONAL_B_SPLINE_CURVE ( ( 0.9999999999999988898, 0.9238795325112878487, 1.000000000000000000, 0.9238795325112867385, 1.000000000000000000, 0.9238795325112867385, 1.000000000000000000, 0.9238795325112856283, 1.000000000000001110 ) ) 
 REPRESENTATION_ITEM ( '' )  );
#12872=B_SPLINE_CURVE_WITH_KNOTS ( 'NONE', 3,
 ( #51910, #102600, #60568, #51374, #93979, #85907, #28752, #60044, #36840, #3908, #28219, #36318, #61088, #20133, #44911, #84289, #10383, #68659, #4429, #102058, #43822, #70234, #11439, #37369, #53517, #27691, #35781, #61635, #69187, #11981, #86444, #77797, #94526, #20678 ),
 .UNSPECIFIED., .F., .F.,
 ( 4, 2, 2, 2, 2, 2, 2, 2, 2, 2, 2, 2, 2, 2, 2, 2, 4 ),
 ( 1.409296014025916843E-17, 0.0007899309203816184607, 0.001579861840763222827, 0.002369792761144826759, 0.003159723681526431342, 0.003949654601908035925, 0.004739585522289639641, 0.005529516442671244224, 0.006319447363052848807, 0.007109378283434453390, 0.007899309203816057973, 0.008689240124197661688, 0.009479171044579265404, 0.01026910196496087085, 0.01105903288534247457, 0.01184896380572408002, 0.01263889472610568374 ),
 .UNSPECIFIED. ) ;
#12889=CARTESIAN_POINT ( 'NONE',  ( 9.999999999999996447, 15.00000000000000000, -4.582575694955844270 ) ) ;
#12908=EDGE_LOOP ( 'NONE', ( #86702, #2054, #15051, #77258, #61403, #88351, #86181 ) ) ;
#12913=CARTESIAN_POINT ( 'NONE',  ( -9.646083234704169840, 26.98709390976521405, -2.643797197754292672 ) ) ;
#12923=ORIENTED_EDGE ( 'NONE', *, *, #102852, .T. ) ;
#12933=CARTESIAN_POINT ( 'NONE',  ( -9.646083234704169840, 101.9870939097652069, -2.643797197754281569 ) ) ;
#12934=CARTESIAN_POINT ( 'NONE',  ( 0.000000000000000000, -30.00000000000000000, 0.000000000000000000 ) ) ;
#12948=CARTESIAN_POINT ( 'NONE',  ( -2.977408999572654480, -14.00000000204838457, 7.188101187499999156 ) ) ;
#12978=EDGE_CURVE ( 'NONE', #71772, #20242, #36526, .T. ) ;
#12980=CARTESIAN_POINT ( 'NONE',  ( -7.344133061198930612, 27.55505607319423689, 3.176267128233874359 ) ) ;
#12987=CARTESIAN_POINT ( 'NONE',  ( 7.188101187500000044, -12.03125000204838635, 0.000000000000000000 ) ) ;
#13002=CARTESIAN_POINT ( 'NONE',  ( -1.469576158976823947E-15, -29.37499999999999645, 8.000000000000000000 ) ) ;
#13013=CARTESIAN_POINT ( 'NONE',  ( -7.188101187500001821, -18.50000000204838457, -2.977408999572651371 ) ) ;
#13028=VERTEX_POINT ( 'NONE', #4117 ) ;
#13064=CARTESIAN_POINT ( 'NONE',  ( -5.082755093536325042, -17.46875000204838813, -5.082755093536325930 ) ) ;
#13074=CARTESIAN_POINT ( 'NONE',  ( 4.401442555609581635E-16, -31.15625000204838813, -7.188101187500000044 ) ) ;
#13080=CARTESIAN_POINT ( 'NONE',  ( -7.801339272325196639, 108.5873147195970319, -1.788609912539670388 ) ) ;
#13083=ORIENTED_EDGE ( 'NONE', *, *, #105168, .F. ) ;
#13116=CARTESIAN_POINT ( 'NONE',  ( 2.977408999572651815, -30.31250000204838813, 7.188101187500000933 ) ) ;
#13130=CARTESIAN_POINT ( 'NONE',  ( -7.188101187500000044, -18.40625000204838457, -8.802885111219163269E-16 ) ) ;
#13136=CARTESIAN_POINT ( 'NONE',  ( 0.000000000000000000, 16.00000000000000000, 0.000000000000000000 ) ) ;
#13137=CARTESIAN_POINT ( 'NONE',  ( -9.177080501238302546, 84.46653057145729804, -3.972956046786644713 ) ) ;
#13140=CARTESIAN_POINT ( 'NONE',  ( 3.313708498984762496, -11.46875000409677092, 7.999999999999998224 ) ) ;
#13148=CARTESIAN_POINT ( 'NONE',  ( -9.698972129396508990, 33.17629712741938874, -2.445345647270327216 ) ) ;
#13192=DIRECTION ( 'NONE',  ( -0.000000000000000000, 1.000000000000000000, -0.000000000000000000 ) ) ;
#13200=ORIENTED_EDGE ( 'NONE', *, *, #90747, .F. ) ;
#13205=CARTESIAN_POINT ( 'NONE',  ( -5.082755093536325042, -23.09375000204838457, -5.082755093536325930 ) ) ;
#13251=ADVANCED_FACE ( 'NONE', ( #19154 ), #89271, .T. ) ;
#13271=CARTESIAN_POINT ( 'NONE',  ( 8.000000000000000000, -33.68750000409677625, 0.000000000000000000 ) ) ;
#13272=CARTESIAN_POINT ( 'NONE',  ( 9.380155525692144280, 15.95825086476136612, 3.484792534604217895 ) ) ;
#13291=CARTESIAN_POINT ( 'NONE',  ( -9.926810856659471938, 15.46725112412266512, 1.404490565848834027 ) ) ;
#13327=CARTESIAN_POINT ( 'NONE',  ( 8.000000000000000000, -14.18750000409677092, 0.000000000000000000 ) ) ;
#13343=ORIENTED_EDGE ( 'NONE', *, *, #34277, .T. ) ;
#13377=CARTESIAN_POINT ( 'NONE',  ( 8.000000000000000000, -24.59375000409677270, -3.313708498984761164 ) ) ;
#13393=CARTESIAN_POINT ( 'NONE',  ( -3.313708498984765161, -20.46874999999999645, 7.999999999999998224 ) ) ;
#13430=ORIENTED_EDGE ( 'NONE', *, *, #21019, .F. ) ;
#13437=FACE_OUTER_BOUND ( 'NONE', #100092, .T. ) ;
#13445=CARTESIAN_POINT ( 'NONE',  ( -8.000000000000001776, -26.65624999999999645, 3.313708498984759387 ) ) ;
#13457=CARTESIAN_POINT ( 'NONE',  ( -9.999999999999998224, 15.00000000000000000, -0.7768758660233218150 ) ) ;
#13461=CARTESIAN_POINT ( 'NONE',  ( -9.948688207305192321, 101.1297685050981841, -1.044946705213430915 ) ) ;
#13463=CARTESIAN_POINT ( 'NONE',  ( 3.648665620917453278, 15.00000000000000178, -9.999999999999998224 ) ) ;
#13478=CARTESIAN_POINT ( 'NONE',  ( -5.082755093536325042, -9.968750002048384573, -5.082755093536325930 ) ) ;
#13522=CARTESIAN_POINT ( 'NONE',  ( -1.320432766682874540E-15, -15.40625000204838635, 7.188101187500000044 ) ) ;
#13534=VERTEX_POINT ( 'NONE', #35202 ) ;
#13545=LINE ( 'NONE', #61609, #2835 ) ;
#13550=CARTESIAN_POINT ( 'NONE',  ( 7.188101187500000044, -22.15625000204838457, 0.000000000000000000 ) ) ;
#13570=UNCERTAINTY_MEASURE_WITH_UNIT (LENGTH_MEASURE( 1.000000000000000082E-05 ), #31284, 'distance_accuracy_value', 'NONE');
#13598=CARTESIAN_POINT ( 'NONE',  ( -7.188101187500002709, -20.18750000204838813, 2.977408999572647819 ) ) ;
#13608=CARTESIAN_POINT ( 'NONE',  ( -7.188101187500002709, -30.68750000204839168, 2.977408999572648707 ) ) ;
#13652=CARTESIAN_POINT ( 'NONE',  ( -7.188101187500001821, -30.87500000204838813, -2.977408999572651371 ) ) ;
#13668=CARTESIAN_POINT ( 'NONE',  ( 7.188101187500000933, -20.56250000204838813, -2.977408999572650483 ) ) ;
#13677=CARTESIAN_POINT ( 'NONE',  ( -1.469576158976823947E-15, -13.06250000409676915, 8.000000000000000000 ) ) ;
#13687=CARTESIAN_POINT ( 'NONE',  ( -1.510421413154896753, 15.23810023151367332, 9.910377230550597716 ) ) ;
#13695=CARTESIAN_POINT ( 'NONE',  ( 7.999999999999998224, -9.781250004096767370, 3.313708498984766049 ) ) ;
#13729=DIRECTION ( 'NONE',  ( 0.000000000000000000, 1.000000000000000000, 0.000000000000000000 ) ) ;
#13734=ORIENTED_EDGE ( 'NONE', *, *, #84601, .T. ) ;
#13739=CARTESIAN_POINT ( 'NONE',  ( -1.320432766682874540E-15, -25.53125000204838813, 7.188101187500000044 ) ) ;
#13741=CARTESIAN_POINT ( 'NONE',  ( 9.999999999999996447, 15.00000000000000000, -10.00000000000000000 ) ) ;
#13804=CARTESIAN_POINT ( 'NONE',  ( 3.313708498984762052, -31.90625000409677270, -8.000000000000000000 ) ) ;
#13827=CARTESIAN_POINT ( 'NONE',  ( -9.673800154115149041, 15.30085158940939039, 2.563280883359885909 ) ) ;
#13831=CARTESIAN_POINT ( 'NONE',  ( -9.165151389911679658, 105.0000000000000000, 4.000000000000001776 ) ) ;
#13846=DIRECTION ( 'NONE',  ( 0.000000000000000000, 0.000000000000000000, -1.000000000000000000 ) ) ;
#13860=CARTESIAN_POINT ( 'NONE',  ( 3.313708498984761608, -13.90625000409677092, -8.000000000000000000 ) ) ;
#13861=CARTESIAN_POINT ( 'NONE',  ( 3.313708498984722972, -12.40625000409676737, -8.000000000000040856 ) ) ;
#13889=EDGE_CURVE ( 'NONE', #6205, #699, #64615, .T. ) ;
#13890=ORIENTED_EDGE ( 'NONE', *, *, #22361, .F. ) ;
#13915=CARTESIAN_POINT ( 'NONE',  ( -9.907626560209530808, 15.45483377860037777, -1.400881274228119144 ) ) ;
#13925=CARTESIAN_POINT ( 'NONE',  ( 5.656854249492378806, -14.18749999999999112, 5.656854249492381470 ) ) ;
#13952=CARTESIAN_POINT ( 'NONE',  ( 9.373884331924955404, 15.95332971149351842, -3.487646406148425804 ) ) ;
#13988=CARTESIAN_POINT ( 'NONE',  ( -9.999999999999998224, 15.00000000000000000, 1.734723475976807489E-15 ) ) ;
#14006=CARTESIAN_POINT ( 'NONE',  ( 7.188101187500000044, -10.53125000204838457, 0.000000000000000000 ) ) ;
#14032=CARTESIAN_POINT ( 'NONE',  ( 3.313708498984743844, -26.46875000409677270, 8.000000000000017764 ) ) ;
#14042=CARTESIAN_POINT ( 'NONE',  ( 7.045755811259134305, 31.30341603013552643, 3.790843699961854885 ) ) ;
#14043=COLOUR_RGB ( '', 0.31764706, 0.68627451, 0.89019608) ;
#14044=CARTESIAN_POINT ( 'NONE',  ( -8.000113193197767814, 25.99977361354138594, -0.2613481123984617849 ) ) ;
#14050=CARTESIAN_POINT ( 'NONE',  ( 3.313708498984762052, -30.21874999999999645, -8.000000000000000000 ) ) ;
#14074=CARTESIAN_POINT ( 'NONE',  ( 7.188101187499999156, -20.75000000204839523, 2.977408999572654924 ) ) ;
#14089=CARTESIAN_POINT ( 'NONE',  ( 5.656854249492380582, -21.50000000409676915, -5.656854249492379694 ) ) ;
#14106=ADVANCED_FACE ( 'NONE', ( #81061 ), #89706, .T. ) ;
#14126=CARTESIAN_POINT ( 'NONE',  ( -7.188101187500000044, -18.78125000204838457, -8.802885111219163269E-16 ) ) ;
#14133=CARTESIAN_POINT ( 'NONE',  ( -2.977408999572654480, -29.00000000204838813, 7.188101187499999156 ) ) ;
#14136=CARTESIAN_POINT ( 'NONE',  ( 2.977408999572651815, -24.31250000204838813, 7.188101187500000933 ) ) ;
#14175=CARTESIAN_POINT ( 'NONE',  ( 2.977408999572650927, -29.75000000204838813, -7.188101187500001821 ) ) ;
#14190=CARTESIAN_POINT ( 'NONE',  ( 5.082755093536324154, -13.34375000204838457, 5.082755093536326818 ) ) ;
#14203=CARTESIAN_POINT ( 'NONE',  ( -5.656854249492379694, -9.125000004096769146, -5.656854249492380582 ) ) ;
#14205=CARTESIAN_POINT ( 'NONE',  ( 9.999999999999996447, 15.00000000000000000, 3.648665620917586505 ) ) ;
#14212=CARTESIAN_POINT ( 'NONE',  ( -9.798380800342663122, 33.46800654315502754, -2.010350564680328134 ) ) ;
#14267=CARTESIAN_POINT ( 'NONE',  ( -7.188101187500000044, -18.40625000204838457, -8.802885111219163269E-16 ) ) ;
#14271=CARTESIAN_POINT ( 'NONE',  ( -1.469576158976823947E-15, -23.37499999999999289, 8.000000000000000000 ) ) ;
#14295=ORIENTED_EDGE ( 'NONE', *, *, #80384, .T. ) ;
#14321=DIRECTION ( 'NONE',  ( 1.734723475976807094E-16, 0.000000000000000000, 1.000000000000000000 ) ) ;
#14329=CARTESIAN_POINT ( 'NONE',  ( -3.313708498984760720, -31.71875000409677625, -8.000000000000000000 ) ) ;
#14371=CARTESIAN_POINT ( 'NONE',  ( 0.9654893961777153422, -30.00000000000000355, 7.122964895856731538 ) ) ;
#14416=ORIENTED_EDGE ( 'NONE', *, *, #6781, .T. ) ;
#14423=CARTESIAN_POINT ( 'NONE',  ( -10.00000000000000355, 0.000000000000000000, -10.00000000000000000 ) ) ;
#14450=CARTESIAN_POINT ( 'NONE',  ( -5.656854249492379694, -17.93749999999999645, -5.656854249492380582 ) ) ;
#14515=CARTESIAN_POINT ( 'NONE',  ( 2.455962139888945739, 15.75268258782372754, -9.700350089084166072 ) ) ;
#14561=( BOUNDED_CURVE ( )  B_SPLINE_CURVE ( 2, ( #17934, #51865, #10344, #51334, #58919, #91813, #60526, #44322, #2242 ),
 .UNSPECIFIED., .F., .F. ) 
 B_SPLINE_CURVE_WITH_KNOTS ( ( 3, 2, 2, 2, 3 ),
 ( 0.8382352941176471894, 0.8455882352941177516, 0.8529411764705882026, 0.8602941176470588758, 0.8676470588235293269 ),
 .UNSPECIFIED. ) 
 CURVE ( )  GEOMETRIC_REPRESENTATION_ITEM ( )  RATIONAL_B_SPLINE_CURVE ( ( 0.9999999999999988898, 0.9238795325112878487, 1.000000000000000000, 0.9238795325112867385, 1.000000000000000000, 0.9238795325112867385, 1.000000000000000000, 0.9238795325112878487, 0.9999999999999988898 ) ) 
 REPRESENTATION_ITEM ( '' )  );
#14570=CARTESIAN_POINT ( 'NONE',  ( -7.744329845603316720, 26.53711769846545110, -2.018701143083231120 ) ) ;
#14577=CARTESIAN_POINT ( 'NONE',  ( -3.313708498984765161, -30.96874999999999645, 7.999999999999998224 ) ) ;
#14600=CARTESIAN_POINT ( 'NONE',  ( -2.977408999572654480, -18.12500000204838457, 7.188101187499999156 ) ) ;
#14650=CARTESIAN_POINT ( 'NONE',  ( 4.401442555609581635E-16, -22.15625000204838457, -7.188101187500000044 ) ) ;
#14657=CARTESIAN_POINT ( 'NONE',  ( 7.122964895856751077, -30.00000000000000355, -0.9654893961775683486 ) ) ;
#14660=CARTESIAN_POINT ( 'NONE',  ( 5.082755093536325930, -23.84375000204838457, -5.082755093536325042 ) ) ;
#14708=CARTESIAN_POINT ( 'NONE',  ( -7.188101187500002709, -24.68750000204838457, 2.977408999572648707 ) ) ;
#14721=CARTESIAN_POINT ( 'NONE',  ( -7.188101187500000044, -10.90625000204838457, -8.802885111219163269E-16 ) ) ;
#14731=CARTESIAN_POINT ( 'NONE',  ( 4.898587196589412829E-16, -19.62499999999999289, -8.000000000000000000 ) ) ;
#14734=CARTESIAN_POINT ( 'NONE',  ( -8.000000000000001776, -10.34375000409676915, 3.313708498984758943 ) ) ;
#14739=CARTESIAN_POINT ( 'NONE',  ( -9.797537890442933772, 88.46557797666194745, 2.014215961808879296 ) ) ;
#14740=CARTESIAN_POINT ( 'NONE',  ( 7.999999999999998224, -20.09374999999999289, 3.313708498984766049 ) ) ;
#14746=( NAMED_UNIT ( * ) PLANE_ANGLE_UNIT ( ) SI_UNIT ( $, .RADIAN. ) );
#14757=VECTOR ( 'NONE', #47706, 1000.000000000000000 ) ;
#14766=ORIENTED_EDGE ( 'NONE', *, *, #96195, .F. ) ;
#14769=AXIS2_PLACEMENT_3D ( 'NONE', #71921, #89173, #55707 ) ;
#14802=CARTESIAN_POINT ( 'NONE',  ( 7.188101187500000044, -17.65625000204838457, 0.000000000000000000 ) ) ;
#14804=CARTESIAN_POINT ( 'NONE',  ( 9.165151389911677882, 84.73264844392886630, -4.000000000000000000 ) ) ;
#14808=VERTEX_POINT ( 'NONE', #85766 ) ;
#14815=ORIENTED_EDGE ( 'NONE', *, *, #43138, .T. ) ;
#14825=AXIS2_PLACEMENT_3D ( 'NONE', #96910, #30605, #13846 ) ;
#14866=CARTESIAN_POINT ( 'NONE',  ( 5.656854249492380582, -30.50000000409677270, -5.656854249492379694 ) ) ;
#14884=CARTESIAN_POINT ( 'NONE',  ( -9.999999999997886135, 15.11700796860587381, 0.7408669144214915514 ) ) ;
#14887=SURFACE_STYLE_USAGE ( .BOTH. , #106557 ) ;
#14941=CYLINDRICAL_SURFACE ( 'NONE', #71575, 8.000000000000000000 ) ;
#14983=CARTESIAN_POINT ( 'NONE',  ( 0.000000000000000000, 0.000000000000000000, 0.000000000000000000 ) ) ;
#14988=CARTESIAN_POINT ( 'NONE',  ( -3.313708498984765161, -14.46874999999999289, 7.999999999999998224 ) ) ;
#14996=VERTEX_POINT ( 'NONE', #46616 ) ;
#15011=VERTEX_POINT ( 'NONE', #63354 ) ;
#15051=ORIENTED_EDGE ( 'NONE', *, *, #3327, .F. ) ;
#15055=CARTESIAN_POINT ( 'NONE',  ( -10.00000000000004086, 14.99999999999998934, -4.210530276627957313 ) ) ;
#15062=CARTESIAN_POINT ( 'NONE',  ( 1.404490565847964501, 15.46725112412266334, -9.926810856659662008 ) ) ;
#15094=AXIS2_PLACEMENT_3D ( 'NONE', #48101, #47046, #23882 ) ;
#15112=CARTESIAN_POINT ( 'NONE',  ( 6.928203230275506996, 30.26883324508997575, -3.999999999999999112 ) ) ;
#15114=CARTESIAN_POINT ( 'NONE',  ( -7.150931910075644105, 28.21374201477736676, -3.588457848165353958 ) ) ;
#15122=CARTESIAN_POINT ( 'NONE',  ( -7.188101187500002709, -9.687500002048384573, 2.977408999572648707 ) ) ;
#15149=CARTESIAN_POINT ( 'NONE',  ( 2.977408999572651815, -17.93750000204838457, 7.188101187500000933 ) ) ;
#15156=DIRECTION ( 'NONE',  ( 1.000000000000000000, -0.000000000000000000, -0.000000000000000000 ) ) ;
#15195=CARTESIAN_POINT ( 'NONE',  ( 7.188101187500000933, -13.43750000204838457, -2.977408999572650483 ) ) ;
#15201=CARTESIAN_POINT ( 'NONE',  ( 7.203362828890048419, -30.00000000000004263, -0.01858974796685433292 ) ) ;
#15207=CARTESIAN_POINT ( 'NONE',  ( 4.401442555609581635E-16, -29.65625000204838813, -7.188101187500000044 ) ) ;
#15251=CARTESIAN_POINT ( 'NONE',  ( 9.989285784994811124, 26.02657572554299747, 0.5301777604595849791 ) ) ;
#15252=CARTESIAN_POINT ( 'NONE',  ( 7.188101187499999156, -25.62500000204838813, 2.977408999572654924 ) ) ;
#15269=CARTESIAN_POINT ( 'NONE',  ( -2.977408999572654480, -12.12500000204838635, 7.188101187499999156 ) ) ;
#15280=CARTESIAN_POINT ( 'NONE',  ( -5.656854249492379694, -12.12500000409676915, -5.656854249492380582 ) ) ;
#15282=CARTESIAN_POINT ( 'NONE',  ( 9.999999999999998224, 15.00000000000000000, -2.283746462400398747E-15 ) ) ;
#15285=CARTESIAN_POINT ( 'NONE',  ( -9.842473135306409660, 88.58931817113585794, 1.785129593756285660 ) ) ;
#15288=CARTESIAN_POINT ( 'NONE',  ( -9.333892298909264085, 31.78275731625031852, -3.590295303293458140 ) ) ;
#15296=CARTESIAN_POINT ( 'NONE',  ( 5.656854249492380582, -9.500000004096769146, -5.656854249492379694 ) ) ;
#15336=ORIENTED_EDGE ( 'NONE', *, *, #88401, .F. ) ;
#15341=CARTESIAN_POINT ( 'NONE',  ( -1.320432766682874540E-15, -16.53125000204838813, 7.188101187500000044 ) ) ;
#15373=DIRECTION ( 'NONE',  ( 1.000000000000000000, -0.000000000000000000, -0.000000000000000000 ) ) ;
#15382=ORIENTED_EDGE ( 'NONE', *, *, #52147, .T. ) ;
#15403=CARTESIAN_POINT ( 'NONE',  ( 8.000000000000000000, -27.59375000409676915, -3.313708498984761608 ) ) ;
#15423=CARTESIAN_POINT ( 'NONE',  ( -9.700350089084256666, 15.75268258782372754, 2.455962139888509199 ) ) ;
#15447=CARTESIAN_POINT ( 'NONE',  ( -2.139906788305918628, -30.00000000000000355, 7.052091621315984327 ) ) ;
#15485=FACE_OUTER_BOUND ( 'NONE', #24863, .T. ) ;
#15498=LINE ( 'NONE', #41897, #105324 ) ;
#15524=CARTESIAN_POINT ( 'NONE',  ( 3.313708498984762496, -15.78124999999999289, 7.999999999999998224 ) ) ;
#15553=CARTESIAN_POINT ( 'NONE',  ( 9.999999999999996447, 15.00000000000000000, -4.397168787612349306 ) ) ;
#15589=CARTESIAN_POINT ( 'NONE',  ( -10.00000000000000000, 15.00000000000000178, -3.082707893549292422 ) ) ;
#15594=CARTESIAN_POINT ( 'NONE',  ( 0.7060372491531136108, 15.23416508906601230, -9.999999999999998224 ) ) ;
#15651=CARTESIAN_POINT ( 'NONE',  ( 5.656854249492380582, -31.81249999999999289, -5.656854249492379694 ) ) ;
#15658=CARTESIAN_POINT ( 'NONE',  ( -5.656854249492381470, -8.750000004096769146, 5.656854249492379694 ) ) ;
#15660=CARTESIAN_POINT ( 'NONE',  ( -4.165977904505308693, 16.00000000000000000, -9.090909090909089940 ) ) ;
#15676=CARTESIAN_POINT ( 'NONE',  ( 2.977408999572650927, -12.87500000204838280, -7.188101187500001821 ) ) ;
#15732=CARTESIAN_POINT ( 'NONE',  ( 7.188101187500000044, -13.53125000204838457, 0.000000000000000000 ) ) ;
#15741=CARTESIAN_POINT ( 'NONE',  ( -7.188101187500001821, -29.37500000204838457, -2.977408999572651371 ) ) ;
#15756=ORIENTED_EDGE ( 'NONE', *, *, #2506, .F. ) ;
#15757=CARTESIAN_POINT ( 'NONE',  ( -7.619701877737480977, 88.17442159532770063, -2.447562251315978710 ) ) ;
#15768=CARTESIAN_POINT ( 'NONE',  ( -8.000000000000000000, -25.53125000409676915, -3.313708498984762496 ) ) ;
#15783=CARTESIAN_POINT ( 'NONE',  ( 5.082755093536325930, -26.84375000204838813, -5.082755093536325042 ) ) ;
#15798=CARTESIAN_POINT ( 'NONE',  ( -2.977408999572654480, -15.12500000204838457, 7.188101187499999156 ) ) ;
#15803=ADVANCED_FACE ( 'NONE', ( #65325 ), #97147, .T. ) ;
#15811=CARTESIAN_POINT ( 'NONE',  ( -5.082755093536325042, -30.59375000204838813, -5.082755093536325930 ) ) ;
#15819=CARTESIAN_POINT ( 'NONE',  ( -9.644834624769977438, 33.00890500205773748, 2.648308524638411932 ) ) ;
#15822=CARTESIAN_POINT ( 'NONE',  ( -2.802461721337177636, 15.83563386295778308, 9.606080321247327802 ) ) ;
#15850=EDGE_LOOP ( 'NONE', ( #9628, #1261, #34472 ) ) ;
#15861=CARTESIAN_POINT ( 'NONE',  ( 7.414580834929599185, 87.64656280281482736, 3.010264818013835164 ) ) ;
#15864=EDGE_CURVE ( 'NONE', #91623, #14996, #100136, .T. ) ;
#15866=DIRECTION ( 'NONE',  ( 0.9090909090909092827, 0.000000000000000000, -0.4165977904505306917 ) ) ;
#15872=CARTESIAN_POINT ( 'NONE',  ( 5.082755093536324154, -16.34375000204838813, 5.082755093536326818 ) ) ;
#15877=CARTESIAN_POINT ( 'NONE',  ( 9.918579450955562038, 81.20696087031315358, 1.297207292923872046 ) ) ;
#15893=CARTESIAN_POINT ( 'NONE',  ( -8.000000000000001776, -19.34375000409677270, 3.313708498984759387 ) ) ;
#15936=CARTESIAN_POINT ( 'NONE',  ( -3.313708498984765161, -31.15625000409677270, 7.999999999999998224 ) ) ;
#15977=CARTESIAN_POINT ( 'NONE',  ( -7.619701877737479201, 33.17442159532767221, -2.447562251315979598 ) ) ;
#16013=VERTEX_POINT ( 'NONE', #106368 ) ;
#16037=CARTESIAN_POINT ( 'NONE',  ( 9.699121749566359085, 108.1766876027581503, 2.444499528233566199 ) ) ;
#16058=CARTESIAN_POINT ( 'NONE',  ( -3.313708498984765161, -15.96874999999999289, 7.999999999999998224 ) ) ;
#16065=CARTESIAN_POINT ( 'NONE',  ( 2.450541714948253347, 15.75132464342601146, -9.701712097384769251 ) ) ;
#16074=EDGE_CURVE ( 'NONE', #71070, #48348, #934, .T. ) ;
#16123=CARTESIAN_POINT ( 'NONE',  ( -5.082755093536326818, -33.21875000204838813, 5.082755093536325042 ) ) ;
#16142=( BOUNDED_CURVE ( )  B_SPLINE_CURVE ( 2, ( #60253, #35448, #49048, #1426, #85579, #19292, #68322, #3043, #43511 ),
 .UNSPECIFIED., .F., .F. ) 
 B_SPLINE_CURVE_WITH_KNOTS ( ( 3, 2, 2, 2, 3 ),
 ( 0.7500000000000001110, 0.7573529411764706731, 0.7647058823529412352, 0.7720588235294119084, 0.7794117647058824705 ),
 .UNSPECIFIED. ) 
 CURVE ( )  GEOMETRIC_REPRESENTATION_ITEM ( )  RATIONAL_B_SPLINE_CURVE ( ( 0.9999999999999988898, 0.9238795325112878487, 1.000000000000000000, 0.9238795325112867385, 1.000000000000000000, 0.9238795325112867385, 1.000000000000000000, 0.9238795325112856283, 1.000000000000001110 ) ) 
 REPRESENTATION_ITEM ( '' )  );
#16172=( BOUNDED_CURVE ( )  B_SPLINE_CURVE ( 2, ( #9384, #27773, #59574, #2897, #60647, #100009, #93533, #26177, #8870 ),
 .UNSPECIFIED., .F., .F. ) 
 B_SPLINE_CURVE_WITH_KNOTS ( ( 3, 2, 2, 2, 3 ),
 ( 0.9264705882352942679, 0.9338235294117648300, 0.9411764705882352811, 0.9485294117647058432, 0.9558823529411765163 ),
 .UNSPECIFIED. ) 
 CURVE ( )  GEOMETRIC_REPRESENTATION_ITEM ( )  RATIONAL_B_SPLINE_CURVE ( ( 0.9999999999999988898, 0.9238795325112878487, 1.000000000000000000, 0.9238795325112867385, 1.000000000000000000, 0.9238795325112867385, 1.000000000000000000, 0.9238795325112867385, 1.000000000000000000 ) ) 
 REPRESENTATION_ITEM ( '' )  );
#16184=CARTESIAN_POINT ( 'NONE',  ( 3.313708498984762052, -33.21875000000000000, -8.000000000000000000 ) ) ;
#16208=CARTESIAN_POINT ( 'NONE',  ( -7.188101187500000044, -13.90625000204838457, -8.802885111219163269E-16 ) ) ;
#16241=EDGE_CURVE ( 'NONE', #7939, #30765, #85861, .T. ) ;
#16260=CARTESIAN_POINT ( 'NONE',  ( 5.082755093536324154, -15.21875000204838457, 5.082755093536326818 ) ) ;
#16263=CARTESIAN_POINT ( 'NONE',  ( 6.889848939933039595, -30.00000000000001066, 2.062583278641663576 ) ) ;
#16269=CARTESIAN_POINT ( 'NONE',  ( 5.082755093536325930, -25.34375000204838813, -5.082755093536325042 ) ) ;
#16285=CARTESIAN_POINT ( 'NONE',  ( -7.999912353029504430, 88.99982470603096374, -0.2691822806795016731 ) ) ;
#16288=CARTESIAN_POINT ( 'NONE',  ( -3.999994092537668244, -10.00072617203139380, 6.928206640937045080 ) ) ;
#16307=CARTESIAN_POINT ( 'NONE',  ( 9.380894568449074100, 27.98869366889058696, -3.467341429141167719 ) ) ;
#16308=CARTESIAN_POINT ( 'NONE',  ( -7.188101187500001821, -27.87500000204838457, -2.977408999572651371 ) ) ;
#16324=CARTESIAN_POINT ( 'NONE',  ( -2.977408999572650039, -14.18750000204838457, -7.188101187500000933 ) ) ;
#16325=CARTESIAN_POINT ( 'NONE',  ( 7.934914944860278041, 26.13154352799888258, -1.051261972695687774 ) ) ;
#16339=CARTESIAN_POINT ( 'NONE',  ( -7.188101187500002709, -30.31250000204838813, 2.977408999572648707 ) ) ;
#16341=CARTESIAN_POINT ( 'NONE',  ( 9.673800154114779559, 15.30085158940939571, 2.563280883360070206 ) ) ;
#16401=CARTESIAN_POINT ( 'NONE',  ( -5.082755093536325042, -21.59375000204838457, -5.082755093536325930 ) ) ;
#16404=CARTESIAN_POINT ( 'NONE',  ( 9.165151389911681434, 84.73680493705116135, 4.000000000000001776 ) ) ;
#16454=CARTESIAN_POINT ( 'NONE',  ( 5.082755093536324154, -29.84375000204838813, 5.082755093536326818 ) ) ;
#16468=CARTESIAN_POINT ( 'NONE',  ( 3.313708498984762496, -26.46875000409677625, 7.999999999999998224 ) ) ;
#16473=VECTOR ( 'NONE', #91346, 1000.000000000000000 ) ;
#16499=VECTOR ( 'NONE', #105414, 1000.000000000000000 ) ;
#16506=CARTESIAN_POINT ( 'NONE',  ( -7.343637806710344051, 32.44363121900617841, 3.177475076494671313 ) ) ;
#16526=( NAMED_UNIT ( * ) PLANE_ANGLE_UNIT ( ) SI_UNIT ( $, .RADIAN. ) );
#16553=EDGE_CURVE ( 'NONE', #44948, #94312, #72814, .T. ) ;
#16554=CARTESIAN_POINT ( 'NONE',  ( -8.000000000000000000, -28.43750000409677270, -9.797174393178825657E-16 ) ) ;
#16576=CARTESIAN_POINT ( 'NONE',  ( 9.918325909156569864, 108.7923523170742754, 1.298699613733150571 ) ) ;
#16594=CARTESIAN_POINT ( 'NONE',  ( -5.656854249492381470, -11.56249999999999289, 5.656854249492379694 ) ) ;
#16596=EDGE_CURVE ( 'NONE', #20391, #42289, #38266, .T. ) ;
#16604=EDGE_LOOP ( 'NONE', ( #80934, #36185, #47905, #91015, #38617, #10962, #48597 ) ) ;
#16661=CARTESIAN_POINT ( 'NONE',  ( 2.977408999572650927, -33.87500000204838813, -7.188101187500001821 ) ) ;
#16712=ORIENTED_EDGE ( 'NONE', *, *, #98052, .F. ) ;
#16722=CARTESIAN_POINT ( 'NONE',  ( 8.000000000000000000, -25.99999999999999645, 0.000000000000000000 ) ) ;
#16728=DIRECTION ( 'NONE',  ( 0.000000000000000000, 0.000000000000000000, 1.000000000000000000 ) ) ;
#16738=EDGE_CURVE ( 'NONE', #58245, #48348, #34537, .T. ) ;
#16745=CARTESIAN_POINT ( 'NONE',  ( 4.401442555609581635E-16, -12.78125000204838280, -7.188101187500000044 ) ) ;
#16772=CARTESIAN_POINT ( 'NONE',  ( 0.000000000000000000, -30.00000000000000000, 0.000000000000000000 ) ) ;
#16783=EDGE_CURVE ( 'NONE', #10653, #3603, #50142, .T. ) ;
#16804=CARTESIAN_POINT ( 'NONE',  ( 2.977408999572650927, -14.75000000204838457, -7.188101187500000933 ) ) ;
#16814=CARTESIAN_POINT ( 'NONE',  ( 5.082755093536324154, -18.21875000204838457, 5.082755093536326818 ) ) ;
#16861=STYLED_ITEM ( 'NONE', ( #23717 ), #60625 ) ;
#16862=CARTESIAN_POINT ( 'NONE',  ( -2.977408999572654480, -17.00000000204838457, 7.188101187499999156 ) ) ;
#16876=CARTESIAN_POINT ( 'NONE',  ( 7.743982712349854580, 26.53786985239263529, 2.020119794285908821 ) ) ;
#16887=CARTESIAN_POINT ( 'NONE',  ( 0.000000000000000000, -30.00000000000000000, 8.000000000000000000 ) ) ;
#16889=CARTESIAN_POINT ( 'NONE',  ( -7.188101187500001821, -33.50000000204838813, -2.977408999572651371 ) ) ;
#16923=CARTESIAN_POINT ( 'NONE',  ( 9.797174393178825657E-16, -30.00000000000000000, -8.000000000000000000 ) ) ;
#16933=LINE ( 'NONE', #80049, #47770 ) ;
#16939=CARTESIAN_POINT ( 'NONE',  ( 7.002990960197237769, 86.05266818383456950, 3.868040364119521790 ) ) ;
#16949=CARTESIAN_POINT ( 'NONE',  ( -7.188101187500002709, -10.81250000204838457, 2.977408999572648707 ) ) ;
#16951=CARTESIAN_POINT ( 'NONE',  ( 9.644834624769973885, 81.99109499794225542, 2.648308524638419925 ) ) ;
#16968=FACE_OUTER_BOUND ( 'NONE', #81119, .T. ) ;
#16982=AXIS2_PLACEMENT_3D ( 'NONE', #43168, #101407, #35644 ) ;
#17006=CARTESIAN_POINT ( 'NONE',  ( -7.188101187500002709, -28.81250000204838813, 2.977408999572647819 ) ) ;
#17015=CARTESIAN_POINT ( 'NONE',  ( -5.656854249492381470, -25.25000000409677270, 5.656854249492379694 ) ) ;
#17026=DIRECTION ( 'NONE',  ( 0.000000000000000000, 1.000000000000000000, 0.000000000000000000 ) ) ;
#17032=CARTESIAN_POINT ( 'NONE',  ( -1.469576158976823947E-15, -16.06250000409677270, 8.000000000000000000 ) ) ;
#17054=CARTESIAN_POINT ( 'NONE',  ( -7.986452802927061612, 33.97309757691886034, 0.5332468218996333498 ) ) ;
#17074=( LENGTH_UNIT ( ) NAMED_UNIT ( * ) SI_UNIT ( .MILLI., .METRE. ) );
#17095=DIRECTION ( 'NONE',  ( -0.000000000000000000, -1.000000000000000000, -0.000000000000000000 ) ) ;
#17097=AXIS2_PLACEMENT_3D ( 'NONE', #66042, #89795, #41234 ) ;
#17110=CARTESIAN_POINT ( 'NONE',  ( 7.743982712349851916, 101.5378698523926033, 2.020119794285909265 ) ) ;
#17143=CARTESIAN_POINT ( 'NONE',  ( 3.313708498984762496, -11.28124999999999289, 7.999999999999998224 ) ) ;
#17210=CARTESIAN_POINT ( 'NONE',  ( 7.188101187500000044, -28.15625000204838813, 0.000000000000000000 ) ) ;
#17232=DIRECTION ( 'NONE',  ( -0.000000000000000000, 1.000000000000000000, -0.000000000000000000 ) ) ;
#17269=CARTESIAN_POINT ( 'NONE',  ( -10.00000000000000355, 30.00000000000000000, 4.000000000000000000 ) ) ;
#17270=CARTESIAN_POINT ( 'NONE',  ( -3.313708498984760720, -28.53124999999999289, -8.000000000000000000 ) ) ;
#17297=CARTESIAN_POINT ( 'NONE',  ( 2.977408999572651815, -16.43750000204838457, 7.188101187500000933 ) ) ;
#17324=B_SPLINE_CURVE_WITH_KNOTS ( 'NONE', 3,
 ( #99541, #83364, #74201, #40776, #65593, #33248, #81748, #105518, #41312, #9463, #15977, #65060, #106573, #49931, #32723, #72615, #24631, #25718, #17054, #41842, #17592, #74730, #90404, #33782, #31659, #66657, #16506, #278, #58577, #49392, #66120, #813, #64542, #89350 ),
 .UNSPECIFIED., .F., .F.,
 ( 4, 2, 2, 2, 2, 2, 2, 2, 2, 2, 2, 2, 2, 2, 2, 2, 4 ),
 ( 3.576224061345498009E-18, 0.0007951492273476417835, 0.001590298454695279881, 0.002385447682042917978, 0.003180596909390556292, 0.003975746136738194172, 0.004770895364085832487, 0.005566044591433469933, 0.006361193818781108247, 0.007156343046128743959, 0.007951492273476381406, 0.008746641500824020588, 0.009541790728171658034, 0.01033693995551929548, 0.01113208918286693466, 0.01192723841021457384, 0.01272238763756220956 ),
 .UNSPECIFIED. ) ;
#17348=AXIS2_PLACEMENT_3D ( 'NONE', #94928, #78188, #22643 ) ;
#17352=CARTESIAN_POINT ( 'NONE',  ( 2.977408999572652260, -13.81250000204838457, 7.188101187500000044 ) ) ;
#17359=CARTESIAN_POINT ( 'NONE',  ( -7.188101187500000044, -20.28125000204838813, -8.802885111219163269E-16 ) ) ;
#17387=CARTESIAN_POINT ( 'NONE',  ( -3.313708498984783812, -25.15625000409677270, 7.999999999999979572 ) ) ;
#17398=CARTESIAN_POINT ( 'NONE',  ( 2.977408999572650927, -19.25000000204838813, -7.188101187500001821 ) ) ;
#17422=CARTESIAN_POINT ( 'NONE',  ( -7.188101187500000044, -33.40625000204838813, -8.802885111219163269E-16 ) ) ;
#17428=CARTESIAN_POINT ( 'NONE',  ( -9.797537890442935549, 33.46557797666191902, 2.014215961808868638 ) ) ;
#17485=CARTESIAN_POINT ( 'NONE',  ( -2.977408999572654480, -13.62500000204838457, 7.188101187499999156 ) ) ;
#17521=CARTESIAN_POINT ( 'NONE',  ( 7.045965687440314262, 83.69607536213965204, 3.790395326974318913 ) ) ;
#17541=CARTESIAN_POINT ( 'NONE',  ( -5.082755093536325042, -26.09375000204838813, -5.082755093536325930 ) ) ;
#17547=( NAMED_UNIT ( * ) SI_UNIT ( $, .STERADIAN. ) SOLID_ANGLE_UNIT ( ) );
#17553=CARTESIAN_POINT ( 'NONE',  ( -5.656854249492379694, -24.12500000409677270, -5.656854249492380582 ) ) ;
#17556=LINE ( 'NONE', #75772, #98204 ) ;
#17592=CARTESIAN_POINT ( 'NONE',  ( -7.896571385775229324, 33.78997999345754266, 1.305932416347437952 ) ) ;
#17607=CARTESIAN_POINT ( 'NONE',  ( -8.000000000000001776, -22.15624999999999645, 3.313708498984759387 ) ) ;
#17608=EDGE_LOOP ( 'NONE', ( #78479, #739, #32811, #57935, #53089, #101735, #10317 ) ) ;
#17610=CARTESIAN_POINT ( 'NONE',  ( 3.836411046841927686, 15.00000000000001066, 9.999999999999959144 ) ) ;
#17673=CARTESIAN_POINT ( 'NONE',  ( -7.212994264445060644, 102.9828865565996097, 3.463766307298588032 ) ) ;
#17688=CYLINDRICAL_SURFACE ( 'NONE', #12407, 8.000000000000000000 ) ;
#17705=SURFACE_STYLE_USAGE ( .BOTH. , #66235 ) ;
#17706=CARTESIAN_POINT ( 'NONE',  ( -6.944371705245973914, 84.46100308575449844, -3.972324460300559856 ) ) ;
#17724=B_SPLINE_CURVE_WITH_KNOTS ( 'NONE', 3,
 ( #85463, #35347, #68210, #101107, #11548, #27267, #60151, #6113, #54121, #20244, #12086, #95672, #47102, #45018, #62784, #77899, #104824, #53093, #28866, #4008, #80004, #45543, #78416, #38517, #21813, #5072, #38005, #63321, #86015, #36939, #69805, #13137, #54653, #12606 ),
 .UNSPECIFIED., .F., .F.,
 ( 4, 2, 2, 2, 2, 2, 2, 2, 2, 2, 2, 2, 2, 2, 2, 2, 4 ),
 ( 0.01263889472610568374, 0.01342810546992895954, 0.01421731621375223360, 0.01500652695757550940, 0.01579573770139878347, 0.01658494844522205927, 0.01737415918904533507, 0.01816336993286861087, 0.01895258067669188667, 0.01974179142051516248, 0.02053100216433843828, 0.02132021290816171408, 0.02210942365198498988, 0.02289863439580826915, 0.02368784513963154148, 0.02447705588345482075, 0.02526626662727809655 ),
 .UNSPECIFIED. ) ;
#17730=CARTESIAN_POINT ( 'NONE',  ( -3.313708498984783812, -27.96874999999999645, 7.999999999999979572 ) ) ;
#17738=CARTESIAN_POINT ( 'NONE',  ( 5.082755093536324154, -31.34375000204838457, 5.082755093536326818 ) ) ;
#17748=CARTESIAN_POINT ( 'NONE',  ( 4.898587196589412829E-16, -25.62499999999999645, -8.000000000000000000 ) ) ;
#17785=ADVANCED_FACE ( 'NONE', ( #2929 ), #27799, .T. ) ;
#17799=CARTESIAN_POINT ( 'NONE',  ( -8.000000000000000000, -25.24999999999999289, -9.797174393178825657E-16 ) ) ;
#17808=CARTESIAN_POINT ( 'NONE',  ( -8.000000000000000000, -33.03125000409677625, -3.313708498984762496 ) ) ;
#17826=CARTESIAN_POINT ( 'NONE',  ( 4.401442555609581635E-16, -14.28125000204838457, -7.188101187500000044 ) ) ;
#17849=CARTESIAN_POINT ( 'NONE',  ( 4.898587196589412829E-16, -25.62499999999999645, -8.000000000000000000 ) ) ;
#17881=CARTESIAN_POINT ( 'NONE',  ( -7.188101187500000044, -9.781250002048384573, -8.802885111219163269E-16 ) ) ;
#17891=CARTESIAN_POINT ( 'NONE',  ( 7.188101187499999156, -22.62500000204838813, 2.977408999572654924 ) ) ;
#17892=CARTESIAN_POINT ( 'NONE',  ( 6.928203230275507885, 105.0000000000000000, -4.000000000000001776 ) ) ;
#17930=CARTESIAN_POINT ( 'NONE',  ( 9.165151389911681434, 29.73680493705114714, 3.999999999999999112 ) ) ;
#17931=CARTESIAN_POINT ( 'NONE',  ( -7.188101187500001821, -20.37500000204838457, -2.977408999572651371 ) ) ;
#17934=CARTESIAN_POINT ( 'NONE',  ( 4.898587196589412829E-16, -12.31250000409676915, -8.000000000000000000 ) ) ;
#17954=CARTESIAN_POINT ( 'NONE',  ( -5.082755093536325042, -32.09375000204838813, -5.082755093536325930 ) ) ;
#17967=CARTESIAN_POINT ( 'NONE',  ( 9.797174393178825657E-16, -30.00000000000000000, -8.000000000000000000 ) ) ;
#17985=ORIENTED_EDGE ( 'NONE', *, *, #63071, .T. ) ;
#18013=CARTESIAN_POINT ( 'NONE',  ( -2.977408999572654480, -15.12500000204838457, 7.188101187499999156 ) ) ;
#18020=DIRECTION ( 'NONE',  ( 0.000000000000000000, 0.000000000000000000, 1.000000000000000000 ) ) ;
#18063=PLANE ( 'NONE',  #6397 ) ;
#18073=CARTESIAN_POINT ( 'NONE',  ( 7.188101187500000933, -22.06250000204838813, -2.977408999572650483 ) ) ;
#18082=CARTESIAN_POINT ( 'NONE',  ( -3.313708498984765161, -22.15625000409677270, 7.999999999999998224 ) ) ;
#18086=CARTESIAN_POINT ( 'NONE',  ( 9.381593208289372043, 32.01438638119505953, -3.465401811657802256 ) ) ;
#18110=AXIS2_PLACEMENT_3D ( 'NONE', #46666, #95236, #5677 ) ;
#18153=VERTEX_POINT ( 'NONE', #57575 ) ;
#18210=CARTESIAN_POINT ( 'NONE',  ( -3.313708498984798467, -21.03124999999998934, -7.999999999999961808 ) ) ;
#18248=CARTESIAN_POINT ( 'NONE',  ( -6.928203230275512325, 84.73116675491002070, -4.000000000000000000 ) ) ;
#18327=ADVANCED_FACE ( 'NONE', ( #19329 ), #43548, .F. ) ;
#18339=CARTESIAN_POINT ( 'NONE',  ( 5.656854249492378806, -26.18749999999999645, 5.656854249492381470 ) ) ;
#18365=CARTESIAN_POINT ( 'NONE',  ( -9.165151389911681434, 85.26319506294885286, 4.000000000000001776 ) ) ;
#18393=B_SPLINE_CURVE_WITH_KNOTS ( 'NONE', 3,
 ( #36488, #68827, #27871, #102235, #60736, #28386, #34350, #59129, #94146, #92011 ),
 .UNSPECIFIED., .F., .F.,
 ( 4, 2, 2, 2, 4 ),
 ( 0.000000000000000000, 0.001118707926289530573, 0.002237415852579061146, 0.003356123778868591936, 0.004474831705158122293 ),
 .UNSPECIFIED. ) ;
#18397=ORIENTED_EDGE ( 'NONE', *, *, #64416, .F. ) ;
#18400=( BOUNDED_CURVE ( )  B_SPLINE_CURVE ( 2, ( #46773, #5263, #38190, #47292, #63509, #79670, #24129, #13861, #71049 ),
 .UNSPECIFIED., .F., .F. ) 
 B_SPLINE_CURVE_WITH_KNOTS ( ( 3, 2, 2, 2, 3 ),
 ( 0.8088235294117647189, 0.8161764705882352811, 0.8235294117647058432, 0.8308823529411766273, 0.8382352941176471894 ),
 .UNSPECIFIED. ) 
 CURVE ( )  GEOMETRIC_REPRESENTATION_ITEM ( )  RATIONAL_B_SPLINE_CURVE ( ( 1.000000000000000000, 0.9238795325112867385, 1.000000000000000000, 0.9238795325112867385, 1.000000000000000000, 0.9238795325112867385, 1.000000000000000000, 0.9238795325112856283, 1.000000000000001110 ) ) 
 REPRESENTATION_ITEM ( '' )  );
#18423=CARTESIAN_POINT ( 'NONE',  ( 3.822317990709313662, -30.00000000000000000, 6.092126002012808961 ) ) ;
#18429=CARTESIAN_POINT ( 'NONE',  ( 2.977408999572651815, -21.31250000204838813, 7.188101187500000933 ) ) ;
#18443=CARTESIAN_POINT ( 'NONE',  ( -7.618844049274133390, 88.17235898929459381, 2.450177051822846064 ) ) ;
#18456=CIRCLE ( 'NONE', #97629, 1.000000000000000444 ) ;
#18469=CARTESIAN_POINT ( 'NONE',  ( -5.082755093536325042, -18.96875000204838457, -5.082755093536325930 ) ) ;
#18478=ORIENTED_EDGE ( 'NONE', *, *, #31670, .F. ) ;
#18494=CARTESIAN_POINT ( 'NONE',  ( 2.977408999572650927, -26.37500000204838457, -7.188101187500001821 ) ) ;
#18499=LINE ( 'NONE', #92887, #96470 ) ;
#18513=CARTESIAN_POINT ( 'NONE',  ( 4.898587196589412829E-16, -22.81250000409677270, -8.000000000000000000 ) ) ;
#18547=CARTESIAN_POINT ( 'NONE',  ( 5.082755093536324154, -27.21875000204838813, 5.082755093536326818 ) ) ;
#18556=CARTESIAN_POINT ( 'NONE',  ( -2.977408999572650039, -12.68750000204838280, -7.188101187500001821 ) ) ;
#18616=CARTESIAN_POINT ( 'NONE',  ( 7.188101187499999156, -25.25000000204839168, 2.977408999572654924 ) ) ;
#18619=( NAMED_UNIT ( * ) PLANE_ANGLE_UNIT ( ) SI_UNIT ( $, .RADIAN. ) );
#18627=CARTESIAN_POINT ( 'NONE',  ( -8.000000000000000000, -15.03125000409677092, -3.313708498984762496 ) ) ;
#18633=CARTESIAN_POINT ( 'NONE',  ( 3.313708498984800688, -20.28124999999999289, 7.999999999999960032 ) ) ;
#18635=CARTESIAN_POINT ( 'NONE',  ( 4.242317035479241660, -29.99999999999999289, -6.258419296384283292 ) ) ;
#18672=CARTESIAN_POINT ( 'NONE',  ( -3.999994092537668244, -10.00072617203139380, 6.928206640937044192 ) ) ;
#18691=CARTESIAN_POINT ( 'NONE',  ( 2.563280883359705609, 15.30085158940939394, 9.673800154114783112 ) ) ;
#18726=( BOUNDED_CURVE ( )  B_SPLINE_CURVE ( 2, ( #28671, #100391, #44292, #26553, #45362, #1685, #10312, #92288, #61556 ),
 .UNSPECIFIED., .F., .F. ) 
 B_SPLINE_CURVE_WITH_KNOTS ( ( 3, 2, 2, 2, 3 ),
 ( 0.8088235294117648300, 0.8161764705882353921, 0.8235294117647060652, 0.8308823529411767383, 0.8382352941176473005 ),
 .UNSPECIFIED. ) 
 CURVE ( )  GEOMETRIC_REPRESENTATION_ITEM ( )  RATIONAL_B_SPLINE_CURVE ( ( 0.9999999999999988898, 0.9238795325112878487, 1.000000000000000000, 0.9238795325112867385, 1.000000000000000000, 0.9238795325112867385, 1.000000000000000000, 0.9238795325112844070, 1.000000000000002220 ) ) 
 REPRESENTATION_ITEM ( '' )  );
#18799=CARTESIAN_POINT ( 'NONE',  ( -9.644834624769973885, 108.0089050020577446, 2.648308524638421702 ) ) ;
#18868=CARTESIAN_POINT ( 'NONE',  ( 3.313708498984753170, -29.46875000409677980, 8.000000000000008882 ) ) ;
#18887=DIRECTION ( 'NONE',  ( 0.000000000000000000, -1.000000000000000000, 0.000000000000000000 ) ) ;
#18889=CARTESIAN_POINT ( 'NONE',  ( -3.313708498984760720, -30.03124999999999645, -8.000000000000000000 ) ) ;
#18956=CARTESIAN_POINT ( 'NONE',  ( 0.000000000000000000, -30.00000000000000000, 8.000000000000000000 ) ) ;
#18976=CARTESIAN_POINT ( 'NONE',  ( 4.401442555609581635E-16, -22.15625000204838457, -7.188101187500000044 ) ) ;
#19003=CARTESIAN_POINT ( 'NONE',  ( 9.981544566921639827, 15.23274035658502079, -0.7016502453917061732 ) ) ;
#19010=B_SPLINE_CURVE_WITH_KNOTS ( 'NONE', 3,
 ( #20345, #11644, #45111, #43501, #12705, #61284, #53191, #20875, #86108, #28961 ),
 .UNSPECIFIED., .F., .F.,
 ( 4, 2, 2, 2, 4 ),
 ( -2.000195913693527015E-05, 0.001085800244612924580, 0.002191602448362784360, 0.003297404652112644139, 0.004403206855862503918 ),
 .UNSPECIFIED. ) ;
#19023=CARTESIAN_POINT ( 'NONE',  ( -7.188101187500000044, -17.28125000204838813, -8.802885111219163269E-16 ) ) ;
#19029=EDGE_LOOP ( 'NONE', ( #57133, #55745, #80034 ) ) ;
#19048=CARTESIAN_POINT ( 'NONE',  ( -5.082755093536326818, -24.21875000204838813, 5.082755093536325042 ) ) ;
#19080=CARTESIAN_POINT ( 'NONE',  ( 5.656854249492380582, -25.81249999999999645, -5.656854249492379694 ) ) ;
#19099=CARTESIAN_POINT ( 'NONE',  ( -2.977408999572650039, -28.06250000204838813, -7.188101187500000933 ) ) ;
#19110=CARTESIAN_POINT ( 'NONE',  ( 7.188101187499999156, -13.25000000204838280, 2.977408999572654924 ) ) ;
#19111=CARTESIAN_POINT ( 'NONE',  ( 4.898587196589412829E-16, -18.31250000409676915, -8.000000000000000000 ) ) ;
#19133=CARTESIAN_POINT ( 'NONE',  ( 3.313708498984762496, -23.46875000409677980, 7.999999999999998224 ) ) ;
#19148=DIRECTION ( 'NONE',  ( -0.000000000000000000, 1.000000000000000000, -0.000000000000000000 ) ) ;
#19154=FACE_OUTER_BOUND ( 'NONE', #81621, .T. ) ;
#19172=CARTESIAN_POINT ( 'NONE',  ( -5.082755093536326818, -27.21875000204838813, 5.082755093536325042 ) ) ;
#19181=CARTESIAN_POINT ( 'NONE',  ( -5.656854249492379694, -19.62500000409677270, -5.656854249492380582 ) ) ;
#19292=CARTESIAN_POINT ( 'NONE',  ( 8.000000000000000000, -15.40624999999999289, -3.313708498984761164 ) ) ;
#19329=FACE_OUTER_BOUND ( 'NONE', #97031, .T. ) ;
#19341=CARTESIAN_POINT ( 'NONE',  ( -9.090909090909089940, 16.00000000000000000, 4.165977904505306029 ) ) ;
#19360=ORIENTED_EDGE ( 'NONE', *, *, #15864, .T. ) ;
#19363=DIRECTION ( 'NONE',  ( -0.000000000000000000, 1.000000000000000000, -0.000000000000000000 ) ) ;
#19385=CARTESIAN_POINT ( 'NONE',  ( 0.000000000000000000, 16.00000000000000000, 0.000000000000000000 ) ) ;
#19387=CARTESIAN_POINT ( 'NONE',  ( -1.469576158976823947E-15, -12.87499999999999467, 8.000000000000000000 ) ) ;
#19434=CARTESIAN_POINT ( 'NONE',  ( -3.313708498984760720, -19.53124999999999289, -8.000000000000000000 ) ) ;
#19451=CARTESIAN_POINT ( 'NONE',  ( 7.046357527897573192, 106.3061565060100548, -3.789683693877204274 ) ) ;
#19456=CARTESIAN_POINT ( 'NONE',  ( -3.594033448928638741, -9.156975712238445197, 6.225088131883842912 ) ) ;
#19457=SURFACE_STYLE_USAGE ( .BOTH. , #20534 ) ;
#19466=EDGE_CURVE ( 'NONE', #16013, #20391, #35535, .T. ) ;
#19479=CARTESIAN_POINT ( 'NONE',  ( -8.000000000000000000, -11.74999999999999289, -9.797174393178825657E-16 ) ) ;
#19518=CARTESIAN_POINT ( 'NONE',  ( -1.320432766682874540E-15, -15.40625000204838635, 7.188101187500000044 ) ) ;
#19525=CARTESIAN_POINT ( 'NONE',  ( 4.898587196589412829E-16, -15.31250000409677092, -8.000000000000000000 ) ) ;
#19549=EDGE_CURVE ( 'NONE', #102469, #65829, #18400, .T. ) ;
#19559=CARTESIAN_POINT ( 'NONE',  ( -7.188101187500000044, -14.28125000204838457, -8.802885111219163269E-16 ) ) ;
#19588=CARTESIAN_POINT ( 'NONE',  ( -7.188101187500000044, -27.40625000204838813, -8.802885111219163269E-16 ) ) ;
#19604=CARTESIAN_POINT ( 'NONE',  ( -1.469576158976823947E-15, -22.06250000409676915, 8.000000000000000000 ) ) ;
#19637=CARTESIAN_POINT ( 'NONE',  ( 7.188101187500000933, -25.43750000204838457, -2.977408999572650483 ) ) ;
#19641=ORIENTED_EDGE ( 'NONE', *, *, #16241, .T. ) ;
#19647=CARTESIAN_POINT ( 'NONE',  ( 5.082755093536324154, -30.21875000204838813, 5.082755093536326818 ) ) ;
#19656=ORIENTED_EDGE ( 'NONE', *, *, #102470, .T. ) ;
#19700=EDGE_CURVE ( 'NONE', #54845, #56071, #28387, .T. ) ;
#19702=CARTESIAN_POINT ( 'NONE',  ( -5.082755093536325042, -23.09375000204838457, -5.082755093536325930 ) ) ;
#19709=CARTESIAN_POINT ( 'NONE',  ( 8.000000000000000000, -20.18750000409677270, 0.000000000000000000 ) ) ;
#19713=CARTESIAN_POINT ( 'NONE',  ( 9.165151389911681434, 30.00000000000000000, -4.000000000000000000 ) ) ;
#19764=CYLINDRICAL_SURFACE ( 'NONE', #53966, 8.000000000000000000 ) ;
#19775=CARTESIAN_POINT ( 'NONE',  ( -7.188101187500002709, -28.81250000204838457, 2.977408999572648707 ) ) ;
#19777=CARTESIAN_POINT ( 'NONE',  ( 6.123233995736772199E-16, 15.00000000000000000, 9.999999999999998224 ) ) ;
#19778=CARTESIAN_POINT ( 'NONE',  ( -10.00000000000000355, 85.00000000000000000, -4.000000000000000000 ) ) ;
#19780=CARTESIAN_POINT ( 'NONE',  ( -8.000000000000001776, -17.65624999999999645, 3.313708498984759387 ) ) ;
#19792=FILL_AREA_STYLE_COLOUR ( '', #4445 ) ;
#19839=CARTESIAN_POINT ( 'NONE',  ( -7.619753052866897747, 101.8254849719282760, -2.447276542590448578 ) ) ;
#19865=CARTESIAN_POINT ( 'NONE',  ( -10.00000000000000000, 15.00000000000000000, 4.582575694955833612 ) ) ;
#19914=CARTESIAN_POINT ( 'NONE',  ( -3.313708498984765161, -12.96874999999999289, 7.999999999999998224 ) ) ;
#19961=CARTESIAN_POINT ( 'NONE',  ( -5.656854249492381470, -22.06249999999999289, 5.656854249492379694 ) ) ;
#20000=( BOUNDED_CURVE ( )  B_SPLINE_CURVE ( 2, ( #6571, #55636, #88572, #54581, #62205, #21223, #70796, #39503, #38968 ),
 .UNSPECIFIED., .F., .T. ) 
 B_SPLINE_CURVE_WITH_KNOTS ( ( 3, 2, 2, 2, 3 ),
 ( 0.2500000000000000555, 0.2573529411764705621, 0.2647058823529411797, 0.2720588235294116863, 0.2794117647058823040 ),
 .UNSPECIFIED. ) 
 CURVE ( )  GEOMETRIC_REPRESENTATION_ITEM ( )  RATIONAL_B_SPLINE_CURVE ( ( 0.9999999999999994449, 0.9238795325112872936, 1.000000000000000000, 0.9238795325112867385, 1.000000000000000000, 0.9238795325112867385, 1.000000000000000000, 0.9238795325112872936, 0.9999999999999994449 ) ) 
 REPRESENTATION_ITEM ( '' )  );
#20006=CARTESIAN_POINT ( 'NONE',  ( -3.999997374469381750, -9.125726201419798400, 6.928204746136267467 ) ) ;
#20028=EDGE_LOOP ( 'NONE', ( #25129, #52113, #36960, #9075 ) ) ;
#20033=CARTESIAN_POINT ( 'NONE',  ( -9.334514330295428763, 103.2137726231821233, -3.588704711590612995 ) ) ;
#20034=DIRECTION ( 'NONE',  ( -0.000000000000000000, 1.000000000000000000, -0.000000000000000000 ) ) ;
#20035=CARTESIAN_POINT ( 'NONE',  ( 3.884543032214245351, 15.13241195026108166, -9.216463528758918500 ) ) ;
#20049=CARTESIAN_POINT ( 'NONE',  ( -5.082755093536325042, -17.46875000204838813, -5.082755093536325930 ) ) ;
#20092=CARTESIAN_POINT ( 'NONE',  ( -7.188101187500001821, -15.87500000204838635, -2.977408999572651371 ) ) ;
#20101=CARTESIAN_POINT ( 'NONE',  ( 9.381593208289377372, 87.01438638119508084, -3.465401811657801368 ) ) ;
#20116=CARTESIAN_POINT ( 'NONE',  ( 5.082755093536324154, -28.34375000204838813, 5.082755093536326818 ) ) ;
#20130=CARTESIAN_POINT ( 'NONE',  ( 5.656854249492378806, -21.87500000409676915, 5.656854249492381470 ) ) ;
#20133=CARTESIAN_POINT ( 'NONE',  ( 9.918010731619574472, 101.2084831515677337, -1.300854425901575739 ) ) ;
#20168=CARTESIAN_POINT ( 'NONE',  ( -7.188101187500000044, -26.28125000204838813, -8.802885111219163269E-16 ) ) ;
#20178=CARTESIAN_POINT ( 'NONE',  ( -2.977408999572654480, -33.50000000204838813, 7.188101187499999156 ) ) ;
#20184=CARTESIAN_POINT ( 'NONE',  ( -7.934883677559676940, 108.8683917793755001, 1.051380792122693419 ) ) ;
#20221=CARTESIAN_POINT ( 'NONE',  ( -7.188101187500000044, -32.28125000204838813, -8.802885111219163269E-16 ) ) ;
#20240=CARTESIAN_POINT ( 'NONE',  ( 7.188101187500000933, -19.06250000204838102, -2.977408999572650483 ) ) ;
#20242=VERTEX_POINT ( 'NONE', #101458 ) ;
#20244=CARTESIAN_POINT ( 'NONE',  ( -9.646032546913147598, 81.98719671525634567, 2.644051433538244122 ) ) ;
#20247=CARTESIAN_POINT ( 'NONE',  ( 8.000000000000000000, -20.09375000409677270, -3.313708498984761608 ) ) ;
#20300=DIRECTION ( 'NONE',  ( 0.000000000000000000, -0.000000000000000000, 1.000000000000000000 ) ) ;
#20315=CARTESIAN_POINT ( 'NONE',  ( 4.401442555609581635E-16, -24.78125000204838813, -7.188101187500000044 ) ) ;
#20319=FACE_OUTER_BOUND ( 'NONE', #12908, .T. ) ;
#20345=CARTESIAN_POINT ( 'NONE',  ( 0.000000000000000000, 15.00000000000000000, 10.00000000000000000 ) ) ;
#20357=CARTESIAN_POINT ( 'NONE',  ( -3.313708498984722528, -16.71875000409677270, -8.000000000000040856 ) ) ;
#20384=CARTESIAN_POINT ( 'NONE',  ( -7.934996450857311423, 101.1313754352746912, -1.050865690281777676 ) ) ;
#20391=VERTEX_POINT ( 'NONE', #67245 ) ;
#20406=SURFACE_STYLE_FILL_AREA ( #78049 ) ;
#20448=DIRECTION ( 'NONE',  ( 0.000000000000000000, 0.000000000000000000, -1.000000000000000000 ) ) ;
#20508=CARTESIAN_POINT ( 'NONE',  ( 8.000000000000000000, -19.90624999999999289, -3.313708498984761608 ) ) ;
#20534=SURFACE_SIDE_STYLE ('',( #3765 ) ) ;
#20582=CARTESIAN_POINT ( 'NONE',  ( 2.802461721337288658, 15.83563386295778308, -9.606080321247290499 ) ) ;
#20597=CARTESIAN_POINT ( 'NONE',  ( -2.977408999572650039, -17.56250000204838813, -7.188101187500001821 ) ) ;
#20624=CARTESIAN_POINT ( 'NONE',  ( 7.150931910075640552, 31.78625798522262258, -3.588457848165356623 ) ) ;
#20631=CARTESIAN_POINT ( 'NONE',  ( 3.313708498984839323, -21.78124999999999645, 7.999999999999921840 ) ) ;
#20634=CARTESIAN_POINT ( 'NONE',  ( -2.977408999572650039, -11.56250000204838635, -7.188101187500001821 ) ) ;
#20660=CARTESIAN_POINT ( 'NONE',  ( 7.188101187500001821, -23.56250000204838813, -2.977408999572650483 ) ) ;
#20671=CARTESIAN_POINT ( 'NONE',  ( 3.313708498984722972, -16.71874999999999289, -8.000000000000040856 ) ) ;
#20674=CIRCLE ( 'NONE', #99827, 8.000000000000000000 ) ;
#20678=CARTESIAN_POINT ( 'NONE',  ( 9.165151389911679658, 105.0000000000000000, 4.000000000000001776 ) ) ;
#20689=CARTESIAN_POINT ( 'NONE',  ( 5.656854249492378806, -26.18749999999999645, 5.656854249492381470 ) ) ;
#20710=CARTESIAN_POINT ( 'NONE',  ( 4.401442555609581635E-16, -28.15625000204838813, -7.188101187500000044 ) ) ;
#20714=ORIENTED_EDGE ( 'NONE', *, *, #48991, .F. ) ;
#20719=CARTESIAN_POINT ( 'NONE',  ( 2.977408999572651815, -33.31250000204838813, 7.188101187500000933 ) ) ;
#20733=EDGE_LOOP ( 'NONE', ( #58490, #2048 ) ) ;
#20758=CARTESIAN_POINT ( 'NONE',  ( 5.082755093536325930, -34.34375000204838813, -5.082755093536325042 ) ) ;
#20769=B_SPLINE_CURVE_WITH_KNOTS ( 'NONE', 3,
 ( #50279, #32542, #57828, #8760, #83183, #98308, #42191, #24461, #82657, #57297, #41140, #74024, #90754, #33073, #41663, #69151, #69667, #102018, #53985, #76682, #68068, #2793, #11944, #60531, #78278, #85319, #2247, #20101, #70193, #35197, #44873, #86405, #77760, #45401 ),
 .UNSPECIFIED., .F., .F.,
 ( 4, 2, 2, 2, 2, 2, 2, 2, 2, 2, 2, 2, 2, 2, 2, 2, 4 ),
 ( 0.01263889472610567853, 0.01342810546992895433, 0.01421731621375223013, 0.01500652695757550420, 0.01579573770139878000, 0.01658494844522205580, 0.01737415918904533160, 0.01816336993286860740, 0.01895258067669188320, 0.01974179142051515901, 0.02053100216433843481, 0.02132021290816171061, 0.02210942365198498294, 0.02289863439580826221, 0.02368784513963153801, 0.02447705588345481381, 0.02526626662727808961 ),
 .UNSPECIFIED. ) ;
#20772=CARTESIAN_POINT ( 'NONE',  ( 5.082755093536325930, -20.46875000204838813, -5.082755093536325042 ) ) ;
#20782=CARTESIAN_POINT ( 'NONE',  ( 7.999999999999998224, -15.78125000409677092, 3.313708498984766493 ) ) ;
#20784=CARTESIAN_POINT ( 'NONE',  ( 9.606080321247342013, 15.83563386295778308, 2.802461721337131451 ) ) ;
#20791=CARTESIAN_POINT ( 'NONE',  ( 4.933445413641555533, -30.00000000000000355, -5.637643499260712510 ) ) ;
#20846=CARTESIAN_POINT ( 'NONE',  ( -2.977408999572650039, -26.18750000204838813, -7.188101187500001821 ) ) ;
#20847=CARTESIAN_POINT ( 'NONE',  ( 5.656854249492378806, -20.37500000409677270, 5.656854249492381470 ) ) ;
#20848=CARTESIAN_POINT ( 'NONE',  ( 4.898587196589412829E-16, -24.12499999999999289, -8.000000000000000000 ) ) ;
#20852=CARTESIAN_POINT ( 'NONE',  ( -8.000000000000000000, -17.84374999999999645, -3.313708498984762496 ) ) ;
#20875=CARTESIAN_POINT ( 'NONE',  ( 3.484756791224362438, 15.95824666716552365, 9.380169522195147991 ) ) ;
#20895=CARTESIAN_POINT ( 'NONE',  ( -0.3498606326581789605, 15.11603512203452837, -10.00000000000000000 ) ) ;
#20915=CARTESIAN_POINT ( 'NONE',  ( 5.656854249492380582, -33.50000000409677625, -5.656854249492379694 ) ) ;
#20954=CYLINDRICAL_SURFACE ( 'NONE', #14825, 10.00000000000000000 ) ;
#21014=CARTESIAN_POINT ( 'NONE',  ( -3.313708498984760276, -10.71875000409677270, -8.000000000000000000 ) ) ;
#21019=EDGE_CURVE ( 'NONE', #90586, #31791, #65947, .T. ) ;
#21024=CARTESIAN_POINT ( 'NONE',  ( -8.000000000000001776, -19.15624999999999289, 3.313708498984758943 ) ) ;
#21071=CARTESIAN_POINT ( 'NONE',  ( -9.699121749566360862, 26.82331239724179994, 2.444499528233560870 ) ) ;
#21072=CARTESIAN_POINT ( 'NONE',  ( -3.313708498984783812, -26.46875000000000000, 7.999999999999979572 ) ) ;
#21073=CYLINDRICAL_SURFACE ( 'NONE', #3075, 8.000000000000000000 ) ;
#21091=CARTESIAN_POINT ( 'NONE',  ( 4.165977904505312246, 15.00000000000000000, -9.090909090909088164 ) ) ;
#21108=CARTESIAN_POINT ( 'NONE',  ( -2.977408999572650039, -13.06250000204838280, -7.188101187500001821 ) ) ;
#21115=CARTESIAN_POINT ( 'NONE',  ( -1.469576158976823947E-15, -24.87499999999999289, 8.000000000000000000 ) ) ;
#21141=ORIENTED_EDGE ( 'NONE', *, *, #27648, .T. ) ;
#21147=CARTESIAN_POINT ( 'NONE',  ( 2.977408999572650927, -16.25000000204838813, -7.188101187500001821 ) ) ;
#21173=DIRECTION ( 'NONE',  ( 0.000000000000000000, 1.000000000000000000, 0.000000000000000000 ) ) ;
#21175=CARTESIAN_POINT ( 'NONE',  ( 2.977408999572650927, -17.37500000204838457, -7.188101187500001821 ) ) ;
#21217=ORIENTED_EDGE ( 'NONE', *, *, #53760, .T. ) ;
#21219=CARTESIAN_POINT ( 'NONE',  ( 5.082755093536325930, -17.84375000204838457, -5.082755093536325042 ) ) ;
#21223=CARTESIAN_POINT ( 'NONE',  ( -8.000000000000001776, -26.84375000409677270, 3.313708498984759387 ) ) ;
#21230=CARTESIAN_POINT ( 'NONE',  ( -2.977408999572654480, -32.00000000204838813, 7.188101187499999156 ) ) ;
#21235=CARTESIAN_POINT ( 'NONE',  ( -7.896571385775229324, 108.7899799934575071, 1.305932416347436398 ) ) ;
#21250=DIRECTION ( 'NONE',  ( -1.000000000000000000, -0.000000000000000000, -0.000000000000000000 ) ) ;
#21269=CARTESIAN_POINT ( 'NONE',  ( 2.977408999572650927, -32.75000000204839523, -7.188101187500001821 ) ) ;
#21280=CARTESIAN_POINT ( 'NONE',  ( -5.082755093536325042, -20.09375000204838457, -5.082755093536325930 ) ) ;
#21288=CARTESIAN_POINT ( 'NONE',  ( 3.313708498984762052, -13.90625000409677092, -8.000000000000000000 ) ) ;
#21290=CARTESIAN_POINT ( 'NONE',  ( 9.240220675753558766, 15.98931925350938243, 3.827754797006297505 ) ) ;
#21350=CARTESIAN_POINT ( 'NONE',  ( -1.320432766682874540E-15, -22.53125000204838457, 7.188101187500000044 ) ) ;
#21383=ORIENTED_EDGE ( 'NONE', *, *, #12795, .T. ) ;
#21392=CARTESIAN_POINT ( 'NONE',  ( -10.00000000000000355, 15.00000000000000000, -10.00000000000000000 ) ) ;
#21437=EDGE_CURVE ( 'NONE', #31791, #57731, #106566, .T. ) ;
#21510=ORIENTED_EDGE ( 'NONE', *, *, #56340, .F. ) ;
#21520=CARTESIAN_POINT ( 'NONE',  ( 4.898587196589412829E-16, -24.31250000409677270, -8.000000000000000000 ) ) ;
#21527=CARTESIAN_POINT ( 'NONE',  ( 0.000000000000000000, -30.00000000000000000, 8.000000000000000000 ) ) ;
#21534=CARTESIAN_POINT ( 'NONE',  ( -3.313708498984760720, -24.03124999999999645, -8.000000000000000000 ) ) ;
#21547=( BOUNDED_CURVE ( )  B_SPLINE_CURVE ( 2, ( #71945, #89198, #98340, #13695, #47655, #80550, #15296, #48183, #32036 ),
 .UNSPECIFIED., .F., .F. ) 
 B_SPLINE_CURVE_WITH_KNOTS ( ( 3, 2, 2, 2, 3 ),
 ( 0.9264705882352941568, 0.9338235294117647189, 0.9411764705882352811, 0.9485294117647057321, 0.9558823529411764053 ),
 .UNSPECIFIED. ) 
 CURVE ( )  GEOMETRIC_REPRESENTATION_ITEM ( )  RATIONAL_B_SPLINE_CURVE ( ( 1.000000000000000000, 0.9238795325112867385, 1.000000000000000000, 0.9238795325112867385, 1.000000000000000000, 0.9238795325112867385, 1.000000000000000000, 0.9238795325112878487, 0.9999999999999988898 ) ) 
 REPRESENTATION_ITEM ( '' )  );
#21561=ORIENTED_EDGE ( 'NONE', *, *, #47594, .T. ) ;
#21573=B_SPLINE_CURVE_WITH_KNOTS ( 'NONE', 3,
 ( #14371, #24115, #72624, #81233, #65601, #15447, #47280, #82310, #32734, #7350, #8420, #56958, #96394, #31666, #64550, #40259, #7879, #32185, #22524, #23576, #89879, #81757, #40786, #73680, #98487, #106582, #88296, #24640 ),
 .UNSPECIFIED., .F., .F.,
 ( 4, 2, 2, 2, 2, 2, 2, 2, 2, 2, 2, 2, 2, 4 ),
 ( 6.362890571982298922E-17, 0.001872779778676164110, 0.002809169668014214073, 0.003745559557352264035, 0.004681949446690313564, 0.005618339336028363960, 0.006554729225366414357, 0.007491119114704463886, 0.009363898893380562943, 0.01030028878271861160, 0.01123667867205666027, 0.01217306856139470893, 0.01310945845073275759, 0.01498223822940885491 ),
 .UNSPECIFIED. ) ;
#21576=CYLINDRICAL_SURFACE ( 'NONE', #17348, 4.000000000000000000 ) ;
#21591=ORIENTED_EDGE ( 'NONE', *, *, #82955, .T. ) ;
#21606=CARTESIAN_POINT ( 'NONE',  ( -9.165151389911683211, 104.7370448908366001, 4.000000000000002665 ) ) ;
#21617=DIRECTION ( 'NONE',  ( 0.000000000000000000, 0.000000000000000000, 1.000000000000000000 ) ) ;
#21620=CARTESIAN_POINT ( 'NONE',  ( -10.00000000000000178, 15.00000000000000000, 4.582575694955834500 ) ) ;
#21621=CARTESIAN_POINT ( 'NONE',  ( -5.082755093536325042, -12.96875000204838280, -5.082755093536325930 ) ) ;
#21656=CARTESIAN_POINT ( 'NONE',  ( -7.934203308536662114, 26.13299659982202883, 1.057099537198549877 ) ) ;
#21662=CARTESIAN_POINT ( 'NONE',  ( -7.188101187500000044, -15.78125000204838635, -8.802885111219163269E-16 ) ) ;
#21667=AXIS2_PLACEMENT_3D ( 'NONE', #101057, #26161, #50896 ) ;
#21690=PLANE ( 'NONE',  #94823 ) ;
#21692=CARTESIAN_POINT ( 'NONE',  ( -2.977408999572654480, -16.62500000204838457, 7.188101187499999156 ) ) ;
#21741=CARTESIAN_POINT ( 'NONE',  ( 7.188101187500000044, -18.03125000204838457, 0.000000000000000000 ) ) ;
#21751=CARTESIAN_POINT ( 'NONE',  ( -5.082755093536325042, -9.593750002048384573, -5.082755093536325930 ) ) ;
#21792=CARTESIAN_POINT ( 'NONE',  ( -5.082755093536325042, -33.96875000204838813, -5.082755093536325930 ) ) ;
#21806=CARTESIAN_POINT ( 'NONE',  ( -5.082755093536325042, -21.59375000204838457, -5.082755093536325930 ) ) ;
#21813=CARTESIAN_POINT ( 'NONE',  ( -9.646083234704171616, 81.98709390976522116, -2.643797197754290007 ) ) ;
#21817=CARTESIAN_POINT ( 'NONE',  ( 3.313708498984762052, -10.90625000409677270, -8.000000000000000000 ) ) ;
#21829=CARTESIAN_POINT ( 'NONE',  ( -3.082707893549554878, 15.00000000000006928, 9.999999999999859668 ) ) ;
#21843=PRODUCT_DEFINITION_SHAPE ( 'NONE', 'NONE',  #8033 ) ;
#21880=CARTESIAN_POINT ( 'NONE',  ( -5.082755093536325042, -27.59375000204838457, -5.082755093536325930 ) ) ;
#21885=CARTESIAN_POINT ( 'NONE',  ( -5.656854249492381470, -23.56249999999999289, 5.656854249492379694 ) ) ;
#21891=VECTOR ( 'NONE', #92777, 1000.000000000000000 ) ;
#21903=EDGE_LOOP ( 'NONE', ( #2621, #99341, #42255, #97070 ) ) ;
#21940=CARTESIAN_POINT ( 'NONE',  ( -3.313708498984760720, -27.21875000409677625, -8.000000000000000000 ) ) ;
#21944=DIRECTION ( 'NONE',  ( 0.000000000000000000, 0.000000000000000000, 1.000000000000000000 ) ) ;
#21965=FACE_BOUND ( 'NONE', #39520, .T. ) ;
#22004=DIRECTION ( 'NONE',  ( -0.000000000000000000, -1.000000000000000000, -0.000000000000000000 ) ) ;
#22053=B_SPLINE_CURVE_WITH_KNOTS ( 'NONE', 3,
 ( #59978, #92840, #19003, #9785, #100401, #34652, #92300, #42701, #75598, #42165 ),
 .UNSPECIFIED., .F., .F.,
 ( 4, 2, 2, 2, 4 ),
 ( -2.000195913693157031E-05, 0.001085800244612924797, 0.002191602448362780890, 0.003297404652112636333, 0.004403206855862491775 ),
 .UNSPECIFIED. ) ;
#22058=CARTESIAN_POINT ( 'NONE',  ( 5.656854249492380582, -16.81249999999999289, -5.656854249492379694 ) ) ;
#22105=CARTESIAN_POINT ( 'NONE',  ( 7.999999999999998224, -27.78125000409677270, 3.313708498984766049 ) ) ;
#22108=CARTESIAN_POINT ( 'NONE',  ( -9.699189539447127473, 26.82307771753288250, -2.444343703917214672 ) ) ;
#22122=CARTESIAN_POINT ( 'NONE',  ( -9.341953373613076650, 15.21714514899110249, -3.572352985695669059 ) ) ;
#22127=EDGE_CURVE ( 'NONE', #91623, #70179, #39253, .T. ) ;
#22138=CYLINDRICAL_SURFACE ( 'NONE', #47745, 8.000000000000000000 ) ;
#22144=CARTESIAN_POINT ( 'NONE',  ( 7.188101187499999156, -10.62500000204838813, 2.977408999572654924 ) ) ;
#22180=ADVANCED_FACE ( 'NONE', ( #90983, #34367, #35971, #67242 ), #101194, .T. ) ;
#22181=CARTESIAN_POINT ( 'NONE',  ( 7.897196874019792645, 33.79127204167807008, -1.302055520192088256 ) ) ;
#22189=CARTESIAN_POINT ( 'NONE',  ( 7.999999999999998224, -30.59374999999999289, 3.313708498984766493 ) ) ;
#22194=CARTESIAN_POINT ( 'NONE',  ( -7.801642220026312025, 101.4120317385096683, 1.787233835843584417 ) ) ;
#22199=ORIENTED_EDGE ( 'NONE', *, *, #77384, .T. ) ;
#22217=CARTESIAN_POINT ( 'NONE',  ( -7.188101187500002709, -19.81250000204838813, 2.977408999572648707 ) ) ;
#22223=EDGE_CURVE ( 'NONE', #54822, #45637, #25206, .T. ) ;
#22231=CARTESIAN_POINT ( 'NONE',  ( -3.594029361870008099, -9.531975552773349847, 6.225090491531444670 ) ) ;
#22268=CARTESIAN_POINT ( 'NONE',  ( -1.320432766682874540E-15, -16.90625000204838813, 7.188101187500000044 ) ) ;
#22278=CARTESIAN_POINT ( 'NONE',  ( -7.188101187500002709, -24.68750000204838457, 2.977408999572648707 ) ) ;
#22322=CARTESIAN_POINT ( 'NONE',  ( 5.082755093536324154, -30.21875000204838813, 5.082755093536326818 ) ) ;
#22336=CARTESIAN_POINT ( 'NONE',  ( -2.977408999572654480, -10.62500000204838813, 7.188101187499999156 ) ) ;
#22350=CARTESIAN_POINT ( 'NONE',  ( 8.000000000000000000, -12.59375000409676737, -3.313708498984761608 ) ) ;
#22352=CARTESIAN_POINT ( 'NONE',  ( 9.151133496030011472, 15.07443463110253923, 4.034557488804340508 ) ) ;
#22356=CARTESIAN_POINT ( 'NONE',  ( 8.000000000000000000, -19.99999999999999289, 0.000000000000000000 ) ) ;
#22358=CARTESIAN_POINT ( 'NONE',  ( -9.483056940782031319, 32.44387790106576830, -3.177305548492605602 ) ) ;
#22361=EDGE_CURVE ( 'NONE', #106390, #39461, #38747, .T. ) ;
#22413=CARTESIAN_POINT ( 'NONE',  ( 4.401442555609581635E-16, -27.78125000204838457, -7.188101187500000044 ) ) ;
#22427=ADVANCED_FACE ( 'NONE', ( #40690 ), #31577, .F. ) ;
#22434=FACE_OUTER_BOUND ( 'NONE', #50276, .T. ) ;
#22448=ORIENTED_EDGE ( 'NONE', *, *, #86935, .T. ) ;
#22465=ORIENTED_EDGE ( 'NONE', *, *, #91432, .T. ) ;
#22481=CARTESIAN_POINT ( 'NONE',  ( 3.313708498984762052, -28.90625000409677270, -8.000000000000000000 ) ) ;
#22504=CARTESIAN_POINT ( 'NONE',  ( -9.240220675753736401, 15.98931925350938243, 3.827754797005848530 ) ) ;
#22507=FACE_OUTER_BOUND ( 'NONE', #32768, .T. ) ;
#22512=( BOUNDED_CURVE ( )  B_SPLINE_CURVE ( 2, ( #87695, #20357, #37045, #78518, #47207, #5180, #53720, #80109, #30535 ),
 .UNSPECIFIED., .F., .F. ) 
 B_SPLINE_CURVE_WITH_KNOTS ( ( 3, 2, 2, 2, 3 ),
 ( 0.6617647058823528106, 0.6691176470588233727, 0.6764705882352941568, 0.6838235294117647189, 0.6911764705882352811 ),
 .UNSPECIFIED. ) 
 CURVE ( )  GEOMETRIC_REPRESENTATION_ITEM ( )  RATIONAL_B_SPLINE_CURVE ( ( 1.000000000000001110, 0.9238795325112856283, 1.000000000000000000, 0.9238795325112867385, 1.000000000000000000, 0.9238795325112867385, 1.000000000000000000, 0.9238795325112867385, 1.000000000000000000 ) ) 
 REPRESENTATION_ITEM ( '' )  );
#22524=CARTESIAN_POINT ( 'NONE',  ( -7.228211769744709692, -29.99999999999998224, 2.785121603415316116 ) ) ;
#22559=ADVANCED_FACE ( 'NONE', ( #16968 ), #60106, .F. ) ;
#22574=EDGE_LOOP ( 'NONE', ( #45529, #62561, #74926, #7625 ) ) ;
#22590=CARTESIAN_POINT ( 'NONE',  ( 3.313708498984743844, -24.96875000409677625, 8.000000000000017764 ) ) ;
#22606=CARTESIAN_POINT ( 'NONE',  ( 4.898587196589412829E-16, -13.62499999999999112, -8.000000000000000000 ) ) ;
#22643=DIRECTION ( 'NONE',  ( 0.000000000000000000, 0.000000000000000000, -1.000000000000000000 ) ) ;
#22646=ORIENTED_EDGE ( 'NONE', *, *, #102470, .F. ) ;
#22647=CARTESIAN_POINT ( 'NONE',  ( 5.656854249492380582, -27.50000000409677270, -5.656854249492379694 ) ) ;
#22716=CARTESIAN_POINT ( 'NONE',  ( 7.344361273354514275, 32.44560530588525182, -3.175733139645580572 ) ) ;
#22718=CARTESIAN_POINT ( 'NONE',  ( -7.413471587080155523, 27.35647840831672895, -3.013058070223542551 ) ) ;
#22725=CARTESIAN_POINT ( 'NONE',  ( -3.313708498984760720, -31.53124999999999645, -8.000000000000000000 ) ) ;
#22749=CARTESIAN_POINT ( 'NONE',  ( -7.188101187500000044, -21.40625000204838457, -8.802885111219163269E-16 ) ) ;
#22762=CARTESIAN_POINT ( 'NONE',  ( -3.898489618125186240, -9.883538051243510481, 6.752435277548301862 ) ) ;
#22797=CARTESIAN_POINT ( 'NONE',  ( -2.977408999572650039, -20.56250000204838813, -7.188101187500000933 ) ) ;
#22807=CARTESIAN_POINT ( 'NONE',  ( -2.977408999572650039, -26.56250000204838457, -7.188101187500001821 ) ) ;
#22819=ADVANCED_FACE ( 'NONE', ( #44428 ), #2881, .T. ) ;
#22828=ORIENTED_EDGE ( 'NONE', *, *, #64628, .T. ) ;
#22832=CARTESIAN_POINT ( 'NONE',  ( 3.313708498984742512, -22.90625000409677270, -8.000000000000019540 ) ) ;
#22851=CARTESIAN_POINT ( 'NONE',  ( -7.188101187500002709, -26.18750000204838813, 2.977408999572648707 ) ) ;
#22863=CARTESIAN_POINT ( 'NONE',  ( -7.188101187500000044, -15.40625000204838635, -8.802885111219163269E-16 ) ) ;
#22877=CARTESIAN_POINT ( 'NONE',  ( -8.000000000000000000, -12.03125000409677270, -3.313708498984762496 ) ) ;
#22881=SURFACE_SIDE_STYLE ('',( #96749 ) ) ;
#22883=CARTESIAN_POINT ( 'NONE',  ( -9.999945253488242258, 33.99986313370533253, -0.2662901834230996800 ) ) ;
#22886=CARTESIAN_POINT ( 'NONE',  ( -4.165977904505307805, 16.00000000000000000, 9.090909090909091717 ) ) ;
#22936=CARTESIAN_POINT ( 'NONE',  ( -2.977408999572654480, -18.12500000204838457, 7.188101187499999156 ) ) ;
#22943=STYLED_ITEM ( 'NONE', ( #1311 ), #39669 ) ;
#22990=CARTESIAN_POINT ( 'NONE',  ( 7.188101187500000933, -28.06250000204838813, -2.977408999572650483 ) ) ;
#23000=CARTESIAN_POINT ( 'NONE',  ( 5.656854249492380582, -32.00000000409676915, -5.656854249492379694 ) ) ;
#23023=CARTESIAN_POINT ( 'NONE',  ( -9.571198553003730680, 15.30040232763764330, 2.918503601031092742 ) ) ;
#23081=AXIS2_PLACEMENT_3D ( 'NONE', #44470, #63718, #69290 ) ;
#23087=CARTESIAN_POINT ( 'NONE',  ( 6.928203230275509661, 104.7347384306741276, 4.000000000000001776 ) ) ;
#23092=ORIENTED_EDGE ( 'NONE', *, *, #71051, .F. ) ;
#23122=CARTESIAN_POINT ( 'NONE',  ( 3.313708498984762496, -17.28124999999999645, 7.999999999999998224 ) ) ;
#23181=CARTESIAN_POINT ( 'NONE',  ( -9.910377230549929806, 15.23810023151366799, -1.510421413154898085 ) ) ;
#23214=CARTESIAN_POINT ( 'NONE',  ( 5.656854249492380582, -24.31249999999999289, -5.656854249492379694 ) ) ;
#23238=CARTESIAN_POINT ( 'NONE',  ( -7.212994264445060644, 27.98288655659961321, 3.463766307298586256 ) ) ;
#23245=CARTESIAN_POINT ( 'NONE',  ( 8.000000000000000000, -31.90625000000000000, -3.313708498984761608 ) ) ;
#23268=CARTESIAN_POINT ( 'NONE',  ( -7.188101187500000044, -16.90625000204838813, -8.802885111219163269E-16 ) ) ;
#23286=ORIENTED_EDGE ( 'NONE', *, *, #19466, .T. ) ;
#23303=MECHANICAL_DESIGN_GEOMETRIC_PRESENTATION_REPRESENTATION('',(#4348),#37107);
#23320=CARTESIAN_POINT ( 'NONE',  ( -1.320432766682874540E-15, -21.40625000204838457, 7.188101187500000044 ) ) ;
#23329=CARTESIAN_POINT ( 'NONE',  ( 5.082755093536324154, -28.71875000204838813, 5.082755093536326818 ) ) ;
#23336=CARTESIAN_POINT ( 'NONE',  ( -7.002641335706726977, 106.0508726268083279, 3.868676264653295060 ) ) ;
#23375=CARTESIAN_POINT ( 'NONE',  ( 5.082755093536325930, -28.34375000204838813, -5.082755093536325042 ) ) ;
#23388=CARTESIAN_POINT ( 'NONE',  ( 2.977408999572650927, -12.87500000204838280, -7.188101187500000933 ) ) ;
#23400=CARTESIAN_POINT ( 'NONE',  ( -3.313708498984760720, -13.71875000409676915, -8.000000000000000000 ) ) ;
#23402=CARTESIAN_POINT ( 'NONE',  ( 9.999999999999998224, 15.00000000000000000, 0.7768758660237408131 ) ) ;
#23408=SHAPE_DEFINITION_REPRESENTATION ( #21843, #55690 ) ;
#23412=CARTESIAN_POINT ( 'NONE',  ( -2.701558353794592193, 15.00000000000000000, 9.999999999999998224 ) ) ;
#23467=CARTESIAN_POINT ( 'NONE',  ( -7.188101187500000044, -16.90625000204838813, -8.802885111219163269E-16 ) ) ;
#23470=CARTESIAN_POINT ( 'NONE',  ( 9.380894568449079429, 82.98869366889060473, -3.467341429141157949 ) ) ;
#23527=CARTESIAN_POINT ( 'NONE',  ( 7.188101187499999156, -28.25000000204838813, 2.977408999572654924 ) ) ;
#23534=CARTESIAN_POINT ( 'NONE',  ( 7.999999999999998224, -27.78125000409676915, 3.313708498984766493 ) ) ;
#23553=CARTESIAN_POINT ( 'NONE',  ( -10.00000000000000000, 15.00000000000000000, 3.082707893549380351 ) ) ;
#23576=CARTESIAN_POINT ( 'NONE',  ( -7.460363399255495409, -29.99999999999998934, 2.207551751280008467 ) ) ;
#23588=CARTESIAN_POINT ( 'NONE',  ( 3.487646406148667833, 15.95332971149351842, 9.373884331924859481 ) ) ;
#23605=CARTESIAN_POINT ( 'NONE',  ( 4.898587196589412829E-16, -16.62499999999999289, -8.000000000000000000 ) ) ;
#23621=CARTESIAN_POINT ( 'NONE',  ( 6.928203230275507885, 105.0000000000000000, -4.000000000000001776 ) ) ;
#23650=CARTESIAN_POINT ( 'NONE',  ( -1.469576158976823947E-15, -12.87499999999999467, 8.000000000000000000 ) ) ;
#23658=AXIS2_PLACEMENT_3D ( 'NONE', #87786, #28510, #20448 ) ;
#23669=AXIS2_PLACEMENT_3D ( 'NONE', #55909, #64580, #89388 ) ;
#23708=ORIENTED_EDGE ( 'NONE', *, *, #103537, .F. ) ;
#23717=PRESENTATION_STYLE_ASSIGNMENT (( #97557 ) ) ;
#23730=CARTESIAN_POINT ( 'NONE',  ( 5.656854249492378806, -27.68749999999999645, 5.656854249492381470 ) ) ;
#23733=ORIENTED_EDGE ( 'NONE', *, *, #79119, .T. ) ;
#23741=CARTESIAN_POINT ( 'NONE',  ( -5.082755093536325042, -11.46875000204838635, -5.082755093536325930 ) ) ;
#23787=CARTESIAN_POINT ( 'NONE',  ( -5.082755093536326818, -9.593750002048384573, 5.082755093536325042 ) ) ;
#23807=CARTESIAN_POINT ( 'NONE',  ( 7.212994264445060644, 107.0171134434003903, 3.463766307298588032 ) ) ;
#23813=CARTESIAN_POINT ( 'NONE',  ( -5.082755093536325042, -14.09375000204838457, -5.082755093536325930 ) ) ;
#23864=CARTESIAN_POINT ( 'NONE',  ( -2.977408999572650039, -11.56250000204838635, -7.188101187500000933 ) ) ;
#23872=CARTESIAN_POINT ( 'NONE',  ( 7.188101187499999156, -28.62500000204838813, 2.977408999572654924 ) ) ;
#23875=CARTESIAN_POINT ( 'NONE',  ( 4.401442555609581635E-16, -26.65625000204838813, -7.188101187500000044 ) ) ;
#23882=DIRECTION ( 'NONE',  ( 0.000000000000000000, 0.000000000000000000, 1.000000000000000000 ) ) ;
#23911=EDGE_LOOP ( 'NONE', ( #38593, #102910, #12599, #44600 ) ) ;
#23917=CARTESIAN_POINT ( 'NONE',  ( -2.977408999572654480, -24.50000000204839168, 7.188101187499999156 ) ) ;
#23933=CARTESIAN_POINT ( 'NONE',  ( -1.320432766682874540E-15, -13.53125000204838457, 7.188101187500000044 ) ) ;
#23947=CARTESIAN_POINT ( 'NONE',  ( 7.188101187500000044, -29.65625000204838813, 0.000000000000000000 ) ) ;
#23957=CARTESIAN_POINT ( 'NONE',  ( -4.397168787612346641, 15.00000000000000000, 9.999999999999998224 ) ) ;
#24006=CARTESIAN_POINT ( 'NONE',  ( -5.082755093536325042, -18.59375000204838457, -5.082755093536325930 ) ) ;
#24008=CARTESIAN_POINT ( 'NONE',  ( 10.00005432054556742, 80.99986419862088383, 0.2621623937322758446 ) ) ;
#24062=AXIS2_PLACEMENT_3D ( 'NONE', #34337, #52067, #59119 ) ;
#24065=CARTESIAN_POINT ( 'NONE',  ( -8.000000000000000000, -29.93750000409677270, -9.797174393178825657E-16 ) ) ;
#24073=CARTESIAN_POINT ( 'NONE',  ( -1.510421413154566572, 15.23810023151366977, -9.910377230549926253 ) ) ;
#24084=CARTESIAN_POINT ( 'NONE',  ( 5.656854249492380582, -15.50000000409677092, -5.656854249492379694 ) ) ;
#24115=CARTESIAN_POINT ( 'NONE',  ( 0.3465236330453798641, -30.00000000000000711, 7.243121741510847755 ) ) ;
#24127=FILL_AREA_STYLE ('',( #33267 ) ) ;
#24129=CARTESIAN_POINT ( 'NONE',  ( 5.656854249492380582, -12.50000000409676915, -5.656854249492379694 ) ) ;
#24162=CARTESIAN_POINT ( 'NONE',  ( 7.412906595240166041, 102.3581172714774539, 3.014362223629233561 ) ) ;
#24191=CARTESIAN_POINT ( 'NONE',  ( 7.999999999999998224, -14.09374999999999112, 3.313708498984766493 ) ) ;
#24197=CARTESIAN_POINT ( 'NONE',  ( 3.826949319562312102, 16.00000000000000000, -9.246271506234595705 ) ) ;
#24209=EDGE_CURVE ( 'NONE', #84434, #62970, #7972, .T. ) ;
#24223=CARTESIAN_POINT ( 'NONE',  ( -7.046357527897574968, 83.69384349398994516, -3.789683693877208270 ) ) ;
#24232=CARTESIAN_POINT ( 'NONE',  ( -4.903509839974908857, -29.96764154726693974, -6.410198659009853195 ) ) ;
#24256=CARTESIAN_POINT ( 'NONE',  ( 5.082755093536324154, -29.84375000204838813, 5.082755093536326818 ) ) ;
#24272=CARTESIAN_POINT ( 'NONE',  ( -7.188101187500000044, -9.781250002048384573, -8.802885111219163269E-16 ) ) ;
#24318=CARTESIAN_POINT ( 'NONE',  ( -1.469576158976823947E-15, -32.37499999999999289, 8.000000000000000000 ) ) ;
#24326=CARTESIAN_POINT ( 'NONE',  ( 4.898587196589412829E-16, -9.312500004096769146, -8.000000000000000000 ) ) ;
#24337=CARTESIAN_POINT ( 'NONE',  ( 7.414580834929599185, 107.6465628028148132, 3.010264818013836940 ) ) ;
#24344=CARTESIAN_POINT ( 'NONE',  ( -7.188101187500001821, -15.50000000204838635, -2.977408999572651371 ) ) ;
#24368=CARTESIAN_POINT ( 'NONE',  ( 4.898587196589412829E-16, -27.12499999999999645, -8.000000000000000000 ) ) ;
#24398=CARTESIAN_POINT ( 'NONE',  ( 2.977408999572650927, -16.25000000204838457, -7.188101187500000933 ) ) ;
#24407=CARTESIAN_POINT ( 'NONE',  ( -7.188101187500000044, -27.78125000204838813, -8.802885111219163269E-16 ) ) ;
#24426=CARTESIAN_POINT ( 'NONE',  ( -6.928203230275510549, 85.00000000000000000, -4.000000000000000000 ) ) ;
#24431=CARTESIAN_POINT ( 'NONE',  ( 9.797174393178825657E-16, -30.00000000000000000, -8.000000000000000000 ) ) ;
#24451=LINE ( 'NONE', #89683, #81152 ) ;
#24452=CARTESIAN_POINT ( 'NONE',  ( 9.165151389911681434, 30.00000000000000000, -4.000000000000000000 ) ) ;
#24453=CARTESIAN_POINT ( 'NONE',  ( 7.188101187500001821, -25.43750000204838813, -2.977408999572650483 ) ) ;
#24461=CARTESIAN_POINT ( 'NONE',  ( 9.482945380845301031, 87.44333058778930479, 3.177595346755237138 ) ) ;
#24466=CARTESIAN_POINT ( 'NONE',  ( 2.977408999572650927, -14.37500000204838280, -7.188101187500000933 ) ) ;
#24481=CARTESIAN_POINT ( 'NONE',  ( -2.977408999572654480, -31.62500000204838813, 7.188101187499999156 ) ) ;
#24532=CARTESIAN_POINT ( 'NONE',  ( 4.401442555609581635E-16, -21.78125000204838457, -7.188101187500000044 ) ) ;
#24590=CARTESIAN_POINT ( 'NONE',  ( -8.000000000000000000, -22.43750000409676915, -9.797174393178825657E-16 ) ) ;
#24598=CARTESIAN_POINT ( 'NONE',  ( -0.7060372491599424816, 15.23416508904354671, -9.999999999999998224 ) ) ;
#24631=CARTESIAN_POINT ( 'NONE',  ( -7.999912353029502654, 33.99982470603092821, -0.2691822806795013956 ) ) ;
#24640=CARTESIAN_POINT ( 'NONE',  ( -7.721181058141405096, -30.00000000000004263, -2.093648267354947912 ) ) ;
#24651=VERTEX_POINT ( 'NONE', #106383 ) ;
#24656=ORIENTED_EDGE ( 'NONE', *, *, #40221, .T. ) ;
#24670=CARTESIAN_POINT ( 'NONE',  ( -5.656854249492379694, -28.62500000409677270, -5.656854249492380582 ) ) ;
#24693=CARTESIAN_POINT ( 'NONE',  ( 9.253800200985681457, 106.3001033108817097, -3.791983798715485410 ) ) ;
#24778=CARTESIAN_POINT ( 'NONE',  ( -7.188101187500002709, -30.31250000204838813, 2.977408999572648707 ) ) ;
#24782=CARTESIAN_POINT ( 'NONE',  ( 2.701558353794771161, 15.00000000000000000, -9.999999999999998224 ) ) ;
#24836=CARTESIAN_POINT ( 'NONE',  ( 3.313708498984762052, -28.71874999999999289, -8.000000000000000000 ) ) ;
#24860=CARTESIAN_POINT ( 'NONE',  ( -5.082755093536326818, -15.21875000204838457, 5.082755093536325042 ) ) ;
#24863=EDGE_LOOP ( 'NONE', ( #23733, #5492, #44687, #54649 ) ) ;
#24867=FACE_OUTER_BOUND ( 'NONE', #23911, .T. ) ;
#24908=VERTEX_POINT ( 'NONE', #91696 ) ;
#24914=CARTESIAN_POINT ( 'NONE',  ( 5.082755093536324154, -10.71875000204838457, 5.082755093536326818 ) ) ;
#24917=CARTESIAN_POINT ( 'NONE',  ( 5.432263563190379507, -29.99999999999999645, 4.731163756734333425 ) ) ;
#24923=CARTESIAN_POINT ( 'NONE',  ( -7.188101187500001821, -21.87500000204838813, -2.977408999572651371 ) ) ;
#24945=DIRECTION ( 'NONE',  ( -0.000000000000000000, 1.000000000000000000, -0.000000000000000000 ) ) ;
#24966=CARTESIAN_POINT ( 'NONE',  ( 2.977408999572651815, -24.31250000204838813, 7.188101187500000933 ) ) ;
#24992=CARTESIAN_POINT ( 'NONE',  ( -2.977408999572654480, -28.62500000204838457, 7.188101187499999156 ) ) ;
#25043=CARTESIAN_POINT ( 'NONE',  ( 7.551892080562058851, 88.00987702539381985, 2.647003822403971807 ) ) ;
#25047=ORIENTED_EDGE ( 'NONE', *, *, #67216, .T. ) ;
#25055=CARTESIAN_POINT ( 'NONE',  ( -5.082755093536326818, -15.21875000204838457, 5.082755093536325042 ) ) ;
#25058=CARTESIAN_POINT ( 'NONE',  ( 9.483056940782031319, 82.55612209893422460, -3.177305548492596721 ) ) ;
#25096=ORIENTED_EDGE ( 'NONE', *, *, #89191, .T. ) ;
#25109=CARTESIAN_POINT ( 'NONE',  ( -2.977408999572650039, -29.18750000204839523, -7.188101187500000933 ) ) ;
#25118=CARTESIAN_POINT ( 'NONE',  ( 5.656854249492378806, -23.37500000409677270, 5.656854249492381470 ) ) ;
#25122=FACE_OUTER_BOUND ( 'NONE', #65, .T. ) ;
#25128=CARTESIAN_POINT ( 'NONE',  ( -3.997425403567602675, 15.99999999372935022, -9.168149550321206931 ) ) ;
#25129=ORIENTED_EDGE ( 'NONE', *, *, #5359, .F. ) ;
#25206=LINE ( 'NONE', #26286, #9441 ) ;
#25209=CARTESIAN_POINT ( 'NONE',  ( -1.469576158976823947E-15, -28.06250000409677270, 8.000000000000000000 ) ) ;
#25220=CARTESIAN_POINT ( 'NONE',  ( 7.618844049274128949, 101.8276410107053636, 2.450177051822848284 ) ) ;
#25252=CARTESIAN_POINT ( 'NONE',  ( -7.002990960197237769, 103.9473318161654163, 3.868040364119524011 ) ) ;
#25268=CARTESIAN_POINT ( 'NONE',  ( -7.721181058141405096, -30.00000000000004263, -2.093648267354947912 ) ) ;
#25286=CARTESIAN_POINT ( 'NONE',  ( -7.744168461338432508, 81.53745938284842509, 2.019395720771550273 ) ) ;
#25311=ORIENTED_EDGE ( 'NONE', *, *, #89578, .F. ) ;
#25316=CARTESIAN_POINT ( 'NONE',  ( 5.082755093536324154, -28.34375000204838813, 5.082755093536326818 ) ) ;
#25322=EDGE_CURVE ( 'NONE', #20242, #50908, #12872, .T. ) ;
#25352=CARTESIAN_POINT ( 'NONE',  ( 3.313708498984761608, -28.90625000409677270, -8.000000000000000000 ) ) ;
#25379=CARTESIAN_POINT ( 'NONE',  ( 8.000000000000000000, -27.49999999999999645, 0.000000000000000000 ) ) ;
#25405=CARTESIAN_POINT ( 'NONE',  ( 5.082755093536325930, -11.46875000204838635, -5.082755093536325042 ) ) ;
#25429=CARTESIAN_POINT ( 'NONE',  ( 4.898587196589412829E-16, -21.31250000409676915, -8.000000000000000000 ) ) ;
#25439=VERTEX_POINT ( 'NONE', #79898 ) ;
#25467=CARTESIAN_POINT ( 'NONE',  ( -2.977408999572654480, -15.50000000204838635, 7.188101187499999156 ) ) ;
#25471=CARTESIAN_POINT ( 'NONE',  ( -5.082755093536325042, -23.46875000204838457, -5.082755093536325930 ) ) ;
#25512=CARTESIAN_POINT ( 'NONE',  ( 9.176855344542989457, 29.47039573022589565, -3.973472207155926750 ) ) ;
#25514=CARTESIAN_POINT ( 'NONE',  ( -5.082755093536326818, -18.59375000204838457, 5.082755093536325042 ) ) ;
#25543=CARTESIAN_POINT ( 'NONE',  ( 7.188101187500000044, -31.15625000204838813, 0.000000000000000000 ) ) ;
#25594=CARTESIAN_POINT ( 'NONE',  ( 7.986711519608433285, 88.97361903623433932, -0.5300249774147592907 ) ) ;
#25604=CARTESIAN_POINT ( 'NONE',  ( -5.082755093536325042, -15.59375000204838635, -5.082755093536325930 ) ) ;
#25640=CYLINDRICAL_SURFACE ( 'NONE', #98594, 8.000000000000000000 ) ;
#25650=EDGE_CURVE ( 'NONE', #79080, #78182, #53394, .T. ) ;
#25662=CARTESIAN_POINT ( 'NONE',  ( 2.977408999572652260, -22.43750000204838813, 7.188101187500000044 ) ) ;
#25672=CARTESIAN_POINT ( 'NONE',  ( 5.656854249492380582, -26.00000000409677270, -5.656854249492379694 ) ) ;
#25677=CARTESIAN_POINT ( 'NONE',  ( 9.699121749566360862, 33.17668760275819295, 2.444499528233558205 ) ) ;
#25680=CARTESIAN_POINT ( 'NONE',  ( 0.000000000000000000, 15.00000000000000000, -9.999999999999998224 ) ) ;
#25683=CARTESIAN_POINT ( 'NONE',  ( 1.224646799147353256E-15, 115.0000000000000000, 10.00000000000000000 ) ) ;
#25697=AXIS2_PLACEMENT_3D ( 'NONE', #33220, #17026, #74700 ) ;
#25707=CARTESIAN_POINT ( 'NONE',  ( 5.656854249492380582, -12.31249999999999289, -5.656854249492379694 ) ) ;
#25713=ORIENTED_EDGE ( 'NONE', *, *, #41767, .F. ) ;
#25718=CARTESIAN_POINT ( 'NONE',  ( -8.000086790516059310, 34.00017358106006071, 0.2639471549312804033 ) ) ;
#25737=CARTESIAN_POINT ( 'NONE',  ( -5.656854249492379694, -22.43749999999999289, -5.656854249492380582 ) ) ;
#25740=CARTESIAN_POINT ( 'NONE',  ( 4.165977904505311358, 15.00000000000000000, 9.090909090909089940 ) ) ;
#25839=CARTESIAN_POINT ( 'NONE',  ( -6.944031699373469202, 84.46539345443871127, 3.972913591453821613 ) ) ;
#25872=CARTESIAN_POINT ( 'NONE',  ( 7.188101187499999156, -28.25000000204838813, 2.977408999572654924 ) ) ;
#25873=AXIS2_PLACEMENT_3D ( 'NONE', #81576, #74569, #67031 ) ;
#25930=CARTESIAN_POINT ( 'NONE',  ( 4.898587196589412829E-16, -22.62499999999999289, -8.000000000000000000 ) ) ;
#25931=CARTESIAN_POINT ( 'NONE',  ( -8.000000000000001776, -25.15624999999999645, 3.313708498984758943 ) ) ;
#25957=CARTESIAN_POINT ( 'NONE',  ( 7.188101187499999156, -14.75000000204838457, 2.977408999572654924 ) ) ;
#25958=CARTESIAN_POINT ( 'NONE',  ( 0.000000000000000000, -30.00000000000000000, 0.000000000000000000 ) ) ;
#26009=CARTESIAN_POINT ( 'NONE',  ( 2.977408999572652260, -12.31250000204838635, 7.188101187500000044 ) ) ;
#26017=CARTESIAN_POINT ( 'NONE',  ( -7.188101187500002709, -23.18750000204838813, 2.977408999572648707 ) ) ;
#26036=CIRCLE ( 'NONE', #101746, 1.000000000000000444 ) ;
#26060=CARTESIAN_POINT ( 'NONE',  ( -7.188101187500002709, -21.68750000204838813, 2.977408999572648707 ) ) ;
#26065=DIRECTION ( 'NONE',  ( -0.000000000000000000, -1.000000000000000000, -0.000000000000000000 ) ) ;
#26073=CARTESIAN_POINT ( 'NONE',  ( -5.082755093536326818, -9.218750002048382797, 5.082755093536325042 ) ) ;
#26083=CARTESIAN_POINT ( 'NONE',  ( 5.082755093536324154, -31.34375000204838457, 5.082755093536326818 ) ) ;
#26142=DIRECTION ( 'NONE',  ( 0.000000000000000000, 0.000000000000000000, -1.000000000000000000 ) ) ;
#26143=CARTESIAN_POINT ( 'NONE',  ( 7.188101187500000044, -14.65625000204838457, 0.000000000000000000 ) ) ;
#26144=CARTESIAN_POINT ( 'NONE',  ( -3.313708498984760276, -18.21875000409676915, -8.000000000000000000 ) ) ;
#26161=DIRECTION ( 'NONE',  ( 1.000000000000000000, -0.000000000000000000, -0.000000000000000000 ) ) ;
#26177=CARTESIAN_POINT ( 'NONE',  ( 3.313708498984761608, -10.71874999999999289, -8.000000000000000000 ) ) ;
#26197=CARTESIAN_POINT ( 'NONE',  ( 4.401442555609581635E-16, -24.78125000204838813, -7.188101187500000044 ) ) ;
#26208=CARTESIAN_POINT ( 'NONE',  ( -3.313708498984760720, -21.21875000409676915, -8.000000000000000000 ) ) ;
#26213=CARTESIAN_POINT ( 'NONE',  ( -1.469576158976823947E-15, -20.37499999999999289, 8.000000000000000000 ) ) ;
#26215=CARTESIAN_POINT ( 'NONE',  ( -3.836411046842014727, 15.00000000000001066, -9.999999999999959144 ) ) ;
#26258=CARTESIAN_POINT ( 'NONE',  ( -8.000000000000001776, -20.84375000409677270, 3.313708498984759387 ) ) ;
#26286=CARTESIAN_POINT ( 'NONE',  ( 10.00000000000000000, 15.00000000000000000, 10.00000000000000000 ) ) ;
#26289=DIRECTION ( 'NONE',  ( 0.000000000000000000, 0.000000000000000000, 1.000000000000000000 ) ) ;
#26338=CARTESIAN_POINT ( 'NONE',  ( -6.928203230275509661, 104.7311667549100491, -4.000000000000001776 ) ) ;
#26353=CARTESIAN_POINT ( 'NONE',  ( -8.000000000000000000, -29.96764154942184888, -1.065389812439802020 ) ) ;
#26375=FACE_OUTER_BOUND ( 'NONE', #31516, .T. ) ;
#26445=EDGE_LOOP ( 'NONE', ( #5907, #88414, #14815, #11005 ) ) ;
#26450=CARTESIAN_POINT ( 'NONE',  ( -3.313708498984765161, -29.46874999999999645, 7.999999999999998224 ) ) ;
#26469=CARTESIAN_POINT ( 'NONE',  ( 7.150931910075644105, 106.7862579852226332, -3.588457848165351738 ) ) ;
#26473=CARTESIAN_POINT ( 'NONE',  ( -9.948513602187995630, 88.86977943343859465, 1.045942665286138107 ) ) ;
#26474=CARTESIAN_POINT ( 'NONE',  ( -1.320432766682874540E-15, -10.53125000204838457, 7.188101187500000044 ) ) ;
#26509=EDGE_CURVE ( 'NONE', #45637, #84193, #16933, .T. ) ;
#26513=DIRECTION ( 'NONE',  ( -0.000000000000000000, -1.000000000000000000, -0.000000000000000000 ) ) ;
#26534=CARTESIAN_POINT ( 'NONE',  ( 4.021832409241297590, -29.99999999999998224, 5.962323058997216485 ) ) ;
#26539=CARTESIAN_POINT ( 'NONE',  ( 7.188101187499999156, -21.12500000204838813, 2.977408999572654924 ) ) ;
#26553=CARTESIAN_POINT ( 'NONE',  ( 7.999999999999998224, -14.09374999999999112, 3.313708498984766049 ) ) ;
#26584=CARTESIAN_POINT ( 'NONE',  ( 5.082755093536325930, -17.84375000204838457, -5.082755093536325042 ) ) ;
#26606=CARTESIAN_POINT ( 'NONE',  ( -2.977408999572654480, -24.12500000204838457, 7.188101187499999156 ) ) ;
#26640=CARTESIAN_POINT ( 'NONE',  ( -1.469576158976823947E-15, -19.06250000409677270, 8.000000000000000000 ) ) ;
#26653=CARTESIAN_POINT ( 'NONE',  ( 7.188101187499999156, -24.12500000204838813, 2.977408999572654924 ) ) ;
#26660=CARTESIAN_POINT ( 'NONE',  ( -5.082755093536325042, -14.09375000204838457, -5.082755093536325930 ) ) ;
#26661=CARTESIAN_POINT ( 'NONE',  ( -8.000000000000001776, -17.84375000409676915, 3.313708498984759387 ) ) ;
#26701=CARTESIAN_POINT ( 'NONE',  ( 7.002641335706727865, 83.94912737319167206, 3.868676264653293728 ) ) ;
#26721=CARTESIAN_POINT ( 'NONE',  ( -2.977408999572650039, -26.18750000204838457, -7.188101187500000933 ) ) ;
#26731=CARTESIAN_POINT ( 'NONE',  ( 8.000000000000000000, -26.09375000409677270, -3.313708498984761608 ) ) ;
#26736=CARTESIAN_POINT ( 'NONE',  ( 9.646083234704169840, 33.01290609023479306, -2.643797197754292228 ) ) ;
#26797=FACE_OUTER_BOUND ( 'NONE', #72133, .T. ) ;
#26811=SURFACE_STYLE_USAGE ( .BOTH. , #35430 ) ;
#26861=CARTESIAN_POINT ( 'NONE',  ( 5.656854249492380582, -10.81249999999999289, -5.656854249492379694 ) ) ;
#26864=CARTESIAN_POINT ( 'NONE',  ( -7.150931910075641440, 103.2137420147773526, -3.588457848165358843 ) ) ;
#26872=CARTESIAN_POINT ( 'NONE',  ( -10.00000000000000355, 105.0000000000000000, 0.000000000000000000 ) ) ;
#26873=CARTESIAN_POINT ( 'NONE',  ( -1.469576158976823947E-15, -18.87499999999999289, 8.000000000000000000 ) ) ;
#26890=CARTESIAN_POINT ( 'NONE',  ( -9.918010731619574472, 108.7915168484322521, -1.300854425901575073 ) ) ;
#26901=CARTESIAN_POINT ( 'NONE',  ( -8.000000000000000000, -24.03125000409677270, -3.313708498984762496 ) ) ;
#26902=ORIENTED_EDGE ( 'NONE', *, *, #12769, .F. ) ;
#26934=CARTESIAN_POINT ( 'NONE',  ( 4.898587196589412829E-16, -13.62499999999999112, -8.000000000000000000 ) ) ;
#26975=CARTESIAN_POINT ( 'NONE',  ( -8.000000000000000000, -28.34374999999999289, -3.313708498984762496 ) ) ;
#27018=ORIENTED_EDGE ( 'NONE', *, *, #89607, .F. ) ;
#27028=CARTESIAN_POINT ( 'NONE',  ( -5.656854249492381470, -25.06249999999999289, 5.656854249492379694 ) ) ;
#27070=CARTESIAN_POINT ( 'NONE',  ( 5.082755093536324154, -21.21875000204838813, 5.082755093536326818 ) ) ;
#27078=CARTESIAN_POINT ( 'NONE',  ( -5.656854249492379694, -15.12500000409677092, -5.656854249492380582 ) ) ;
#27084=CARTESIAN_POINT ( 'NONE',  ( -7.800703710507058908, 88.58595692657945619, 1.791736796405269505 ) ) ;
#27108=CARTESIAN_POINT ( 'NONE',  ( -1.320432766682874540E-15, -16.90625000204838813, 7.188101187500000044 ) ) ;
#27123=CARTESIAN_POINT ( 'NONE',  ( -4.413590570192279294, -9.188952443232103917, 5.751919616880372566 ) ) ;
#27135=CARTESIAN_POINT ( 'NONE',  ( 7.188101187500000044, -23.65625000204838457, 0.000000000000000000 ) ) ;
#27154=CARTESIAN_POINT ( 'NONE',  ( -5.656854249492381470, -22.25000000409676915, 5.656854249492379694 ) ) ;
#27165=ORIENTED_EDGE ( 'NONE', *, *, #16738, .F. ) ;
#27184=CARTESIAN_POINT ( 'NONE',  ( -2.977408999572654480, -27.50000000204838457, 7.188101187499999156 ) ) ;
#27194=CARTESIAN_POINT ( 'NONE',  ( -7.188101187500001821, -15.50000000204838635, -2.977408999572651371 ) ) ;
#27233=ORIENTED_EDGE ( 'NONE', *, *, #10371, .F. ) ;
#27235=CARTESIAN_POINT ( 'NONE',  ( 7.800703710507058908, 81.41404307342060065, 1.791736796405269061 ) ) ;
#27258=CARTESIAN_POINT ( 'NONE',  ( -2.977408999572650039, -27.68750000204838457, -7.188101187500000933 ) ) ;
#27267=CARTESIAN_POINT ( 'NONE',  ( -9.333555687487613994, 83.21897303391028800, 3.591168747312688314 ) ) ;
#27269=CARTESIAN_POINT ( 'NONE',  ( 5.656854249492378806, -20.37500000409677270, 5.656854249492381470 ) ) ;
#27279=CARTESIAN_POINT ( 'NONE',  ( 2.625273426274975730, -29.99999999999998934, -7.180406059207282254 ) ) ;
#27300=ORIENTED_EDGE ( 'NONE', *, *, #25650, .T. ) ;
#27336=CARTESIAN_POINT ( 'NONE',  ( 3.316968746324327366, 15.92795519102023860, 9.435590127032936536 ) ) ;
#27355=VECTOR ( 'NONE', #95339, 1000.000000000000000 ) ;
#27403=CARTESIAN_POINT ( 'NONE',  ( -6.944371705245973914, 104.4610030857544984, -3.972324460300566074 ) ) ;
#27439=CARTESIAN_POINT ( 'NONE',  ( 4.898587196589412829E-16, -24.31250000409677270, -8.000000000000000000 ) ) ;
#27445=CARTESIAN_POINT ( 'NONE',  ( -3.999995229665001428, -8.688226215992830959, 6.928205984420947594 ) ) ;
#27449=EDGE_LOOP ( 'NONE', ( #64676, #83979, #61838, #87305, #975, #101894, #33292, #45036, #37605 ) ) ;
#27452=CARTESIAN_POINT ( 'NONE',  ( -8.000000000000000000, -28.34374999999999289, -3.313708498984762496 ) ) ;
#27471=CARTESIAN_POINT ( 'NONE',  ( -8.000000000000000000, -13.24999999999999467, -9.797174393178825657E-16 ) ) ;
#27487=CIRCLE ( 'NONE', #43001, 10.00000000000000000 ) ;
#27518=CARTESIAN_POINT ( 'NONE',  ( -8.000000000000001776, -20.65624999999998934, 3.313708498984758943 ) ) ;
#27521=CIRCLE ( 'NONE', #17097, 1.000000000000000888 ) ;
#27583=FILL_AREA_STYLE_COLOUR ( '', #39273 ) ;
#27587=CARTESIAN_POINT ( 'NONE',  ( -9.537927238823506570, 102.3537314288182074, -3.010735687602419386 ) ) ;
#27605=CARTESIAN_POINT ( 'NONE',  ( 5.082755093536325930, -11.84375000204838635, -5.082755093536325042 ) ) ;
#27609=CARTESIAN_POINT ( 'NONE',  ( 4.898587196589412829E-16, -10.62499999999999289, -8.000000000000000000 ) ) ;
#27645=CARTESIAN_POINT ( 'NONE',  ( 9.333079356992101339, 28.22166919925128425, 3.592383266237780592 ) ) ;
#27646=CARTESIAN_POINT ( 'NONE',  ( 2.977408999572650927, -17.75000000204838457, -7.188101187500001821 ) ) ;
#27648=EDGE_CURVE ( 'NONE', #7449, #42837, #36391, .T. ) ;
#27650=AXIS2_PLACEMENT_3D ( 'NONE', #52396, #26065, #60003 ) ;
#27675=CARTESIAN_POINT ( 'NONE',  ( -5.082755093536326818, -25.71875000204838813, 5.082755093536325042 ) ) ;
#27681=VERTEX_POINT ( 'NONE', #50353 ) ;
#27687=CARTESIAN_POINT ( 'NONE',  ( 5.656854249492378806, -17.18749999999999289, 5.656854249492381470 ) ) ;
#27691=CARTESIAN_POINT ( 'NONE',  ( 9.536842176398144133, 102.3576463011601021, 3.014135744008186180 ) ) ;
#27704=CARTESIAN_POINT ( 'NONE',  ( 3.313708498984743844, -26.28125000000000000, 8.000000000000017764 ) ) ;
#27727=CARTESIAN_POINT ( 'NONE',  ( -7.188101187500002709, -26.18750000204838457, 2.977408999572647819 ) ) ;
#27738=CARTESIAN_POINT ( 'NONE',  ( -2.977408999572654480, -30.50000000204838813, 7.188101187499999156 ) ) ;
#27744=CARTESIAN_POINT ( 'NONE',  ( -5.656854249492379694, -14.93749999999999289, -5.656854249492380582 ) ) ;
#27768=ORIENTED_EDGE ( 'NONE', *, *, #65597, .F. ) ;
#27773=CARTESIAN_POINT ( 'NONE',  ( 3.313708498984800688, -11.28124999999998934, 7.999999999999960032 ) ) ;
#27795=CARTESIAN_POINT ( 'NONE',  ( -1.320432766682874540E-15, -25.53125000204838813, 7.188101187500000044 ) ) ;
#27799=CYLINDRICAL_SURFACE ( 'NONE', #23081, 8.000000000000000000 ) ;
#27805=CARTESIAN_POINT ( 'NONE',  ( -3.313708498984765161, -16.15625000409677270, 7.999999999999998224 ) ) ;
#27830=( NAMED_UNIT ( * ) SI_UNIT ( $, .STERADIAN. ) SOLID_ANGLE_UNIT ( ) );
#27867=CARTESIAN_POINT ( 'NONE',  ( -5.082755093536326818, -30.21875000204838813, 5.082755093536325042 ) ) ;
#27871=CARTESIAN_POINT ( 'NONE',  ( -3.484792534604214342, 15.95825086476136967, 9.380155525692146057 ) ) ;
#27877=ORIENTED_EDGE ( 'NONE', *, *, #103459, .T. ) ;
#27879=VECTOR ( 'NONE', #44670, 1000.000000000000000 ) ;
#27904=ORIENTED_EDGE ( 'NONE', *, *, #95483, .T. ) ;
#27926=EDGE_CURVE ( 'NONE', #88535, #41081, #9997, .T. ) ;
#27933=CARTESIAN_POINT ( 'NONE',  ( -7.344361273354515163, 102.5543946941147766, -3.175733139645589009 ) ) ;
#27934=CARTESIAN_POINT ( 'NONE',  ( 9.090909090909088164, 16.00000000000000000, 4.165977904505314910 ) ) ;
#27973=FACE_OUTER_BOUND ( 'NONE', #27449, .T. ) ;
#27993=FACE_OUTER_BOUND ( 'NONE', #28272, .T. ) ;
#28013=DIRECTION ( 'NONE',  ( -1.734723475976807094E-16, -0.000000000000000000, -1.000000000000000000 ) ) ;
#28046=CARTESIAN_POINT ( 'NONE',  ( 7.999999999999998224, -23.09374999999999645, 3.313708498984766493 ) ) ;
#28047=VECTOR ( 'NONE', #24945, 1000.000000000000000 ) ;
#28068=CARTESIAN_POINT ( 'NONE',  ( 2.977408999572650927, -9.875000002048386349, -7.188101187500001821 ) ) ;
#28095=CARTESIAN_POINT ( 'NONE',  ( -9.989690267985800176, 26.02555583405089479, -0.5238310916885813295 ) ) ;
#28112=CARTESIAN_POINT ( 'NONE',  ( -9.176803346051512378, 104.4705284420256106, 3.973598758023531019 ) ) ;
#28114=CARTESIAN_POINT ( 'NONE',  ( 4.165977904505312246, 16.00000000000000000, -9.090909090909088164 ) ) ;
#28124=CARTESIAN_POINT ( 'NONE',  ( 8.000000000000000000, -18.68750000409676915, 0.000000000000000000 ) ) ;
#28130=CARTESIAN_POINT ( 'NONE',  ( 2.977408999572651815, -16.81250000204838457, 7.188101187500000933 ) ) ;
#28165=VERTEX_POINT ( 'NONE', #64196 ) ;
#28172=CARTESIAN_POINT ( 'NONE',  ( 4.401442555609581635E-16, -13.15625000204838280, -7.188101187500000044 ) ) ;
#28202=CARTESIAN_POINT ( 'NONE',  ( -2.977408999572650039, -27.68750000204838813, -7.188101187500001821 ) ) ;
#28219=CARTESIAN_POINT ( 'NONE',  ( 9.698972129396508990, 101.8237028725806113, -2.445345647270323663 ) ) ;
#28248=CARTESIAN_POINT ( 'NONE',  ( 7.188101187500000933, -28.43750000204839523, -2.977408999572650483 ) ) ;
#28257=CARTESIAN_POINT ( 'NONE',  ( 7.188101187500001821, -10.06250000204838280, -2.977408999572650483 ) ) ;
#28267=VERTEX_POINT ( 'NONE', #13831 ) ;
#28272=EDGE_LOOP ( 'NONE', ( #12106, #1135, #104252, #78407 ) ) ;
#28296=CARTESIAN_POINT ( 'NONE',  ( 7.188101187500001821, -31.43750000204839168, -2.977408999572650483 ) ) ;
#28309=CARTESIAN_POINT ( 'NONE',  ( -7.188101187500000044, -21.40625000204838457, -8.802885111219163269E-16 ) ) ;
#28317=CARTESIAN_POINT ( 'NONE',  ( 8.000000000000000000, -17.09375000409676915, -3.313708498984761608 ) ) ;
#28330=CARTESIAN_POINT ( 'NONE',  ( 0.000000000000000000, -30.00000000000000000, 0.000000000000000000 ) ) ;
#28382=CARTESIAN_POINT ( 'NONE',  ( -5.082755093536326818, -25.71875000204838813, 5.082755093536325042 ) ) ;
#28383=ORIENTED_EDGE ( 'NONE', *, *, #45470, .F. ) ;
#28386=CARTESIAN_POINT ( 'NONE',  ( -1.749942564367552134, 15.56091200510339512, 9.852211596319792264 ) ) ;
#28387=LINE ( 'NONE', #19778, #62267 ) ;
#28446=CARTESIAN_POINT ( 'NONE',  ( -7.897196874019794421, 101.2087279583219299, -1.302055520192093141 ) ) ;
#28450=FACE_OUTER_BOUND ( 'NONE', #77419, .T. ) ;
#28473=FACE_OUTER_BOUND ( 'NONE', #78034, .T. ) ;
#28479=CARTESIAN_POINT ( 'NONE',  ( -10.00005432054556742, 109.0001358013791304, 0.2621623937322789533 ) ) ;
#28510=DIRECTION ( 'NONE',  ( 1.000000000000000000, -0.000000000000000000, -0.000000000000000000 ) ) ;
#28518=CARTESIAN_POINT ( 'NONE',  ( 0.000000000000000000, -30.00000000000000000, 0.000000000000000000 ) ) ;
#28530=ORIENTED_EDGE ( 'NONE', *, *, #46857, .F. ) ;
#28546=ORIENTED_EDGE ( 'NONE', *, *, #24209, .F. ) ;
#28559=CARTESIAN_POINT ( 'NONE',  ( -9.246271506234601034, 16.00000000000000000, -3.826949319562308105 ) ) ;
#28562=ORIENTED_EDGE ( 'NONE', *, *, #83989, .F. ) ;
#28567=CARTESIAN_POINT ( 'NONE',  ( -8.000000000000000000, -23.74999999999999289, -9.797174393178825657E-16 ) ) ;
#28625=CARTESIAN_POINT ( 'NONE',  ( -9.918325909156573417, 26.20764768292568903, 1.298699613733151459 ) ) ;
#28643=CARTESIAN_POINT ( 'NONE',  ( 4.210530276628051460, 15.00000000000000000, -9.999999999999998224 ) ) ;
#28659=CARTESIAN_POINT ( 'NONE',  ( -7.188101187500000044, -14.28125000204838457, -8.802885111219163269E-16 ) ) ;
#28671=CARTESIAN_POINT ( 'NONE',  ( -1.469576158976823947E-15, -14.37499999999999112, 8.000000000000000000 ) ) ;
#28695=CARTESIAN_POINT ( 'NONE',  ( 7.046357527897571416, 31.30615650601003352, -3.789683693877207826 ) ) ;
#28703=CARTESIAN_POINT ( 'NONE',  ( 2.977408999572650927, -11.75000000204838813, -7.188101187500001821 ) ) ;
#28728=CARTESIAN_POINT ( 'NONE',  ( -7.188101187500001821, -24.50000000204839168, -2.977408999572651371 ) ) ;
#28732=COLOUR_RGB ( '', 0.31764706, 0.68627451, 0.89019608) ;
#28752=CARTESIAN_POINT ( 'NONE',  ( 9.380894568449075877, 102.9886936688906047, -3.467341429141160170 ) ) ;
#28788=CARTESIAN_POINT ( 'NONE',  ( 4.401442555609581635E-16, -23.65625000204838457, -7.188101187500000044 ) ) ;
#28798=CARTESIAN_POINT ( 'NONE',  ( 5.082755093536325930, -32.84375000204838813, -5.082755093536325042 ) ) ;
#28843=CARTESIAN_POINT ( 'NONE',  ( 7.188101187500001821, -28.43750000204839168, -2.977408999572650483 ) ) ;
#28854=VERTEX_POINT ( 'NONE', #38574 ) ;
#28859=CARTESIAN_POINT ( 'NONE',  ( -5.082755093536326818, -21.21875000204838457, 5.082755093536325042 ) ) ;
#28866=CARTESIAN_POINT ( 'NONE',  ( -9.989690267985798400, 81.02555583405090545, -0.5238310916885774438 ) ) ;
#28869=CARTESIAN_POINT ( 'NONE',  ( 5.656854249492378806, -15.87500000409677092, 5.656854249492381470 ) ) ;
#28904=CARTESIAN_POINT ( 'NONE',  ( 0.000000000000000000, -30.00000000000000000, 0.000000000000000000 ) ) ;
#28931=CARTESIAN_POINT ( 'NONE',  ( -2.977408999572650039, -27.68750000204838813, -7.188101187500001821 ) ) ;
#28961=CARTESIAN_POINT ( 'NONE',  ( 4.165977904505308693, 16.00000000000000000, 9.090909090909091717 ) ) ;
#28968=VERTEX_POINT ( 'NONE', #98377 ) ;
#29028=( LENGTH_UNIT ( ) NAMED_UNIT ( * ) SI_UNIT ( .MILLI., .METRE. ) );
#29034=CARTESIAN_POINT ( 'NONE',  ( -9.536842176398140580, 107.6423536988398553, 3.014135744008186624 ) ) ;
#29057=CARTESIAN_POINT ( 'NONE',  ( -1.469576158976823947E-15, -14.56250000409677092, 8.000000000000000000 ) ) ;
#29073=EDGE_CURVE ( 'NONE', #93124, #6205, #18456, .T. ) ;
#29100=CARTESIAN_POINT ( 'NONE',  ( 9.221216839714873714, 106.0475974816897917, 3.869414262756992517 ) ) ;
#29107=DIRECTION ( 'NONE',  ( -1.734723475976807094E-16, -0.000000000000000000, -1.000000000000000000 ) ) ;
#29123=CARTESIAN_POINT ( 'NONE',  ( -5.656854249492379694, -19.43749999999999289, -5.656854249492380582 ) ) ;
#29130=AXIS2_PLACEMENT_3D ( 'NONE', #54142, #103776, #38024 ) ;
#29170=CARTESIAN_POINT ( 'NONE',  ( -9.797936955406314041, 26.53328310229516518, -2.012343231877595340 ) ) ;
#29171=CARTESIAN_POINT ( 'NONE',  ( -8.000000000000000000, -26.84374999999999289, -3.313708498984762496 ) ) ;
#29172=CARTESIAN_POINT ( 'NONE',  ( 0.000000000000000000, -30.00000000000000000, 0.000000000000000000 ) ) ;
#29206=CARTESIAN_POINT ( 'NONE',  ( -7.188101187500001821, -14.37500000204838635, -2.977408999572651371 ) ) ;
#29214=CARTESIAN_POINT ( 'NONE',  ( -8.000000000000000000, -15.03125000409677092, -3.313708498984762496 ) ) ;
#29234=CARTESIAN_POINT ( 'NONE',  ( 7.344133061198930612, 32.44494392680575601, 3.176267128233873471 ) ) ;
#29237=CARTESIAN_POINT ( 'NONE',  ( 0.000000000000000000, -30.00000000000000000, 8.000000000000000000 ) ) ;
#29241=CARTESIAN_POINT ( 'NONE',  ( -2.977408999572654480, -15.50000000204838635, 7.188101187499999156 ) ) ;
#29266=CARTESIAN_POINT ( 'NONE',  ( -7.188101187500001821, -20.00000000204838813, -2.977408999572651371 ) ) ;
#29277=VERTEX_POINT ( 'NONE', #96136 ) ;
#29311=CARTESIAN_POINT ( 'NONE',  ( 5.082755093536324154, -18.21875000204838457, 5.082755093536326818 ) ) ;
#29319=CARTESIAN_POINT ( 'NONE',  ( -7.188101187500000044, -32.28125000204838813, -8.802885111219163269E-16 ) ) ;
#29338=B_SPLINE_CURVE_WITH_KNOTS ( 'NONE', 3,
 ( #70348, #47111, #62274, #104836, #94089, #53099, #86022, #87072, #12092, #48170, #9164, #1601, #56791, #64903, #76036, #66901, #31504, #67438, #43154, #26473, #32022, #15285, #14739, #89716, #105364, #97785, #42608, #64385, #97261, #34028, #55717, #80539, #18365, #58815 ),
 .UNSPECIFIED., .F., .F.,
 ( 4, 2, 2, 2, 2, 2, 2, 2, 2, 2, 2, 2, 2, 2, 2, 2, 4 ),
 ( 1.422579022190208801E-17, 0.0007899309203816185692, 0.001579861840763223044, 0.002369792761144827193, 0.003159723681526431776, 0.003949654601908035925, 0.004739585522289639641, 0.005529516442671244224, 0.006319447363052848807, 0.007109378283434453390, 0.007899309203816057973, 0.008689240124197661688, 0.009479171044579265404, 0.01026910196496087085, 0.01105903288534247457, 0.01184896380572408002, 0.01263889472610568374 ),
 .UNSPECIFIED. ) ;
#29360=CARTESIAN_POINT ( 'NONE',  ( -2.977408999572654480, -32.00000000204838813, 7.188101187499999156 ) ) ;
#29373=CARTESIAN_POINT ( 'NONE',  ( 7.188101187500000933, -16.06250000204838457, -2.977408999572650483 ) ) ;
#29385=CARTESIAN_POINT ( 'NONE',  ( 8.000000000000000000, -15.59375000409677270, -3.313708498984761608 ) ) ;
#29387=CARTESIAN_POINT ( 'NONE',  ( 9.999999999999996447, 15.00000000000000000, 4.582575694955847823 ) ) ;
#29451=CARTESIAN_POINT ( 'NONE',  ( 7.188101187500001821, -25.06250000204838457, -2.977408999572650483 ) ) ;
#29498=ORIENTED_EDGE ( 'NONE', *, *, #61575, .F. ) ;
#29499=EDGE_CURVE ( 'NONE', #33789, #70286, #378, .T. ) ;
#29571=ADVANCED_FACE ( 'NONE', ( #30224 ), #22138, .T. ) ;
#29576=LINE ( 'NONE', #62448, #27355 ) ;
#29625=CARTESIAN_POINT ( 'NONE',  ( -9.380155525692149610, 15.95825086476136967, -3.484792534604211234 ) ) ;
#29633=CARTESIAN_POINT ( 'NONE',  ( 8.000000000000000000, -22.90624999999999645, -3.313708498984761608 ) ) ;
#29683=CARTESIAN_POINT ( 'NONE',  ( -9.165151389911679658, 30.00000000000000000, 4.000000000000000000 ) ) ;
#29703=CARTESIAN_POINT ( 'NONE',  ( -9.699121749566359085, 101.8233123972417928, 2.444499528233565755 ) ) ;
#29718=CARTESIAN_POINT ( 'NONE',  ( 2.977408999572650927, -14.75000000204838457, -7.188101187500001821 ) ) ;
#29729=VERTEX_POINT ( 'NONE', #11220 ) ;
#29752=CARTESIAN_POINT ( 'NONE',  ( 6.944031699373469202, 30.53460654556128162, 3.972913591453821613 ) ) ;
#29753=CARTESIAN_POINT ( 'NONE',  ( -6.928203230275510549, 29.73520732746428408, 3.999999999999999112 ) ) ;
#29757=CARTESIAN_POINT ( 'NONE',  ( 4.898587196589412829E-16, -21.12499999999999289, -8.000000000000000000 ) ) ;
#29759=CARTESIAN_POINT ( 'NONE',  ( 4.401442555609581635E-16, -14.65625000204838457, -7.188101187500000044 ) ) ;
#29787=CARTESIAN_POINT ( 'NONE',  ( -5.082755093536325042, -21.59375000204838457, -5.082755093536325930 ) ) ;
#29833=CARTESIAN_POINT ( 'NONE',  ( 7.188101187499999156, -21.12500000204838813, 2.977408999572654924 ) ) ;
#29843=CARTESIAN_POINT ( 'NONE',  ( -7.188101187500000044, -30.78125000204838813, -8.802885111219163269E-16 ) ) ;
#29882=CARTESIAN_POINT ( 'NONE',  ( 7.188101187500000044, -31.53125000204838457, 0.000000000000000000 ) ) ;
#29892=CARTESIAN_POINT ( 'NONE',  ( 4.401442555609581635E-16, -21.78125000204838457, -7.188101187500000044 ) ) ;
#29900=CARTESIAN_POINT ( 'NONE',  ( 5.656854249492380582, -12.50000000409676915, -5.656854249492379694 ) ) ;
#29905=CARTESIAN_POINT ( 'NONE',  ( 5.656854249492380582, -19.81249999999999289, -5.656854249492379694 ) ) ;
#29908=CARTESIAN_POINT ( 'NONE',  ( -9.989435848181784650, 33.97380292528427503, -0.5278651953176126677 ) ) ;
#29935=CARTESIAN_POINT ( 'NONE',  ( 9.999999999999996447, 0.000000000000000000, -10.00000000000000000 ) ) ;
#29961=CARTESIAN_POINT ( 'NONE',  ( 9.797174393178825657E-16, -30.00000000000000000, -8.000000000000000000 ) ) ;
#29963=FACE_OUTER_BOUND ( 'NONE', #94187, .T. ) ;
#29964=CARTESIAN_POINT ( 'NONE',  ( 5.082755093536324154, -23.84375000204838457, 5.082755093536326818 ) ) ;
#29966=CARTESIAN_POINT ( 'NONE',  ( 9.165151389911681434, 30.00000000000000000, -4.000000000000000000 ) ) ;
#29967=CARTESIAN_POINT ( 'NONE',  ( -8.000000000000001776, -23.65624999999999645, 3.313708498984759387 ) ) ;
#30030=CARTESIAN_POINT ( 'NONE',  ( -8.000000000000001776, -29.84375000409677270, 3.313708498984758943 ) ) ;
#30038=ORIENTED_EDGE ( 'NONE', *, *, #95678, .T. ) ;
#30083=CARTESIAN_POINT ( 'NONE',  ( 7.999999999999998224, -14.28125000409677092, 3.313708498984766049 ) ) ;
#30122=ORIENTED_EDGE ( 'NONE', *, *, #39704, .T. ) ;
#30149=CARTESIAN_POINT ( 'NONE',  ( 5.656854249492380582, -12.31249999999999289, -5.656854249492379694 ) ) ;
#30170=CARTESIAN_POINT ( 'NONE',  ( 9.910377230549942240, 15.23810023151299653, -1.510421413154837245 ) ) ;
#30193=VECTOR ( 'NONE', #26513, 1000.000000000000000 ) ;
#30194=CARTESIAN_POINT ( 'NONE',  ( -9.165151389911684987, 29.73289218717087223, -4.000000000000000888 ) ) ;
#30211=CARTESIAN_POINT ( 'NONE',  ( -9.090909090909095269, 15.00000000000000000, -4.165977904505304252 ) ) ;
#30216=SURFACE_STYLE_USAGE ( .BOTH. , #36745 ) ;
#30224=FACE_OUTER_BOUND ( 'NONE', #22574, .T. ) ;
#30229=CARTESIAN_POINT ( 'NONE',  ( 4.401442555609581635E-16, -10.15625000204838457, -7.188101187500000044 ) ) ;
#30231=COLOUR_RGB ( '', 0.31764706, 0.68627451, 0.89019608) ;
#30237=CARTESIAN_POINT ( 'NONE',  ( 8.000000000000000000, -24.40624999999999289, -3.313708498984761164 ) ) ;
#30255=CARTESIAN_POINT ( 'NONE',  ( 8.000000000000000000, -26.09375000409676915, -3.313708498984761164 ) ) ;
#30257=CARTESIAN_POINT ( 'NONE',  ( 4.898587196589412829E-16, -16.81250000409677270, -8.000000000000000000 ) ) ;
#30263=ORIENTED_EDGE ( 'NONE', *, *, #95268, .F. ) ;
#30266=CARTESIAN_POINT ( 'NONE',  ( 7.934996450857311423, 33.86862456472530170, -1.050865690281770126 ) ) ;
#30274=CARTESIAN_POINT ( 'NONE',  ( -7.188101187500002709, -11.18750000204838457, 2.977408999572648707 ) ) ;
#30298=EDGE_CURVE ( 'NONE', #56071, #90051, #36783, .T. ) ;
#30302=CARTESIAN_POINT ( 'NONE',  ( 5.082755093536325930, -17.46875000204838457, -5.082755093536325042 ) ) ;
#30350=CARTESIAN_POINT ( 'NONE',  ( 7.188101187500000933, -17.93750000204838457, -2.977408999572650483 ) ) ;
#30361=CARTESIAN_POINT ( 'NONE',  ( -7.188101187500000044, -24.78125000204838813, -8.802885111219163269E-16 ) ) ;
#30364=( BOUNDED_CURVE ( )  B_SPLINE_CURVE ( 2, ( #26873, #85072, #33885, #60290, #91050, #9033, #41941, #50030, #59742 ),
 .UNSPECIFIED., .F., .F. ) 
 B_SPLINE_CURVE_WITH_KNOTS ( ( 3, 2, 2, 2, 3 ),
 ( 0.6323529411764706731, 0.6397058823529412352, 0.6470588235294119084, 0.6544117647058823595, 0.6617647058823529216 ),
 .UNSPECIFIED. ) 
 CURVE ( )  GEOMETRIC_REPRESENTATION_ITEM ( )  RATIONAL_B_SPLINE_CURVE ( ( 0.9999999999999988898, 0.9238795325112878487, 1.000000000000000000, 0.9238795325112867385, 1.000000000000000000, 0.9238795325112867385, 1.000000000000000000, 0.9238795325112867385, 1.000000000000000000 ) ) 
 REPRESENTATION_ITEM ( '' )  );
#30405=CARTESIAN_POINT ( 'NONE',  ( 5.082755093536325930, -32.84375000204838813, -5.082755093536325042 ) ) ;
#30417=CARTESIAN_POINT ( 'NONE',  ( 2.977408999572650927, -18.87500000204838457, -7.188101187500000933 ) ) ;
#30430=CARTESIAN_POINT ( 'NONE',  ( -8.000000000000001776, -11.84375000409677270, 3.313708498984758943 ) ) ;
#30438=FILL_AREA_STYLE_COLOUR ( '', #28732 ) ;
#30440=CARTESIAN_POINT ( 'NONE',  ( -9.253817200599833370, 31.29992729916860483, -3.791916801615161869 ) ) ;
#30472=EDGE_LOOP ( 'NONE', ( #41859, #23092 ) ) ;
#30492=CARTESIAN_POINT ( 'NONE',  ( 7.188101187499999156, -25.25000000204839523, 2.977408999572654924 ) ) ;
#30535=CARTESIAN_POINT ( 'NONE',  ( -1.469576158976823947E-15, -16.06250000409677270, 8.000000000000000000 ) ) ;
#30558=CARTESIAN_POINT ( 'NONE',  ( -5.656854249492379694, -28.62500000409677270, -5.656854249492380582 ) ) ;
#30582=CARTESIAN_POINT ( 'NONE',  ( -9.606080321247056020, 15.83563386295778308, 2.802461721337994760 ) ) ;
#30605=DIRECTION ( 'NONE',  ( -0.000000000000000000, -1.000000000000000000, -0.000000000000000000 ) ) ;
#30608=CARTESIAN_POINT ( 'NONE',  ( -3.313708498984798467, -21.21875000409677270, -7.999999999999961808 ) ) ;
#30681=CARTESIAN_POINT ( 'NONE',  ( -9.701712097384769251, 15.75132464342601857, -2.450541714948249794 ) ) ;
#30690=CARTESIAN_POINT ( 'NONE',  ( -3.313708498984760720, -18.03124999999999645, -8.000000000000000000 ) ) ;
#30698=PLANE ( 'NONE',  #2171 ) ;
#30740=CARTESIAN_POINT ( 'NONE',  ( -10.00000000000000000, 15.11603512204006883, 0.3498606326563452606 ) ) ;
#30759=CARTESIAN_POINT ( 'NONE',  ( 1.510421413154031223, 15.23810023151232862, -9.910377230549265448 ) ) ;
#30765=VERTEX_POINT ( 'NONE', #35039 ) ;
#30774=CARTESIAN_POINT ( 'NONE',  ( -4.413588872740236368, -9.563952367645420338, 5.751921314332417268 ) ) ;
#30811=CARTESIAN_POINT ( 'NONE',  ( -7.896254658894418021, 26.21070817245799489, 1.307282859663298158 ) ) ;
#30818=CARTESIAN_POINT ( 'NONE',  ( -3.313708498984765161, -32.46875000000000000, 7.999999999999998224 ) ) ;
#30828=ORIENTED_EDGE ( 'NONE', *, *, #81717, .T. ) ;
#30845=CARTESIAN_POINT ( 'NONE',  ( -7.188101187500002709, -18.31250000204838457, 2.977408999572648707 ) ) ;
#30870=( BOUNDED_CURVE ( )  B_SPLINE_CURVE ( 2, ( #71160, #4310, #69590, #29171, #102481, #13445, #45838, #21072, #95442 ),
 .UNSPECIFIED., .F., .F. ) 
 B_SPLINE_CURVE_WITH_KNOTS ( ( 3, 2, 2, 2, 3 ),
 ( 0.3088235294117646634, 0.3161764705882352255, 0.3235294117647058432, 0.3308823529411764053, 0.3382352941176470229 ),
 .UNSPECIFIED. ) 
 CURVE ( )  GEOMETRIC_REPRESENTATION_ITEM ( )  RATIONAL_B_SPLINE_CURVE ( ( 1.000000000000000666, 0.9238795325112861834, 1.000000000000000000, 0.9238795325112867385, 1.000000000000000000, 0.9238795325112867385, 1.000000000000000000, 0.9238795325112872936, 0.9999999999999994449 ) ) 
 REPRESENTATION_ITEM ( '' )  );
#30895=CARTESIAN_POINT ( 'NONE',  ( 7.188101187500000044, -16.53125000204838813, 0.000000000000000000 ) ) ;
#30904=CARTESIAN_POINT ( 'NONE',  ( 5.082755093536324154, -24.21875000204838813, 5.082755093536326818 ) ) ;
#30918=ORIENTED_EDGE ( 'NONE', *, *, #55419, .F. ) ;
#30948=CARTESIAN_POINT ( 'NONE',  ( 7.188101187500000044, -27.03125000204838813, 0.000000000000000000 ) ) ;
#30962=CARTESIAN_POINT ( 'NONE',  ( -5.082755093536325042, -15.59375000204838635, -5.082755093536325930 ) ) ;
#30971=ORIENTED_EDGE ( 'NONE', *, *, #44988, .T. ) ;
#30972=CARTESIAN_POINT ( 'NONE',  ( 3.313708498984762496, -12.96875000409676915, 7.999999999999998224 ) ) ;
#30983=CARTESIAN_POINT ( 'NONE',  ( 6.123233995736772199E-16, 15.00000000000000000, 9.999999999999998224 ) ) ;
#31016=CARTESIAN_POINT ( 'NONE',  ( -6.928203230275510549, 30.00000000000000000, 4.000000000000000000 ) ) ;
#31038=CARTESIAN_POINT ( 'NONE',  ( -7.188101187500002709, -18.31250000204838457, 2.977408999572648707 ) ) ;
#31103=CARTESIAN_POINT ( 'NONE',  ( 3.313708498984762052, -27.40625000409676915, -8.000000000000000000 ) ) ;
#31116=EDGE_CURVE ( 'NONE', #11237, #7939, #22512, .T. ) ;
#31127=CARTESIAN_POINT ( 'NONE',  ( -9.999999999999998224, 15.23416508905887490, 0.7060372491548249085 ) ) ;
#31152=AXIS2_PLACEMENT_3D ( 'NONE', #88094, #32531, #31473 ) ;
#31178=DIRECTION ( 'NONE',  ( 1.000000000000000000, -0.000000000000000000, -0.000000000000000000 ) ) ;
#31220=EDGE_LOOP ( 'NONE', ( #89963, #55510 ) ) ;
#31226=CARTESIAN_POINT ( 'NONE',  ( -5.656854249492381470, -14.56249999999999289, 5.656854249492379694 ) ) ;
#31231=DIRECTION ( 'NONE',  ( 0.000000000000000000, -0.000000000000000000, 1.000000000000000000 ) ) ;
#31250=CARTESIAN_POINT ( 'NONE',  ( 9.999999999999998224, 15.00000000000000000, -0.7768758660234752478 ) ) ;
#31284=( LENGTH_UNIT ( ) NAMED_UNIT ( * ) SI_UNIT ( .MILLI., .METRE. ) );
#31304=CARTESIAN_POINT ( 'NONE',  ( -2.977408999572650039, -11.56250000204838635, -7.188101187500001821 ) ) ;
#31307=( BOUNDED_CURVE ( )  B_SPLINE_CURVE ( 2, ( #103928, #30608, #39223, #72097, #64035, #26258, #67214, #822, #50993 ),
 .UNSPECIFIED., .F., .F. ) 
 B_SPLINE_CURVE_WITH_KNOTS ( ( 3, 2, 2, 2, 3 ),
 ( 0.4852941176470589313, 0.4926470588235295489, 0.5000000000000001110, 0.5073529411764706731, 0.5147058823529412352 ),
 .UNSPECIFIED. ) 
 CURVE ( )  GEOMETRIC_REPRESENTATION_ITEM ( )  RATIONAL_B_SPLINE_CURVE ( ( 0.9999999999999988898, 0.9238795325112878487, 1.000000000000000000, 0.9238795325112867385, 1.000000000000000000, 0.9238795325112867385, 1.000000000000000000, 0.9238795325112856283, 1.000000000000001110 ) ) 
 REPRESENTATION_ITEM ( '' )  );
#31344=MECHANICAL_DESIGN_GEOMETRIC_PRESENTATION_REPRESENTATION('',(#64047),#100207);
#31352=CARTESIAN_POINT ( 'NONE',  ( -8.000000000000000000, -31.24999999999999645, -9.797174393178825657E-16 ) ) ;
#31355=( GEOMETRIC_REPRESENTATION_CONTEXT ( 3 ) GLOBAL_UNCERTAINTY_ASSIGNED_CONTEXT ( ( #7322 ) ) GLOBAL_UNIT_ASSIGNED_CONTEXT ( ( #97941, #59631, #27830 ) ) REPRESENTATION_CONTEXT ( 'NONE', 'WORKASPACE' ) );
#31376=CARTESIAN_POINT ( 'NONE',  ( -2.977408999572650039, -18.68750000204838102, -7.188101187500001821 ) ) ;
#31426=CARTESIAN_POINT ( 'NONE',  ( 2.977408999572650927, -22.25000000204839523, -7.188101187500000933 ) ) ;
#31436=CARTESIAN_POINT ( 'NONE',  ( -2.977408999572650039, -28.06250000204838813, -7.188101187500001821 ) ) ;
#31473=DIRECTION ( 'NONE',  ( 0.000000000000000000, 0.000000000000000000, 1.000000000000000000 ) ) ;
#31476=CARTESIAN_POINT ( 'NONE',  ( 7.188101187500000044, -22.53125000204838457, 0.000000000000000000 ) ) ;
#31487=EDGE_CURVE ( 'NONE', #28267, #99675, #36577, .T. ) ;
#31490=CARTESIAN_POINT ( 'NONE',  ( 2.977408999572652260, -10.43750000204838457, 7.188101187500000044 ) ) ;
#31500=CARTESIAN_POINT ( 'NONE',  ( 7.999999999999998224, -9.781250004096770923, 3.313708498984766493 ) ) ;
#31504=CARTESIAN_POINT ( 'NONE',  ( -9.999945253488242258, 88.99986313370533253, -0.2662901834230884113 ) ) ;
#31510=CARTESIAN_POINT ( 'NONE',  ( -4.034557488803550918, 15.07443463110242199, 9.151133496028460712 ) ) ;
#31516=EDGE_LOOP ( 'NONE', ( #90305, #65500, #87172, #30828, #5005, #30038, #58149, #18397 ) ) ;
#31536=ADVANCED_FACE ( 'NONE', ( #49951 ), #88633, .F. ) ;
#31557=DIRECTION ( 'NONE',  ( 0.000000000000000000, 0.000000000000000000, -1.000000000000000000 ) ) ;
#31559=CARTESIAN_POINT ( 'NONE',  ( -2.977408999572650039, -17.18750000204838813, -7.188101187500001821 ) ) ;
#31577=PLANE ( 'NONE',  #92145 ) ;
#31613=CARTESIAN_POINT ( 'NONE',  ( -5.082755093536325042, -29.09375000204838813, -5.082755093536325930 ) ) ;
#31619=CARTESIAN_POINT ( 'NONE',  ( -5.656854249492381470, -32.75000000409677625, 5.656854249492379694 ) ) ;
#31624=SURFACE_SIDE_STYLE ('',( #48297 ) ) ;
#31627=CARTESIAN_POINT ( 'NONE',  ( 4.898587196589412829E-16, -10.62499999999999289, -8.000000000000000000 ) ) ;
#31642=CARTESIAN_POINT ( 'NONE',  ( -9.216463528758735535, 15.13241195026071928, 3.884543032213891411 ) ) ;
#31646=PRESENTATION_STYLE_ASSIGNMENT (( #14887 ) ) ;
#31659=CARTESIAN_POINT ( 'NONE',  ( -7.550180524134850302, 33.00559247213185898, 2.651855549982496729 ) ) ;
#31666=CARTESIAN_POINT ( 'NONE',  ( -5.409176543609191867, -29.99999999999998934, 5.306317252530670991 ) ) ;
#31670=EDGE_CURVE ( 'NONE', #699, #79080, #18393, .T. ) ;
#31678=ORIENTED_EDGE ( 'NONE', *, *, #85079, .T. ) ;
#31696=CARTESIAN_POINT ( 'NONE',  ( 0.000000000000000000, 15.00000000000000000, 0.000000000000000000 ) ) ;
#31698=VERTEX_POINT ( 'NONE', #78484 ) ;
#31707=CARTESIAN_POINT ( 'NONE',  ( 7.551437640244098581, 101.9912753747709075, -2.648272645923387625 ) ) ;
#31718=ADVANCED_FACE ( 'NONE', ( #20319 ), #53681, .F. ) ;
#31740=CARTESIAN_POINT ( 'NONE',  ( -8.000000000000000000, -13.24999999999999467, -9.797174393178825657E-16 ) ) ;
#31759=EDGE_CURVE ( 'NONE', #82593, #20391, #99648, .T. ) ;
#31764=CARTESIAN_POINT ( 'NONE',  ( 9.240220675753668900, 15.98931925350938243, -3.827754797006023058 ) ) ;
#31791=VERTEX_POINT ( 'NONE', #95743 ) ;
#31797=CARTESIAN_POINT ( 'NONE',  ( -9.700350089084274430, 15.75268258782372754, -2.455962139888423490 ) ) ;
#31857=EDGE_CURVE ( 'NONE', #13534, #24651, #48362, .T. ) ;
#31864=DIRECTION ( 'NONE',  ( 1.000000000000000000, 0.000000000000000000, 0.000000000000000000 ) ) ;
#31865=CARTESIAN_POINT ( 'NONE',  ( 8.000000000000000000, -31.99999999999999289, 0.000000000000000000 ) ) ;
#31882=CARTESIAN_POINT ( 'NONE',  ( 6.944031699373470090, 105.5346065455613171, 3.972913591453824278 ) ) ;
#31888=CARTESIAN_POINT ( 'NONE',  ( 2.977408999572650927, -15.87500000204838635, -7.188101187500001821 ) ) ;
#31904=FACE_OUTER_BOUND ( 'NONE', #50778, .T. ) ;
#31916=EDGE_CURVE ( 'NONE', #93035, #29729, #37719, .T. ) ;
#31939=CARTESIAN_POINT ( 'NONE',  ( -7.188101187500000044, -12.78125000204838635, -8.802885111219163269E-16 ) ) ;
#31947=CARTESIAN_POINT ( 'NONE',  ( 4.401442555609581635E-16, -29.65625000204838813, -7.188101187500000044 ) ) ;
#31950=CARTESIAN_POINT ( 'NONE',  ( -1.320432766682874540E-15, -28.90625000204838813, 7.188101187500000044 ) ) ;
#31952=CARTESIAN_POINT ( 'NONE',  ( -7.721181058141405096, -30.00000000000004263, -2.093648267354947912 ) ) ;
#31991=CARTESIAN_POINT ( 'NONE',  ( 9.333892298909262308, 28.21724268374966016, -3.590295303293458584 ) ) ;
#31992=CARTESIAN_POINT ( 'NONE',  ( -2.977408999572650039, -25.06250000204838457, -7.188101187500001821 ) ) ;
#32006=CARTESIAN_POINT ( 'NONE',  ( 5.082755093536325930, -15.96875000204838635, -5.082755093536325042 ) ) ;
#32007=CARTESIAN_POINT ( 'NONE',  ( 7.550180524134847637, 26.99440752786814102, 2.651855549982494953 ) ) ;
#32015=CARTESIAN_POINT ( 'NONE',  ( -8.000000000000001776, -19.15624999999999289, 3.313708498984759387 ) ) ;
#32018=CARTESIAN_POINT ( 'NONE',  ( 5.656854249492378806, -9.875000004096769146, 5.656854249492381470 ) ) ;
#32022=CARTESIAN_POINT ( 'NONE',  ( -9.918579450955563814, 88.79303912968688905, 1.297207292923873156 ) ) ;
#32036=CARTESIAN_POINT ( 'NONE',  ( 4.898587196589412829E-16, -9.312500004096769146, -8.000000000000000000 ) ) ;
#32054=ORIENTED_EDGE ( 'NONE', *, *, #84657, .F. ) ;
#32072=CARTESIAN_POINT ( 'NONE',  ( -10.00000000000000355, 15.00000000000000000, -10.00000000000000000 ) ) ;
#32079=CARTESIAN_POINT ( 'NONE',  ( -7.188101187500002709, -21.31250000204838813, 2.977408999572648707 ) ) ;
#32082=CARTESIAN_POINT ( 'NONE',  ( 9.537909130738274399, 82.35385169036607067, -3.010726932293856795 ) ) ;
#32142=CARTESIAN_POINT ( 'NONE',  ( -8.000000000000000000, -31.53125000409677270, -3.313708498984762496 ) ) ;
#32146=CARTESIAN_POINT ( 'NONE',  ( 9.699189539447125696, 33.17692228246711039, -2.444343703917216448 ) ) ;
#32157=CARTESIAN_POINT ( 'NONE',  ( 8.000000000000000000, -15.68750000409677092, 0.000000000000000000 ) ) ;
#32185=CARTESIAN_POINT ( 'NONE',  ( -7.093569395281086543, -30.00000000000000355, 3.069303058423363151 ) ) ;
#32220=DIRECTION ( 'NONE',  ( 0.000000000000000000, 0.000000000000000000, 1.000000000000000000 ) ) ;
#32233=CARTESIAN_POINT ( 'NONE',  ( 7.896571385775231100, 101.2100200065424787, 1.305932416347435732 ) ) ;
#32243=CARTESIAN_POINT ( 'NONE',  ( 9.537927238823508347, 107.6462685711817926, -3.010735687602429600 ) ) ;
#32259=VERTEX_POINT ( 'NONE', #31952 ) ;
#32266=CARTESIAN_POINT ( 'NONE',  ( -1.469576158976823947E-15, -17.37499999999999289, 8.000000000000000000 ) ) ;
#32271=CARTESIAN_POINT ( 'NONE',  ( -7.934203308536663890, 101.1329965998220217, 1.057099537198549655 ) ) ;
#32276=ORIENTED_EDGE ( 'NONE', *, *, #48991, .T. ) ;
#32313=ORIENTED_EDGE ( 'NONE', *, *, #88401, .T. ) ;
#32317=CARTESIAN_POINT ( 'NONE',  ( -3.979266480701241449, -30.00000000000000000, -6.940132439339151027 ) ) ;
#32331=VERTEX_POINT ( 'NONE', #27609 ) ;
#32339=CARTESIAN_POINT ( 'NONE',  ( -10.00000000000000000, 15.00000000000000000, -2.701558353794502931 ) ) ;
#32341=CARTESIAN_POINT ( 'NONE',  ( -7.188101187500000044, -30.40625000204838813, -8.802885111219163269E-16 ) ) ;
#32401=CARTESIAN_POINT ( 'NONE',  ( 4.898587196589412829E-16, -33.12499999999999289, -8.000000000000000000 ) ) ;
#32423=CARTESIAN_POINT ( 'NONE',  ( 6.928203230275509661, 105.0000000000000000, 4.000000000000001776 ) ) ;
#32428=CARTESIAN_POINT ( 'NONE',  ( -7.188101187500001821, -11.00000000204838635, -2.977408999572651371 ) ) ;
#32461=ORIENTED_EDGE ( 'NONE', *, *, #66784, .F. ) ;
#32480=CARTESIAN_POINT ( 'NONE',  ( -5.082755093536326818, -11.09375000204838457, 5.082755093536325042 ) ) ;
#32491=CARTESIAN_POINT ( 'NONE',  ( -5.082755093536325042, -27.96875000204838457, -5.082755093536325930 ) ) ;
#32531=DIRECTION ( 'NONE',  ( -0.000000000000000000, 1.000000000000000000, -0.000000000000000000 ) ) ;
#32533=CARTESIAN_POINT ( 'NONE',  ( -2.977408999572650039, -26.56250000204838457, -7.188101187500001821 ) ) ;
#32542=CARTESIAN_POINT ( 'NONE',  ( 9.165151389911683211, 85.26295510916339992, 3.999999999999999112 ) ) ;
#32546=CARTESIAN_POINT ( 'NONE',  ( 7.188101187499999156, -13.25000000204838280, 2.977408999572654924 ) ) ;
#32547=CARTESIAN_POINT ( 'NONE',  ( 7.343637806710344940, 27.55636878099382869, 3.177475076494675310 ) ) ;
#32559=CARTESIAN_POINT ( 'NONE',  ( -7.188101187500002709, -28.81250000204838457, 2.977408999572648707 ) ) ;
#32619=FACE_OUTER_BOUND ( 'NONE', #92007, .T. ) ;
#32620=CARTESIAN_POINT ( 'NONE',  ( 7.188101187500001821, -17.56250000204838457, -2.977408999572650483 ) ) ;
#32622=CARTESIAN_POINT ( 'NONE',  ( 9.165151389911679658, 85.00000000000000000, 4.000000000000000000 ) ) ;
#32686=CARTESIAN_POINT ( 'NONE',  ( 7.999999999999998224, -23.28125000409677270, 3.313708498984766493 ) ) ;
#32694=CARTESIAN_POINT ( 'NONE',  ( -0.7408669144225156211, 15.11700796859873108, -9.999999999997889688 ) ) ;
#32723=CARTESIAN_POINT ( 'NONE',  ( -7.934914944860276265, 33.86845647200111387, -1.051261972695689106 ) ) ;
#32734=CARTESIAN_POINT ( 'NONE',  ( -3.323053273850956835, -29.99999999999999289, 6.657831141027028110 ) ) ;
#32768=EDGE_LOOP ( 'NONE', ( #101724, #49105, #13200, #93683 ) ) ;
#32786=CARTESIAN_POINT ( 'NONE',  ( 10.00004721872059754, 109.0001180468114939, -0.2617599822266517551 ) ) ;
#32787=VECTOR ( 'NONE', #6603, 1000.000000000000000 ) ;
#32811=ORIENTED_EDGE ( 'NONE', *, *, #82955, .F. ) ;
#32834=AXIS2_PLACEMENT_3D ( 'NONE', #65531, #98418, #57413 ) ;
#32835=ORIENTED_EDGE ( 'NONE', *, *, #71127, .T. ) ;
#32838=CARTESIAN_POINT ( 'NONE',  ( -7.896254658894416245, 81.21070817245799844, 1.307282859663297714 ) ) ;
#32871=CARTESIAN_POINT ( 'NONE',  ( -2.977408999572650039, -32.18750000204838813, -7.188101187500001821 ) ) ;
#32890=CARTESIAN_POINT ( 'NONE',  ( 0.000000000000000000, -30.00000000000000000, 8.000000000000000000 ) ) ;
#32912=CARTESIAN_POINT ( 'NONE',  ( -1.469576158976823947E-15, -20.56250000409676915, 8.000000000000000000 ) ) ;
#32931=CARTESIAN_POINT ( 'NONE',  ( 5.656854249492378806, -29.18749999999999645, 5.656854249492381470 ) ) ;
#32957=CARTESIAN_POINT ( 'NONE',  ( -2.977408999572650039, -14.18750000204838280, -7.188101187500001821 ) ) ;
#33013=CARTESIAN_POINT ( 'NONE',  ( -1.320432766682874540E-15, -10.90625000204838457, 7.188101187500000044 ) ) ;
#33017=CARTESIAN_POINT ( 'NONE',  ( 6.560701988338252910, -30.00000000000000000, 2.946301444182167106 ) ) ;
#33022=CARTESIAN_POINT ( 'NONE',  ( 7.188101187500001821, -22.43750000204838813, -2.977408999572650483 ) ) ;
#33029=CARTESIAN_POINT ( 'NONE',  ( 4.898587196589412829E-16, -22.62499999999999289, -8.000000000000000000 ) ) ;
#33063=CARTESIAN_POINT ( 'NONE',  ( -1.320432766682874540E-15, -25.90625000204838813, 7.188101187500000044 ) ) ;
#33069=DIRECTION ( 'NONE',  ( 1.000000000000000000, -0.000000000000000000, -0.000000000000000000 ) ) ;
#33073=CARTESIAN_POINT ( 'NONE',  ( 9.918325909156569864, 88.79235231707430387, 1.298699613733149683 ) ) ;
#33079=CARTESIAN_POINT ( 'NONE',  ( -5.082755093536325042, -11.09375000204838457, -5.082755093536325930 ) ) ;
#33091=CARTESIAN_POINT ( 'NONE',  ( 5.082755093536325930, -32.46875000204838813, -5.082755093536325042 ) ) ;
#33097=CARTESIAN_POINT ( 'NONE',  ( -9.842473135306409660, 33.58931817113587925, 1.785129593756275224 ) ) ;
#33146=CARTESIAN_POINT ( 'NONE',  ( 4.401442555609581635E-16, -20.28125000204838813, -7.188101187500000044 ) ) ;
#33149=CARTESIAN_POINT ( 'NONE',  ( 9.843039827103241990, 81.40916497491664927, -1.781495459429541572 ) ) ;
#33208=CARTESIAN_POINT ( 'NONE',  ( -5.656854249492381470, -26.75000000409677625, 5.656854249492379694 ) ) ;
#33214=COLOUR_RGB ( '', 0.66274510, 0.83137255, 0.94901961) ;
#33215=CARTESIAN_POINT ( 'NONE',  ( -1.619566622897594232, -29.99999999999998579, -7.705259353042192672 ) ) ;
#33219=COLOUR_RGB ( '', 0.72549020, 0.75294118, 0.79215686) ;
#33220=CARTESIAN_POINT ( 'NONE',  ( 0.000000000000000000, 16.00000000000000000, 0.000000000000000000 ) ) ;
#33243=ADVANCED_FACE ( 'NONE', ( #74525, #602 ), #48120, .T. ) ;
#33248=CARTESIAN_POINT ( 'NONE',  ( -7.151217271224854954, 31.78749400445714812, -3.587901469523285591 ) ) ;
#33267=FILL_AREA_STYLE_COLOUR ( '', #98028 ) ;
#33292=ORIENTED_EDGE ( 'NONE', *, *, #84657, .T. ) ;
#33303=ORIENTED_EDGE ( 'NONE', *, *, #62580, .F. ) ;
#33314=CARTESIAN_POINT ( 'NONE',  ( 9.334514330295428763, 106.7862273768178625, -3.588704711590612106 ) ) ;
#33336=CARTESIAN_POINT ( 'NONE',  ( 5.656854249492378806, -11.18749999999999289, 5.656854249492381470 ) ) ;
#33340=CARTESIAN_POINT ( 'NONE',  ( -6.928203230275508773, 105.0000000000000000, 4.000000000000001776 ) ) ;
#33400=CARTESIAN_POINT ( 'NONE',  ( 2.977408999572651815, -32.93750000204839523, 7.188101187500000933 ) ) ;
#33457=CARTESIAN_POINT ( 'NONE',  ( -5.656854249492379694, -28.43749999999999289, -5.656854249492380582 ) ) ;
#33479=CARTESIAN_POINT ( 'NONE',  ( -7.188101187500002709, -13.81250000204838280, 2.977408999572648707 ) ) ;
#33480=DIRECTION ( 'NONE',  ( 0.000000000000000000, 0.000000000000000000, 1.000000000000000000 ) ) ;
#33504=DIRECTION ( 'NONE',  ( 0.000000000000000000, 0.000000000000000000, 1.000000000000000000 ) ) ;
#33535=CARTESIAN_POINT ( 'NONE',  ( -5.082755093536326818, -15.59375000204838635, 5.082755093536325042 ) ) ;
#33536=CARTESIAN_POINT ( 'NONE',  ( 4.587132918264077652, -29.99999999999999289, 5.539110995917003066 ) ) ;
#33541=CARTESIAN_POINT ( 'NONE',  ( 5.082755093536325930, -17.84375000204838457, -5.082755093536325042 ) ) ;
#33569=CARTESIAN_POINT ( 'NONE',  ( -3.313708498984741180, -25.71875000409677625, -8.000000000000019540 ) ) ;
#33574=EDGE_CURVE ( 'NONE', #35576, #90586, #105935, .T. ) ;
#33582=CARTESIAN_POINT ( 'NONE',  ( -7.188101187500000044, -21.78125000204838457, -8.802885111219163269E-16 ) ) ;
#33604=VERTEX_POINT ( 'NONE', #32912 ) ;
#33611=CARTESIAN_POINT ( 'NONE',  ( -3.999980918664427065, -8.688225714286829771, 6.928214246854706992 ) ) ;
#33667=CARTESIAN_POINT ( 'NONE',  ( -10.00000000000000178, 16.00000000000000000, 4.582575694955834500 ) ) ;
#33674=CARTESIAN_POINT ( 'NONE',  ( 7.188101187500000044, -11.65625000204838635, 0.000000000000000000 ) ) ;
#33708=CARTESIAN_POINT ( 'NONE',  ( 6.928203230275510549, 85.00000000000000000, -4.000000000000000000 ) ) ;
#33727=CARTESIAN_POINT ( 'NONE',  ( 7.188101187500000044, -25.15625000204838813, 0.000000000000000000 ) ) ;
#33731=( NAMED_UNIT ( * ) PLANE_ANGLE_UNIT ( ) SI_UNIT ( $, .RADIAN. ) );
#33737=DIRECTION ( 'NONE',  ( 1.734723475976807094E-16, 0.000000000000000000, 1.000000000000000000 ) ) ;
#33739=CARTESIAN_POINT ( 'NONE',  ( -5.656854249492379694, -22.62500000409676915, -5.656854249492380582 ) ) ;
#33778=ORIENTED_EDGE ( 'NONE', *, *, #93960, .T. ) ;
#33780=CARTESIAN_POINT ( 'NONE',  ( -3.594029361870008099, -9.531975552773349847, 6.225090491531444670 ) ) ;
#33782=CARTESIAN_POINT ( 'NONE',  ( -7.618844049274130725, 33.17235898929458671, 2.450177051822846064 ) ) ;
#33789=VERTEX_POINT ( 'NONE', #26640 ) ;
#33814=PRODUCT_DEFINITION_CONTEXT ( 'detailed design', #58288, 'design' ) ;
#33827=FILL_AREA_STYLE ('',( #19792 ) ) ;
#33842=CARTESIAN_POINT ( 'NONE',  ( 7.986452802927059835, 101.0269024230811539, 0.5332468218996369025 ) ) ;
#33856=CARTESIAN_POINT ( 'NONE',  ( 0.000000000000000000, 15.00000000000000000, 0.000000000000000000 ) ) ;
#33885=CARTESIAN_POINT ( 'NONE',  ( 5.656854249492378806, -18.68749999999999289, 5.656854249492381470 ) ) ;
#33912=CARTESIAN_POINT ( 'NONE',  ( -7.413471587080149305, 82.35647840831674671, -3.013058070223552765 ) ) ;
#33930=EDGE_LOOP ( 'NONE', ( #12923, #102757, #99006, #1506 ) ) ;
#33943=CARTESIAN_POINT ( 'NONE',  ( -7.188101187500000044, -31.90625000204838813, -8.802885111219163269E-16 ) ) ;
#34004=CARTESIAN_POINT ( 'NONE',  ( 4.898587196589412829E-16, -25.62499999999999645, -8.000000000000000000 ) ) ;
#34013=CARTESIAN_POINT ( 'NONE',  ( -3.313708498984760720, -33.21875000409677625, -8.000000000000000000 ) ) ;
#34028=CARTESIAN_POINT ( 'NONE',  ( -9.253583916535172094, 86.29803908005033009, 3.792462592445556169 ) ) ;
#34029=CARTESIAN_POINT ( 'NONE',  ( -7.188101187500001821, -12.50000000204838990, -2.977408999572651371 ) ) ;
#34065=LINE ( 'NONE', #83106, #30193 ) ;
#34086=CARTESIAN_POINT ( 'NONE',  ( -5.082755093536325042, -12.96875000204838280, -5.082755093536325930 ) ) ;
#34094=CARTESIAN_POINT ( 'NONE',  ( -7.188101187500001821, -18.87500000204838457, -2.977408999572651371 ) ) ;
#34134=CARTESIAN_POINT ( 'NONE',  ( 7.188101187499999156, -21.12500000204838813, 2.977408999572654924 ) ) ;
#34144=CARTESIAN_POINT ( 'NONE',  ( 6.928203230275509661, 30.00000000000000000, 4.000000000000000000 ) ) ;
#34156=CARTESIAN_POINT ( 'NONE',  ( 5.082755093536325930, -33.96875000204838813, -5.082755093536325042 ) ) ;
#34207=CARTESIAN_POINT ( 'NONE',  ( 7.744168461338432508, 88.46254061715157491, 2.019395720771550273 ) ) ;
#34217=CARTESIAN_POINT ( 'NONE',  ( -5.082755093536326818, -13.71875000204838457, 5.082755093536325042 ) ) ;
#34252=CARTESIAN_POINT ( 'NONE',  ( 7.934914944860278041, 81.13154352799891456, -1.051261972695689551 ) ) ;
#34269=CARTESIAN_POINT ( 'NONE',  ( -2.977408999572650039, -23.18750000204838813, -7.188101187500000933 ) ) ;
#34277=EDGE_CURVE ( 'NONE', #44667, #62970, #69438, .T. ) ;
#34282=CARTESIAN_POINT ( 'NONE',  ( -1.469576158976823947E-15, -22.06250000409676915, 8.000000000000000000 ) ) ;
#34337=CARTESIAN_POINT ( 'NONE',  ( 0.000000000000000000, -30.00000000000000000, 0.000000000000000000 ) ) ;
#34341=( BOUNDED_CURVE ( )  B_SPLINE_CURVE ( 2, ( #51000, #297, #25737, #57495, #81765, #17607, #8429, #42935, #41328 ),
 .UNSPECIFIED., .F., .F. ) 
 B_SPLINE_CURVE_WITH_KNOTS ( ( 3, 2, 2, 2, 3 ),
 ( 0.4852941176470589868, 0.4926470588235296044, 0.5000000000000002220, 0.5073529411764707842, 0.5147058823529413463 ),
 .UNSPECIFIED. ) 
 CURVE ( )  GEOMETRIC_REPRESENTATION_ITEM ( )  RATIONAL_B_SPLINE_CURVE ( ( 0.9999999999999982236, 0.9238795325112885148, 1.000000000000000000, 0.9238795325112867385, 1.000000000000000000, 0.9238795325112867385, 1.000000000000000000, 0.9238795325112844070, 1.000000000000002220 ) ) 
 REPRESENTATION_ITEM ( '' )  );
#34350=CARTESIAN_POINT ( 'NONE',  ( -1.400881274228119588, 15.45483377860037955, 9.907626560209529032 ) ) ;
#34367=FACE_BOUND ( 'NONE', #68351, .T. ) ;
#34370=( NAMED_UNIT ( * ) SI_UNIT ( $, .STERADIAN. ) SOLID_ANGLE_UNIT ( ) );
#34446=VECTOR ( 'NONE', #94336, 1000.000000000000000 ) ;
#34452=CARTESIAN_POINT ( 'NONE',  ( -7.213352437320216914, 82.98163526992318850, -3.463014597543480733 ) ) ;
#34472=ORIENTED_EDGE ( 'NONE', *, *, #2146, .F. ) ;
#34537=LINE ( 'NONE', #17269, #5956 ) ;
#34538=CARTESIAN_POINT ( 'NONE',  ( 3.313708498984762052, -25.71874999999999645, -8.000000000000000000 ) ) ;
#34546=DIRECTION ( 'NONE',  ( -0.000000000000000000, 1.000000000000000000, -0.000000000000000000 ) ) ;
#34554=VECTOR ( 'NONE', #21250, 1000.000000000000000 ) ;
#34558=CARTESIAN_POINT ( 'NONE',  ( 7.413471587080148417, 107.6435215916832675, -3.013058070223554985 ) ) ;
#34565=DIRECTION ( 'NONE',  ( -0.000000000000000000, 1.000000000000000000, -0.000000000000000000 ) ) ;
#34596=ORIENTED_EDGE ( 'NONE', *, *, #72874, .T. ) ;
#34626=CARTESIAN_POINT ( 'NONE',  ( -7.188101187500000044, -18.78125000204838457, -8.802885111219163269E-16 ) ) ;
#34644=CARTESIAN_POINT ( 'NONE',  ( -6.943926999490791729, 85.53300992626147092, -3.973092371898545139 ) ) ;
#34652=CARTESIAN_POINT ( 'NONE',  ( 9.701736001019304112, 15.75130202679986624, -2.450449656239129137 ) ) ;
#34665=CARTESIAN_POINT ( 'NONE',  ( 9.176645556628253431, 29.47260967593268788, 3.973966573947708802 ) ) ;
#34666=CARTESIAN_POINT ( 'NONE',  ( -7.188101187500000044, -18.78125000204838457, -8.802885111219163269E-16 ) ) ;
#34669=AXIS2_PLACEMENT_3D ( 'NONE', #33856, #65663, #99612 ) ;
#34680=CARTESIAN_POINT ( 'NONE',  ( 5.082755093536325930, -9.968750002048384573, -5.082755093536325042 ) ) ;
#34692=FACE_OUTER_BOUND ( 'NONE', #76602, .T. ) ;
#34693=CARTESIAN_POINT ( 'NONE',  ( 5.082755093536324154, -26.84375000204838813, 5.082755093536326818 ) ) ;
#34704=ORIENTED_EDGE ( 'NONE', *, *, #11734, .T. ) ;
#34745=CARTESIAN_POINT ( 'NONE',  ( 5.082755093536324154, -25.71875000204838813, 5.082755093536326818 ) ) ;
#34752=CARTESIAN_POINT ( 'NONE',  ( -2.977408999572650039, -15.68750000204838457, -7.188101187500001821 ) ) ;
#34758=CARTESIAN_POINT ( 'NONE',  ( -8.000000000000000000, -14.84374999999999289, -3.313708498984762496 ) ) ;
#34788=CARTESIAN_POINT ( 'NONE',  ( 7.412906595240167817, 82.35811727147745387, 3.014362223629231341 ) ) ;
#34809=CARTESIAN_POINT ( 'NONE',  ( 5.082755093536325930, -27.96875000204838457, -5.082755093536325042 ) ) ;
#34821=CARTESIAN_POINT ( 'NONE',  ( 3.313708498984762496, -21.96875000409677270, 7.999999999999998224 ) ) ;
#34963=( BOUNDED_CURVE ( )  B_SPLINE_CURVE ( 1, ( #81071, #1053 ),
 .UNSPECIFIED., .F., .F. ) 
 B_SPLINE_CURVE_WITH_KNOTS ( ( 2, 2 ),
 ( 0.000000000000000000, 1.000000000000000000 ),
 .UNSPECIFIED. ) 
 CURVE ( )  GEOMETRIC_REPRESENTATION_ITEM ( )  RATIONAL_B_SPLINE_CURVE ( ( 0.9660720326926630630, 0.9660720326926630630 ) ) 
 REPRESENTATION_ITEM ( '' )  );
#34966=DIRECTION ( 'NONE',  ( -1.000000000000000000, 0.000000000000000000, -0.000000000000000000 ) ) ;
#34975=CARTESIAN_POINT ( 'NONE',  ( -9.333079356992097786, 106.7783308007486909, 3.592383266237785922 ) ) ;
#35039=CARTESIAN_POINT ( 'NONE',  ( -1.469576158976823947E-15, -15.87499999999999289, 8.000000000000000000 ) ) ;
#35043=CARTESIAN_POINT ( 'NONE',  ( 4.898587196589412829E-16, -28.81250000409677270, -8.000000000000000000 ) ) ;
#35060=CARTESIAN_POINT ( 'NONE',  ( 3.313708498984800688, -23.28125000000000000, 7.999999999999960032 ) ) ;
#35061=CARTESIAN_POINT ( 'NONE',  ( 8.000000000000000000, -24.49999999999999289, 0.000000000000000000 ) ) ;
#35074=PLANE ( 'NONE',  #42068 ) ;
#35141=CARTESIAN_POINT ( 'NONE',  ( 8.000000000000000000, -18.59375000409676915, -3.313708498984761164 ) ) ;
#35146=CARTESIAN_POINT ( 'NONE',  ( 4.401442555609581635E-16, -23.65625000204838457, -7.188101187500000044 ) ) ;
#35189=CARTESIAN_POINT ( 'NONE',  ( 4.401442555609581635E-16, -17.65625000204838813, -7.188101187500000044 ) ) ;
#35197=CARTESIAN_POINT ( 'NONE',  ( 9.253800200985686786, 86.30010331088172393, -3.791983798715484522 ) ) ;
#35202=CARTESIAN_POINT ( 'NONE',  ( 0.000000000000000000, 115.0000000000000000, -8.000000000000000000 ) ) ;
#35214=CARTESIAN_POINT ( 'NONE',  ( 4.401442555609581635E-16, -27.78125000204838457, -7.188101187500000044 ) ) ;
#35266=CARTESIAN_POINT ( 'NONE',  ( -1.320432766682874540E-15, -22.90625000204838457, 7.188101187500000044 ) ) ;
#35274=CARTESIAN_POINT ( 'NONE',  ( 2.977408999572651815, -11.93750000204838457, 7.188101187500000933 ) ) ;
#35316=CARTESIAN_POINT ( 'NONE',  ( 7.151217271224856731, 83.21250599554284122, -3.587901469523282927 ) ) ;
#35325=ORIENTED_EDGE ( 'NONE', *, *, #16783, .T. ) ;
#35339=CARTESIAN_POINT ( 'NONE',  ( 4.401442555609581635E-16, -26.28125000204838813, -7.188101187500000044 ) ) ;
#35347=CARTESIAN_POINT ( 'NONE',  ( -9.165151389911684987, 84.73704489083661429, 4.000000000000000000 ) ) ;
#35349=CARTESIAN_POINT ( 'NONE',  ( 5.656854249492378806, -18.87500000409677270, 5.656854249492381470 ) ) ;
#35353=CARTESIAN_POINT ( 'NONE',  ( 9.253800200985683233, 31.30010331088172748, -3.791983798715485410 ) ) ;
#35411=CARTESIAN_POINT ( 'NONE',  ( 0.7768758660235928204, 15.00000000000000000, 9.999999999999998224 ) ) ;
#35430=SURFACE_SIDE_STYLE ('',( #50493 ) ) ;
#35448=CARTESIAN_POINT ( 'NONE',  ( 3.313708498984800688, -15.78124999999999289, 7.999999999999960032 ) ) ;
#35449=STYLED_ITEM ( 'NONE', ( #85559 ), #11818 ) ;
#35455=CARTESIAN_POINT ( 'NONE',  ( -3.484756791224363770, 15.95824666716552365, -9.380169522195147991 ) ) ;
#35457=CARTESIAN_POINT ( 'NONE',  ( 7.999999999999998224, -11.28125000409677092, 3.313708498984766049 ) ) ;
#35479=CARTESIAN_POINT ( 'NONE',  ( -7.801777176595946273, 101.4117201418736727, -1.786991866639925597 ) ) ;
#35494=EDGE_CURVE ( 'NONE', #66787, #72025, #98356, .T. ) ;
#35496=FACE_OUTER_BOUND ( 'NONE', #16604, .T. ) ;
#35506=CARTESIAN_POINT ( 'NONE',  ( -9.176645556628256983, 105.5273903240672837, 3.973966573947711023 ) ) ;
#35530=ORIENTED_EDGE ( 'NONE', *, *, #75629, .T. ) ;
#35535=LINE ( 'NONE', #68410, #27879 ) ;
#35540=CARTESIAN_POINT ( 'NONE',  ( 9.797174393178825657E-16, -30.00000000000000000, -8.000000000000000000 ) ) ;
#35561=CARTESIAN_POINT ( 'NONE',  ( 9.999999999999994671, 16.00000000000000000, 4.582575694955847823 ) ) ;
#35576=VERTEX_POINT ( 'NONE', #69719 ) ;
#35597=CARTESIAN_POINT ( 'NONE',  ( 8.000000000000000000, -18.40624999999998934, -3.313708498984761608 ) ) ;
#35616=EDGE_CURVE ( 'NONE', #70143, #53794, #57095, .T. ) ;
#35620=CARTESIAN_POINT ( 'NONE',  ( 7.934996450857311423, 108.8686245647253088, -1.050865690281775677 ) ) ;
#35644=DIRECTION ( 'NONE',  ( 0.000000000000000000, 0.000000000000000000, 1.000000000000000000 ) ) ;
#35688=CARTESIAN_POINT ( 'NONE',  ( 0.9654893961777153422, -30.00000000000000355, 7.122964895856731538 ) ) ;
#35693=CARTESIAN_POINT ( 'NONE',  ( 7.188101187499999156, -12.12500000204838990, 2.977408999572654924 ) ) ;
#35725=ORIENTED_EDGE ( 'NONE', *, *, #33574, .T. ) ;
#35728=CARTESIAN_POINT ( 'NONE',  ( -1.469576158976823947E-15, -21.87499999999999289, 8.000000000000000000 ) ) ;
#35731=CARTESIAN_POINT ( 'NONE',  ( -5.082755093536326818, -17.09375000204838813, 5.082755093536325042 ) ) ;
#35761=CARTESIAN_POINT ( 'NONE',  ( 7.188101187499999156, -23.75000000204839168, 2.977408999572654924 ) ) ;
#35781=CARTESIAN_POINT ( 'NONE',  ( 9.482856158761270748, 102.5569288414527875, 3.177891129109652546 ) ) ;
#35810=CARTESIAN_POINT ( 'NONE',  ( 7.188101187499999156, -25.62500000204838813, 2.977408999572654924 ) ) ;
#35819=CARTESIAN_POINT ( 'NONE',  ( -7.188101187500001821, -11.00000000204838635, -2.977408999572651371 ) ) ;
#35838=CARTESIAN_POINT ( 'NONE',  ( 0.000000000000000000, -30.00000000000000000, 0.000000000000000000 ) ) ;
#35857=CARTESIAN_POINT ( 'NONE',  ( 0.000000000000000000, -30.00000000000000000, 0.000000000000000000 ) ) ;
#35878=CARTESIAN_POINT ( 'NONE',  ( 5.082755093536324154, -25.34375000204838813, 5.082755093536326818 ) ) ;
#35881=( LENGTH_UNIT ( ) NAMED_UNIT ( * ) SI_UNIT ( .MILLI., .METRE. ) );
#35889=CARTESIAN_POINT ( 'NONE',  ( -1.469576158976823947E-15, -16.06250000409677270, 8.000000000000000000 ) ) ;
#35897=CARTESIAN_POINT ( 'NONE',  ( 5.936373709703198998, -30.00000000000001066, -4.453514806643029011 ) ) ;
#35918=DIRECTION ( 'NONE',  ( 0.000000000000000000, 0.000000000000000000, 1.000000000000000000 ) ) ;
#35943=DIRECTION ( 'NONE',  ( -0.000000000000000000, 1.000000000000000000, -0.000000000000000000 ) ) ;
#35952=CARTESIAN_POINT ( 'NONE',  ( 5.082755093536324154, -32.84375000204838813, 5.082755093536326818 ) ) ;
#35971=FACE_BOUND ( 'NONE', #20733, .T. ) ;
#36001=ORIENTED_EDGE ( 'NONE', *, *, #71127, .F. ) ;
#36051=CARTESIAN_POINT ( 'NONE',  ( -9.165151389911679658, 104.9999999999999858, -4.000000000000001776 ) ) ;
#36107=CARTESIAN_POINT ( 'NONE',  ( 9.999999999999996447, 15.00000000000000000, -10.00000000000000000 ) ) ;
#36140=CARTESIAN_POINT ( 'NONE',  ( 0.000000000000000000, 0.000000000000000000, 0.000000000000000000 ) ) ;
#36142=CARTESIAN_POINT ( 'NONE',  ( -3.313708498984765161, -21.96875000000000000, 7.999999999999998224 ) ) ;
#36150=EDGE_LOOP ( 'NONE', ( #7936, #22465, #103684, #51643 ) ) ;
#36185=ORIENTED_EDGE ( 'NONE', *, *, #22223, .F. ) ;
#36190=LINE ( 'NONE', #43698, #70383 ) ;
#36227=CARTESIAN_POINT ( 'NONE',  ( -7.188101187500000044, -12.78125000204838635, -8.802885111219163269E-16 ) ) ;
#36243=CARTESIAN_POINT ( 'NONE',  ( -7.412906595240169594, 87.64188272852254613, 3.014362223629231785 ) ) ;
#36272=CARTESIAN_POINT ( 'NONE',  ( 5.082755093536324154, -10.71875000204838457, 5.082755093536326818 ) ) ;
#36283=CARTESIAN_POINT ( 'NONE',  ( 0.000000000000000000, -30.00000000000000000, 0.000000000000000000 ) ) ;
#36302=CARTESIAN_POINT ( 'NONE',  ( 7.188101187500001821, -25.06250000204838457, -2.977408999572650483 ) ) ;
#36315=CARTESIAN_POINT ( 'NONE',  ( -1.469576158976823947E-15, -22.06250000409676915, 8.000000000000000000 ) ) ;
#36318=CARTESIAN_POINT ( 'NONE',  ( 9.798380800342661345, 101.5319934568449725, -2.010350564680324137 ) ) ;
#36324=CARTESIAN_POINT ( 'NONE',  ( -10.00000000000000355, 0.000000000000000000, -10.00000000000000000 ) ) ;
#36350=CARTESIAN_POINT ( 'NONE',  ( 5.082755093536325930, -25.34375000204838813, -5.082755093536325042 ) ) ;
#36360=CARTESIAN_POINT ( 'NONE',  ( 5.082755093536325930, -29.84375000204838813, -5.082755093536325042 ) ) ;
#36391=( BOUNDED_CURVE ( )  B_SPLINE_CURVE ( 2, ( #1800, #59545, #27744, #34758, #68704, #101585, #60615, #2338, #50884 ),
 .UNSPECIFIED., .F., .F. ) 
 B_SPLINE_CURVE_WITH_KNOTS ( ( 3, 2, 2, 2, 3 ),
 ( 0.7794117647058824705, 0.7867647058823530326, 0.7941176470588235947, 0.8014705882352942679, 0.8088235294117648300 ),
 .UNSPECIFIED. ) 
 CURVE ( )  GEOMETRIC_REPRESENTATION_ITEM ( )  RATIONAL_B_SPLINE_CURVE ( ( 0.9999999999999988898, 0.9238795325112878487, 1.000000000000000000, 0.9238795325112867385, 1.000000000000000000, 0.9238795325112867385, 1.000000000000000000, 0.9238795325112856283, 1.000000000000001110 ) ) 
 REPRESENTATION_ITEM ( '' )  );
#36402=CARTESIAN_POINT ( 'NONE',  ( -2.977408999572650039, -32.56250000204838813, -7.188101187500001821 ) ) ;
#36414=CARTESIAN_POINT ( 'NONE',  ( 2.977408999572650927, -20.37500000204838813, -7.188101187500000933 ) ) ;
#36425=CARTESIAN_POINT ( 'NONE',  ( -3.313708498984765161, -17.65625000409677270, 7.999999999999998224 ) ) ;
#36435=SURFACE_STYLE_FILL_AREA ( #93029 ) ;
#36459=DIRECTION ( 'NONE',  ( 0.000000000000000000, 0.000000000000000000, 1.000000000000000000 ) ) ;
#36485=CARTESIAN_POINT ( 'NONE',  ( 7.188101187499999156, -26.75000000204838457, 2.977408999572654924 ) ) ;
#36488=CARTESIAN_POINT ( 'NONE',  ( -4.165977904505308693, 16.00000000000000000, 9.090909090909091717 ) ) ;
#36526=LINE ( 'NONE', #49050, #103798 ) ;
#36534=CARTESIAN_POINT ( 'NONE',  ( 8.000000000000000000, -11.18750000409677092, 0.000000000000000000 ) ) ;
#36556=EDGE_LOOP ( 'NONE', ( #15756, #27300, #19656 ) ) ;
#36577=B_SPLINE_CURVE_WITH_KNOTS ( 'NONE', 3,
 ( #77694, #21606, #28112, #86337, #62576, #94954, #44264, #53926, #12402, #45334, #29703, #54437, #60987, #85804, #78214, #3803, #86857, #61526, #87385, #13461, #101435, #44805, #77155, #2723, #12933, #27587, #36743, #45853, #20033, #78727, #11878, #69605, #4865, #85248 ),
 .UNSPECIFIED., .F., .F.,
 ( 4, 2, 2, 2, 2, 2, 2, 2, 2, 2, 2, 2, 2, 2, 2, 2, 4 ),
 ( 0.01263889472610568547, 0.01342810546992896127, 0.01421731621375223707, 0.01500652695757551114, 0.01579573770139878694, 0.01658494844522206274, 0.01737415918904533854, 0.01816336993286861434, 0.01895258067669189014, 0.01974179142051516594, 0.02053100216433844175, 0.02132021290816171755, 0.02210942365198499335, 0.02289863439580826915, 0.02368784513963154842, 0.02447705588345482075, 0.02526626662727809655 ),
 .UNSPECIFIED. ) ;
#36669=CARTESIAN_POINT ( 'NONE',  ( -5.656854249492381470, -20.56249999999999289, 5.656854249492379694 ) ) ;
#36722=CARTESIAN_POINT ( 'NONE',  ( -5.656854249492379694, -11.93749999999999289, -5.656854249492380582 ) ) ;
#36743=CARTESIAN_POINT ( 'NONE',  ( -9.482993638194542996, 102.5565127974632560, -3.177441187500465336 ) ) ;
#36745=SURFACE_SIDE_STYLE ('',( #77157 ) ) ;
#36758=CARTESIAN_POINT ( 'NONE',  ( 7.188101187499999156, -15.12500000204838457, 2.977408999572654924 ) ) ;
#36783=B_SPLINE_CURVE_WITH_KNOTS ( 'NONE', 3,
 ( #24426, #9777, #34644, #41104, #9247, #1137, #65904, #90183, #89657, #67512, #15757, #57795, #81524, #7648, #40565, #106343, #16285, #49170, #73984, #66, #78246, #27084, #93908, #18443, #61021, #36243, #11366, #52368, #85835, #100393, #101467, #92831, #76116, #102529 ),
 .UNSPECIFIED., .F., .F.,
 ( 4, 2, 2, 2, 2, 2, 2, 2, 2, 2, 2, 2, 2, 2, 2, 2, 4 ),
 ( 0.000000000000000000, 0.0007951492273476376636, 0.001590298454695275327, 0.002385447682042913208, 0.003180596909390550654, 0.003975746136738188101, 0.004770895364085826415, 0.005566044591433463862, 0.006361193818781101308, 0.007156343046128739623, 0.007951492273476376202, 0.008746641500824015383, 0.009541790728171654565, 0.01033693995551929375, 0.01113208918286693293, 0.01192723841021457211, 0.01272238763756221129 ),
 .UNSPECIFIED. ) ;
#36784=CARTESIAN_POINT ( 'NONE',  ( 0.000000000000000000, -30.00000000000000000, 0.000000000000000000 ) ) ;
#36795=CARTESIAN_POINT ( 'NONE',  ( -1.320432766682874540E-15, -13.90625000204838457, 7.188101187500000044 ) ) ;
#36821=CARTESIAN_POINT ( 'NONE',  ( 4.401442555609581635E-16, -24.78125000204838813, -7.188101187500000044 ) ) ;
#36840=CARTESIAN_POINT ( 'NONE',  ( 9.537909130738276176, 102.3538516903660565, -3.010726932293859459 ) ) ;
#36870=CARTESIAN_POINT ( 'NONE',  ( -1.320432766682874540E-15, -24.40625000204838813, 7.188101187500000044 ) ) ;
#36880=CARTESIAN_POINT ( 'NONE',  ( 2.977408999572650927, -32.75000000204839523, -7.188101187500001821 ) ) ;
#36909=CARTESIAN_POINT ( 'NONE',  ( 9.165151389911679658, 30.00000000000000000, 4.000000000000000000 ) ) ;
#36919=CARTESIAN_POINT ( 'NONE',  ( 2.977408999572651815, -33.31250000204838813, 7.188101187500000933 ) ) ;
#36934=CARTESIAN_POINT ( 'NONE',  ( -2.977408999572654480, -16.62500000204838813, 7.188101187499999156 ) ) ;
#36939=CARTESIAN_POINT ( 'NONE',  ( -9.253800200985685009, 83.69989668911827607, -3.791983798715483189 ) ) ;
#36941=CARTESIAN_POINT ( 'NONE',  ( -8.000000000000000000, -16.53125000409677270, -3.313708498984762496 ) ) ;
#36960=ORIENTED_EDGE ( 'NONE', *, *, #19700, .T. ) ;
#37006=CARTESIAN_POINT ( 'NONE',  ( 7.188101187499999156, -23.75000000204839168, 2.977408999572654924 ) ) ;
#37038=ORIENTED_EDGE ( 'NONE', *, *, #102852, .F. ) ;
#37045=CARTESIAN_POINT ( 'NONE',  ( -5.656854249492379694, -16.62500000409677270, -5.656854249492380582 ) ) ;
#37075=VECTOR ( 'NONE', #31178, 1000.000000000000000 ) ;
#37098=SURFACE_STYLE_USAGE ( .BOTH. , #68374 ) ;
#37107=( GEOMETRIC_REPRESENTATION_CONTEXT ( 3 ) GLOBAL_UNCERTAINTY_ASSIGNED_CONTEXT ( ( #52365 ) ) GLOBAL_UNIT_ASSIGNED_CONTEXT ( ( #87594, #86019, #63326 ) ) REPRESENTATION_CONTEXT ( 'NONE', 'WORKASPACE' ) );
#37154=ORIENTED_EDGE ( 'NONE', *, *, #79119, .F. ) ;
#37167=DIRECTION ( 'NONE',  ( -1.000000000000000000, -0.000000000000000000, -0.000000000000000000 ) ) ;
#37191=CARTESIAN_POINT ( 'NONE',  ( 5.656854249492378806, -20.18749999999999289, 5.656854249492381470 ) ) ;
#37213=VECTOR ( 'NONE', #19363, 1000.000000000000000 ) ;
#37230=ADVANCED_FACE ( 'NONE', ( #103554 ), #12403, .T. ) ;
#37242=ORIENTED_EDGE ( 'NONE', *, *, #73465, .T. ) ;
#37244=CARTESIAN_POINT ( 'NONE',  ( -5.656854249492381470, -11.56249999999999289, 5.656854249492379694 ) ) ;
#37245=CARTESIAN_POINT ( 'NONE',  ( -9.999952458099484076, 26.00011885476135376, 0.2653554233229072357 ) ) ;
#37264=PRESENTATION_STYLE_ASSIGNMENT (( #30216 ) ) ;
#37280=CARTESIAN_POINT ( 'NONE',  ( 7.188101187499999156, -13.62500000204838457, 2.977408999572654924 ) ) ;
#37319=LINE ( 'NONE', #29237, #68318 ) ;
#37324=CARTESIAN_POINT ( 'NONE',  ( -2.977408999572654480, -14.00000000204838457, 7.188101187499999156 ) ) ;
#37349=CARTESIAN_POINT ( 'NONE',  ( 2.977408999572651815, -22.43750000204838813, 7.188101187500000933 ) ) ;
#37369=CARTESIAN_POINT ( 'NONE',  ( 9.699016383038308931, 101.8236182855165453, 2.444973590251038775 ) ) ;
#37404=CARTESIAN_POINT ( 'NONE',  ( -7.188101187500002709, -18.68750000204838457, 2.977408999572647819 ) ) ;
#37413=CARTESIAN_POINT ( 'NONE',  ( 7.188101187499999156, -33.12500000204838813, 2.977408999572654924 ) ) ;
#37453=CARTESIAN_POINT ( 'NONE',  ( 7.188101187499999156, -33.12500000204838813, 2.977408999572654924 ) ) ;
#37462=VECTOR ( 'NONE', #6302, 1000.000000000000000 ) ;
#37471=CARTESIAN_POINT ( 'NONE',  ( 5.082755093536324154, -16.34375000204838813, 5.082755093536326818 ) ) ;
#37480=CARTESIAN_POINT ( 'NONE',  ( -8.000000000000001776, -17.84375000409677270, 3.313708498984758943 ) ) ;
#37485=CARTESIAN_POINT ( 'NONE',  ( 0.000000000000000000, 16.00000000000000000, 0.000000000000000000 ) ) ;
#37487=CARTESIAN_POINT ( 'NONE',  ( 5.561881810733785514, -30.00000000000001421, -4.944729227524142345 ) ) ;
#37525=ADVANCED_FACE ( 'NONE', ( #27993 ), #37676, .F. ) ;
#37541=CARTESIAN_POINT ( 'NONE',  ( -7.188101187500001821, -27.50000000204838813, -2.977408999572651371 ) ) ;
#37563=CARTESIAN_POINT ( 'NONE',  ( 0.000000000000000000, -30.00000000000000000, 0.000000000000000000 ) ) ;
#37592=CARTESIAN_POINT ( 'NONE',  ( -1.749814335632529083, 15.56087475005694643, -9.852235012526419311 ) ) ;
#37594=CARTESIAN_POINT ( 'NONE',  ( 3.313708498984761608, -10.90625000409677092, -8.000000000000000000 ) ) ;
#37605=ORIENTED_EDGE ( 'NONE', *, *, #31670, .T. ) ;
#37606=CARTESIAN_POINT ( 'NONE',  ( 7.150053860865852151, 28.21734546086023343, 3.590189269391290239 ) ) ;
#37613=CARTESIAN_POINT ( 'NONE',  ( 9.607612890400023531, 15.83452282593334637, 2.797297131808757165 ) ) ;
#37634=CARTESIAN_POINT ( 'NONE',  ( -9.090909090909089940, 15.00000000000000000, 4.165977904505306917 ) ) ;
#37676=CYLINDRICAL_SURFACE ( 'NONE', #23658, 4.000000000000000000 ) ;
#37705=CARTESIAN_POINT ( 'NONE',  ( 0.9654893961777153422, -30.00000000000000355, 7.122964895856731538 ) ) ;
#37719=B_SPLINE_CURVE_WITH_KNOTS ( 'NONE', 3,
 ( #63920, #14804, #48751, #73026, #98897, #183, #23470, #25058, #32082, #73562, #66017, #106464, #33149, #55776, #96808, #105936, #88712, #24008, #56852, #47698, #15877, #97318, #64957, #80598, #16951, #7240, #57381, #90294, #57912, #7771, #89774, #6720, #16404, #32622 ),
 .UNSPECIFIED., .F., .F.,
 ( 4, 2, 2, 2, 2, 2, 2, 2, 2, 2, 2, 2, 2, 2, 2, 2, 4 ),
 ( 1.409296014025916843E-17, 0.0007899309203816181355, 0.001579861840763222176, 0.002369792761144825892, 0.003159723681526430041, 0.003949654601908034190, 0.004739585522289637906, 0.005529516442671242489, 0.006319447363052846205, 0.007109378283434449920, 0.007899309203816054503, 0.008689240124197658219, 0.009479171044579261934, 0.01026910196496086565, 0.01105903288534247110, 0.01184896380572407482, 0.01263889472610567853 ),
 .UNSPECIFIED. ) ;
#37720=DIRECTION ( 'NONE',  ( -0.000000000000000000, 1.000000000000000000, -0.000000000000000000 ) ) ;
#37721=EDGE_CURVE ( 'NONE', #99675, #88535, #88836, .T. ) ;
#37734=CARTESIAN_POINT ( 'NONE',  ( 3.313708498984762496, -18.78124999999998934, 7.999999999999998224 ) ) ;
#37754=EDGE_CURVE ( 'NONE', #24908, #3711, #71573, .T. ) ;
#37759=VERTEX_POINT ( 'NONE', #75159 ) ;
#37769=AXIS2_PLACEMENT_3D ( 'NONE', #4154, #85069, #102846 ) ;
#37778=CARTESIAN_POINT ( 'NONE',  ( -9.253800200985683233, 28.69989668911828318, -3.791983798715485410 ) ) ;
#37800=CARTESIAN_POINT ( 'NONE',  ( 3.997425403568004132, 15.99999999372935022, -9.168149550321022190 ) ) ;
#37813=ORIENTED_EDGE ( 'NONE', *, *, #57500, .T. ) ;
#37817=CARTESIAN_POINT ( 'NONE',  ( 7.188101187500000044, -15.03125000204838457, 0.000000000000000000 ) ) ;
#37857=CARTESIAN_POINT ( 'NONE',  ( -7.188101187500002709, -14.18750000204838280, 2.977408999572648707 ) ) ;
#37882=CARTESIAN_POINT ( 'NONE',  ( 2.977408999572651815, -19.43750000204838457, 7.188101187500000933 ) ) ;
#37932=CARTESIAN_POINT ( 'NONE',  ( -7.188101187500002709, -17.18750000204838813, 2.977408999572647819 ) ) ;
#37942=CARTESIAN_POINT ( 'NONE',  ( 5.082755093536325930, -9.968750002048384573, -5.082755093536325042 ) ) ;
#37985=CARTESIAN_POINT ( 'NONE',  ( 7.188101187500001821, -29.93750000204839523, -2.977408999572650483 ) ) ;
#37995=CARTESIAN_POINT ( 'NONE',  ( -3.313708498984726969, -20.46874999999999289, 8.000000000000039080 ) ) ;
#37998=CARTESIAN_POINT ( 'NONE',  ( 5.082755093536324154, -20.84375000204838813, 5.082755093536326818 ) ) ;
#38005=CARTESIAN_POINT ( 'NONE',  ( -9.482993638194541219, 82.55651279746325599, -3.177441187500463116 ) ) ;
#38008=CARTESIAN_POINT ( 'NONE',  ( -3.313708498984760720, -10.71875000409676915, -8.000000000000000000 ) ) ;
#38011=CARTESIAN_POINT ( 'NONE',  ( 9.700350089084166072, 15.75268258782372754, 2.455962139888934193 ) ) ;
#38014=CARTESIAN_POINT ( 'NONE',  ( 3.313708498984722972, -19.71874999999999289, -8.000000000000040856 ) ) ;
#38015=CARTESIAN_POINT ( 'NONE',  ( -9.989285784994811124, 33.97342427445700963, 0.5301777604595827587 ) ) ;
#38024=DIRECTION ( 'NONE',  ( 0.000000000000000000, 0.000000000000000000, 1.000000000000000000 ) ) ;
#38043=CARTESIAN_POINT ( 'NONE',  ( 0.000000000000000000, 15.00000000000000000, -10.00000000000000000 ) ) ;
#38072=CARTESIAN_POINT ( 'NONE',  ( 7.188101187500001821, -28.06250000204838813, -2.977408999572650483 ) ) ;
#38074=CARTESIAN_POINT ( 'NONE',  ( 0.000000000000000000, 0.000000000000000000, 0.000000000000000000 ) ) ;
#38094=CARTESIAN_POINT ( 'NONE',  ( -1.469576158976823947E-15, -14.37499999999999112, 8.000000000000000000 ) ) ;
#38139=CARTESIAN_POINT ( 'NONE',  ( 3.313708498984762496, -29.46875000409677625, 7.999999999999998224 ) ) ;
#38156=CARTESIAN_POINT ( 'NONE',  ( -9.999999999999998224, 15.00000000000000000, 0.7768758660237131686 ) ) ;
#38180=DIRECTION ( 'NONE',  ( 0.000000000000000000, 0.000000000000000000, 1.000000000000000000 ) ) ;
#38190=CARTESIAN_POINT ( 'NONE',  ( 5.656854249492378806, -12.87500000409676915, 5.656854249492381470 ) ) ;
#38205=PRODUCT ( '7. Anchor', '7. Anchor', '', ( #40099 ) ) ;
#38251=CARTESIAN_POINT ( 'NONE',  ( 7.999999999999998224, -17.09374999999999289, 3.313708498984766493 ) ) ;
#38266=( BOUNDED_CURVE ( )  B_SPLINE_CURVE ( 2, ( #101364, #35060, #51733, #91164, #76538, #58235, #67928, #75481, #25930 ),
 .UNSPECIFIED., .F., .F. ) 
 B_SPLINE_CURVE_WITH_KNOTS ( ( 3, 2, 2, 2, 3 ),
 ( 0.4558823529411765718, 0.4632352941176471894, 0.4705882352941177516, 0.4779411764705884247, 0.4852941176470589868 ),
 .UNSPECIFIED. ) 
 CURVE ( )  GEOMETRIC_REPRESENTATION_ITEM ( )  RATIONAL_B_SPLINE_CURVE ( ( 0.9999999999999988898, 0.9238795325112878487, 1.000000000000000000, 0.9238795325112867385, 1.000000000000000000, 0.9238795325112867385, 1.000000000000000000, 0.9238795325112849621, 1.000000000000001776 ) ) 
 REPRESENTATION_ITEM ( '' )  );
#38298=CARTESIAN_POINT ( 'NONE',  ( -9.177080501238306098, 29.46653057145731580, -3.972956046786646489 ) ) ;
#38303=EDGE_LOOP ( 'NONE', ( #54972, #74612, #93676, #78494 ) ) ;
#38317=( LENGTH_UNIT ( ) NAMED_UNIT ( * ) SI_UNIT ( .MILLI., .METRE. ) );
#38364=CARTESIAN_POINT ( 'NONE',  ( 7.986711519608433285, 33.97361903623433932, -0.5300249774147544057 ) ) ;
#38365=CARTESIAN_POINT ( 'NONE',  ( -7.619753052866897747, 26.82548497192825465, -2.447276542590443249 ) ) ;
#38372=CARTESIAN_POINT ( 'NONE',  ( -7.188101187500000044, -11.28125000204838457, -8.802885111219163269E-16 ) ) ;
#38398=CARTESIAN_POINT ( 'NONE',  ( -2.977408999572654480, -21.12500000204838813, 7.188101187499999156 ) ) ;
#38410=CARTESIAN_POINT ( 'NONE',  ( 4.898587196589412829E-16, -21.31250000409676915, -8.000000000000000000 ) ) ;
#38446=CARTESIAN_POINT ( 'NONE',  ( 5.082755093536325930, -22.34375000204838457, -5.082755093536325042 ) ) ;
#38456=CARTESIAN_POINT ( 'NONE',  ( -5.082755093536326818, -30.59375000204838813, 5.082755093536325042 ) ) ;
#38473=LINE ( 'NONE', #70823, #52089 ) ;
#38490=( GEOMETRIC_REPRESENTATION_CONTEXT ( 3 ) GLOBAL_UNCERTAINTY_ASSIGNED_CONTEXT ( ( #9291 ) ) GLOBAL_UNIT_ASSIGNED_CONTEXT ( ( #43931, #18619, #17547 ) ) REPRESENTATION_CONTEXT ( 'NONE', 'WORKASPACE' ) );
#38497=CARTESIAN_POINT ( 'NONE',  ( 4.401442555609581635E-16, -32.65625000204838813, -7.188101187500000044 ) ) ;
#38508=CARTESIAN_POINT ( 'NONE',  ( 7.188101187500000044, -17.65625000204838457, 0.000000000000000000 ) ) ;
#38517=CARTESIAN_POINT ( 'NONE',  ( -9.699189539447123920, 81.82307771753286829, -2.444343703917209343 ) ) ;
#38519=CARTESIAN_POINT ( 'NONE',  ( -8.000000000000001776, -13.34375000409676915, 3.313708498984758943 ) ) ;
#38521=PRESENTATION_STYLE_ASSIGNMENT (( #102707 ) ) ;
#38525=CARTESIAN_POINT ( 'NONE',  ( 8.000000000000000000, -19.90624999999999289, -3.313708498984761164 ) ) ;
#38552=( BOUNDED_CURVE ( )  B_SPLINE_CURVE ( 2, ( #66700, #98523, #24670, #90443, #16554, #49437, #74248, #99041, #25209 ),
 .UNSPECIFIED., .F., .F. ) 
 B_SPLINE_CURVE_WITH_KNOTS ( ( 3, 2, 2, 2, 3 ),
 ( 0.1911764705882352811, 0.1985294117647058709, 0.2058823529411764608, 0.2132352941176470784, 0.2205882352941176683 ),
 .UNSPECIFIED. ) 
 CURVE ( )  GEOMETRIC_REPRESENTATION_ITEM ( )  RATIONAL_B_SPLINE_CURVE ( ( 1.000000000000000000, 0.9238795325112867385, 1.000000000000000000, 0.9238795325112867385, 1.000000000000000000, 0.9238795325112867385, 1.000000000000000000, 0.9238795325112864054, 1.000000000000000222 ) ) 
 REPRESENTATION_ITEM ( '' )  );
#38574=CARTESIAN_POINT ( 'NONE',  ( 4.165977904505308693, 16.00000000000000000, 9.090909090909091717 ) ) ;
#38580=CARTESIAN_POINT ( 'NONE',  ( 7.188101187500000044, -22.15625000204838457, 0.000000000000000000 ) ) ;
#38593=ORIENTED_EDGE ( 'NONE', *, *, #54812, .F. ) ;
#38617=ORIENTED_EDGE ( 'NONE', *, *, #71269, .F. ) ;
#38647=CARTESIAN_POINT ( 'NONE',  ( 3.313708498984762496, -27.96875000409677980, 7.999999999999998224 ) ) ;
#38673=ORIENTED_EDGE ( 'NONE', *, *, #83718, .T. ) ;
#38747=CIRCLE ( 'NONE', #18110, 1.000000000000000888 ) ;
#38760=EDGE_LOOP ( 'NONE', ( #65423, #74385, #56361, #45515 ) ) ;
#38766=CARTESIAN_POINT ( 'NONE',  ( -8.000000000000000000, -17.84374999999999289, -3.313708498984762496 ) ) ;
#38787=CARTESIAN_POINT ( 'NONE',  ( 9.341953373612906120, 15.21714514899110071, -3.572352985695328442 ) ) ;
#38808=CARTESIAN_POINT ( 'NONE',  ( 5.656854249492378806, -27.87500000409677270, 5.656854249492381470 ) ) ;
#38821=ORIENTED_EDGE ( 'NONE', *, *, #63984, .F. ) ;
#38827=( NAMED_UNIT ( * ) SI_UNIT ( $, .STERADIAN. ) SOLID_ANGLE_UNIT ( ) );
#38879=CARTESIAN_POINT ( 'NONE',  ( 6.928203230275509661, 30.26479267253571592, 3.999999999999999112 ) ) ;
#38888=CARTESIAN_POINT ( 'NONE',  ( -4.413588872808956509, -9.563952367648484554, 5.751921314263696239 ) ) ;
#38915=CARTESIAN_POINT ( 'NONE',  ( -5.082755093536325042, -20.09375000204838457, -5.082755093536325930 ) ) ;
#38936=DIRECTION ( 'NONE',  ( -0.9090909090909091717, 0.000000000000000000, -0.4165977904505311913 ) ) ;
#38963=CARTESIAN_POINT ( 'NONE',  ( 4.401442555609581635E-16, -17.65625000204838813, -7.188101187500000044 ) ) ;
#38968=CARTESIAN_POINT ( 'NONE',  ( -1.469576158976823947E-15, -26.56250000409677270, 8.000000000000000000 ) ) ;
#38971=CARTESIAN_POINT ( 'NONE',  ( -7.188101187500000044, -29.28125000204838813, -8.802885111219163269E-16 ) ) ;
#38974=CARTESIAN_POINT ( 'NONE',  ( 5.082755093536324154, -27.21875000204838813, 5.082755093536326818 ) ) ;
#39015=CARTESIAN_POINT ( 'NONE',  ( -2.977408999572654480, -27.50000000204838813, 7.188101187499999156 ) ) ;
#39031=CARTESIAN_POINT ( 'NONE',  ( 7.188101187499999156, -14.75000000204838457, 2.977408999572654924 ) ) ;
#39041=CARTESIAN_POINT ( 'NONE',  ( 8.000000000000000000, -11.09375000409677092, -3.313708498984761608 ) ) ;
#39051=DIRECTION ( 'NONE',  ( 0.000000000000000000, 0.000000000000000000, 1.000000000000000000 ) ) ;
#39057=CARTESIAN_POINT ( 'NONE',  ( -2.563280883359616791, 15.30085158940939571, 9.673800154114420735 ) ) ;
#39068=CARTESIAN_POINT ( 'NONE',  ( 10.00000000000000000, 15.00000000000000000, 10.00000000000000000 ) ) ;
#39109=CARTESIAN_POINT ( 'NONE',  ( -2.977408999572650039, -18.68750000204838102, -7.188101187500001821 ) ) ;
#39122=DIRECTION ( 'NONE',  ( 0.000000000000000000, 0.000000000000000000, -1.000000000000000000 ) ) ;
#39132=CARTESIAN_POINT ( 'NONE',  ( -3.313708498984760276, -19.71875000409677270, -8.000000000000000000 ) ) ;
#39173=CARTESIAN_POINT ( 'NONE',  ( 8.000000000000000000, -29.18750000409677270, 0.000000000000000000 ) ) ;
#39201=CARTESIAN_POINT ( 'NONE',  ( 0.000000000000000000, 115.0000000000000000, 0.000000000000000000 ) ) ;
#39223=CARTESIAN_POINT ( 'NONE',  ( -5.656854249492379694, -21.12500000409676915, -5.656854249492380582 ) ) ;
#39251=ORIENTED_EDGE ( 'NONE', *, *, #82549, .T. ) ;
#39253=LINE ( 'NONE', #72128, #37075 ) ;
#39273=COLOUR_RGB ( '', 0.40784314, 0.44705882, 0.49803922) ;
#39299=CARTESIAN_POINT ( 'NONE',  ( -8.000000000000001776, -17.65624999999999289, 3.313708498984758943 ) ) ;
#39301=ADVANCED_FACE ( 'NONE', ( #3340 ), #83705, .T. ) ;
#39325=CARTESIAN_POINT ( 'NONE',  ( 9.999999999999998224, 15.00000000000000000, -1.734723475976806306E-15 ) ) ;
#39417=CARTESIAN_POINT ( 'NONE',  ( -6.928203230275512325, 29.73116675491001715, -4.000000000000001776 ) ) ;
#39424=CARTESIAN_POINT ( 'NONE',  ( 8.000000000000000000, -30.40625000000000000, -3.313708498984761608 ) ) ;
#39427=VECTOR ( 'NONE', #58654, 1000.000000000000000 ) ;
#39445=CIRCLE ( 'NONE', #84238, 10.00000000000000000 ) ;
#39451=CARTESIAN_POINT ( 'NONE',  ( 5.082755093536324154, -20.84375000204838813, 5.082755093536326818 ) ) ;
#39454=( GEOMETRIC_REPRESENTATION_CONTEXT ( 3 ) GLOBAL_UNCERTAINTY_ASSIGNED_CONTEXT ( ( #46150 ) ) GLOBAL_UNIT_ASSIGNED_CONTEXT ( ( #17074, #16526, #66680 ) ) REPRESENTATION_CONTEXT ( 'NONE', 'WORKASPACE' ) );
#39455=ORIENTED_EDGE ( 'NONE', *, *, #78040, .T. ) ;
#39461=VERTEX_POINT ( 'NONE', #15660 ) ;
#39479=( BOUNDED_CURVE ( )  B_SPLINE_CURVE ( 2, ( #25268, #26353, #59748, #75372, #1471, #912, #57580 ),
 .UNSPECIFIED., .F., .F. ) 
 B_SPLINE_CURVE_WITH_KNOTS ( ( 3, 2, 2, 3 ),
 ( 0.1445660357747511060, 0.1470588235294117696, 0.1544117647058823317, 0.1617647058823529216 ),
 .UNSPECIFIED. ) 
 CURVE ( )  GEOMETRIC_REPRESENTATION_ITEM ( )  RATIONAL_B_SPLINE_CURVE ( ( 0.9658850655769295468, 0.9741937049840523333, 1.000000000000000000, 0.9238795325112867385, 1.000000000000000000, 0.9238795325112870716, 0.9999999999999996669 ) ) 
 REPRESENTATION_ITEM ( '' )  );
#39500=CARTESIAN_POINT ( 'NONE',  ( -5.082755093536326818, -20.09375000204838457, 5.082755093536325042 ) ) ;
#39503=CARTESIAN_POINT ( 'NONE',  ( -3.313708498984783812, -26.65625000409676915, 7.999999999999979572 ) ) ;
#39509=CARTESIAN_POINT ( 'NONE',  ( 2.977408999572650927, -23.75000000204839168, -7.188101187500001821 ) ) ;
#39520=EDGE_LOOP ( 'NONE', ( #765, #76543 ) ) ;
#39534=DIRECTION ( 'NONE',  ( 0.000000000000000000, 1.000000000000000000, 0.000000000000000000 ) ) ;
#39550=CYLINDRICAL_SURFACE ( 'NONE', #31152, 8.000000000000000000 ) ;
#39552=CARTESIAN_POINT ( 'NONE',  ( -7.188101187500000044, -26.28125000204838813, -8.802885111219163269E-16 ) ) ;
#39562=AXIS2_PLACEMENT_3D ( 'NONE', #59239, #84032, #76458 ) ;
#39567=CARTESIAN_POINT ( 'NONE',  ( 7.188101187500000933, -10.06250000204838457, -2.977408999572650483 ) ) ;
#39579=CARTESIAN_POINT ( 'NONE',  ( -8.000000000000000000, -11.93750000409677092, -9.797174393178825657E-16 ) ) ;
#39591=( LENGTH_UNIT ( ) NAMED_UNIT ( * ) SI_UNIT ( .MILLI., .METRE. ) );
#39643=CARTESIAN_POINT ( 'NONE',  ( 2.977408999572651815, -19.43750000204838457, 7.188101187500000933 ) ) ;
#39659=DIRECTION ( 'NONE',  ( 0.000000000000000000, 0.000000000000000000, 1.000000000000000000 ) ) ;
#39669=ADVANCED_BREP_SHAPE_REPRESENTATION ( '', ( #51906, #10728 ), #38490 ) ;
#39701=CARTESIAN_POINT ( 'NONE',  ( 5.656854249492378806, -29.37500000409677270, 5.656854249492381470 ) ) ;
#39704=EDGE_CURVE ( 'NONE', #103615, #84434, #58799, .T. ) ;
#39706=CARTESIAN_POINT ( 'NONE',  ( 9.842984802582137149, 33.59069590475652234, 1.781981959250508618 ) ) ;
#39778=ORIENTED_EDGE ( 'NONE', *, *, #31759, .F. ) ;
#39801=ADVANCED_FACE ( 'NONE', ( #28450 ), #64678, .T. ) ;
#39814=( BOUNDED_CURVE ( )  B_SPLINE_CURVE ( 2, ( #69359, #44006, #102238, #20852, #60739, #19780, #69879, #61263, #53686 ),
 .UNSPECIFIED., .F., .F. ) 
 B_SPLINE_CURVE_WITH_KNOTS ( ( 3, 2, 2, 2, 3 ),
 ( 0.6617647058823529216, 0.6691176470588234837, 0.6764705882352941568, 0.6838235294117648300, 0.6911764705882353921 ),
 .UNSPECIFIED. ) 
 CURVE ( )  GEOMETRIC_REPRESENTATION_ITEM ( )  RATIONAL_B_SPLINE_CURVE ( ( 1.000000000000000000, 0.9238795325112867385, 1.000000000000000000, 0.9238795325112867385, 1.000000000000000000, 0.9238795325112867385, 1.000000000000000000, 0.9238795325112856283, 1.000000000000001110 ) ) 
 REPRESENTATION_ITEM ( '' )  );
#39824=CARTESIAN_POINT ( 'NONE',  ( 8.000000000000000000, -13.99999999999999112, 0.000000000000000000 ) ) ;
#39829=CARTESIAN_POINT ( 'NONE',  ( 4.165977904505311358, 16.00000000000000000, -9.090909090909089940 ) ) ;
#39850=CARTESIAN_POINT ( 'NONE',  ( 9.673800154114786665, 15.30085158940974921, -2.563280883359599027 ) ) ;
#39867=CARTESIAN_POINT ( 'NONE',  ( -9.607634652977999679, 15.83450757143046950, 2.797224791467300076 ) ) ;
#39881=CARTESIAN_POINT ( 'NONE',  ( -10.00000000000000000, 15.00000000000000000, -4.582575694955836276 ) ) ;
#39900=CARTESIAN_POINT ( 'NONE',  ( 2.977408999572650927, -10.25000000204838813, -7.188101187500001821 ) ) ;
#39944=CARTESIAN_POINT ( 'NONE',  ( -1.469576158976823947E-15, -33.87499999999999289, 8.000000000000000000 ) ) ;
#39968=CARTESIAN_POINT ( 'NONE',  ( 7.188101187499999156, -16.25000000204838813, 2.977408999572654924 ) ) ;
#39980=ORIENTED_EDGE ( 'NONE', *, *, #12978, .T. ) ;
#39982=DIRECTION ( 'NONE',  ( -0.5000109054779156015, 0.000000000000000000, 0.8660191074122758348 ) ) ;
#40017=CARTESIAN_POINT ( 'NONE',  ( 2.977408999572650927, -11.75000000204838813, -7.188101187500000933 ) ) ;
#40027=CARTESIAN_POINT ( 'NONE',  ( 5.082755093536325930, -26.84375000204838813, -5.082755093536325042 ) ) ;
#40035=B_SPLINE_CURVE_WITH_KNOTS ( 'NONE', 3,
 ( #36051, #60826, #51105, #61900, #93718, #85635, #10646, #43563, #92641, #76449, #94795, #44102, #84023, #26890, #59764, #10129, #43038, #28479, #12248, #44646, #77530, #3647, #69448, #2027, #18799, #29034, #86176, #45178, #34975, #100728, #2558, #35506, #68384, #76992 ),
 .UNSPECIFIED., .F., .F.,
 ( 4, 2, 2, 2, 2, 2, 2, 2, 2, 2, 2, 2, 2, 2, 2, 2, 4 ),
 ( 1.422579022190208801E-17, 0.0007899309203816186776, 0.001579861840763223261, 0.002369792761144827627, 0.003159723681526432210, 0.003949654601908035925, 0.004739585522289640508, 0.005529516442671245091, 0.006319447363052849674, 0.007109378283434454257, 0.007899309203816057973, 0.008689240124197663423, 0.009479171044579267139, 0.01026910196496087259, 0.01105903288534247630, 0.01184896380572408175, 0.01263889472610568547 ),
 .UNSPECIFIED. ) ;
#40048=DIRECTION ( 'NONE',  ( 0.000000000000000000, -0.000000000000000000, 1.000000000000000000 ) ) ;
#40065=CARTESIAN_POINT ( 'NONE',  ( 7.188101187499999156, -27.12500000204838457, 2.977408999572654924 ) ) ;
#40077=CARTESIAN_POINT ( 'NONE',  ( 4.401442555609581635E-16, -11.28125000204838457, -7.188101187500000044 ) ) ;
#40092=CARTESIAN_POINT ( 'NONE',  ( -5.656854249492379694, -10.62500000409677092, -5.656854249492380582 ) ) ;
#40099=PRODUCT_CONTEXT ( 'NONE', #56217, 'mechanical' ) ;
#40138=LINE ( 'NONE', #32072, #62459 ) ;
#40145=FACE_BOUND ( 'NONE', #83732, .T. ) ;
#40146=CARTESIAN_POINT ( 'NONE',  ( -7.188101187500001821, -17.00000000204838457, -2.977408999572651371 ) ) ;
#40152=CARTESIAN_POINT ( 'NONE',  ( -3.313708498984760276, -13.71875000409676737, -8.000000000000000000 ) ) ;
#40210=CARTESIAN_POINT ( 'NONE',  ( 7.999999999999998224, -29.28125000409677270, 3.313708498984766493 ) ) ;
#40214=CARTESIAN_POINT ( 'NONE',  ( 9.843481099141458301, 33.59204556153386534, -1.779148000612201352 ) ) ;
#40221=EDGE_CURVE ( 'NONE', #45098, #54191, #94310, .T. ) ;
#40222=CARTESIAN_POINT ( 'NONE',  ( -8.000000000000001776, -10.15624999999999112, 3.313708498984759387 ) ) ;
#40233=CARTESIAN_POINT ( 'NONE',  ( 4.898587196589412829E-16, -15.12499999999999289, -8.000000000000000000 ) ) ;
#40259=CARTESIAN_POINT ( 'NONE',  ( -6.274085929497640102, -30.00000000000001066, 4.398938879594368245 ) ) ;
#40290=( NAMED_UNIT ( * ) PLANE_ANGLE_UNIT ( ) SI_UNIT ( $, .RADIAN. ) );
#40311=VERTEX_POINT ( 'NONE', #22231 ) ;
#40316=CARTESIAN_POINT ( 'NONE',  ( 9.843481099141454749, 108.5920455615338653, -1.779148000612198022 ) ) ;
#40337=CARTESIAN_POINT ( 'NONE',  ( 5.656854249492378806, -17.18749999999999289, 5.656854249492381470 ) ) ;
#40401=CARTESIAN_POINT ( 'NONE',  ( 4.401442555609581635E-16, -33.78125000204838813, -7.188101187500000044 ) ) ;
#40404=CARTESIAN_POINT ( 'NONE',  ( 1.544939622598899831, 15.00000000000000000, -9.999999999999998224 ) ) ;
#40455=CARTESIAN_POINT ( 'NONE',  ( 5.082755093536325930, -14.46875000204838457, -5.082755093536325042 ) ) ;
#40463=CARTESIAN_POINT ( 'NONE',  ( 5.656854249492378806, -30.68749999999999645, 5.656854249492381470 ) ) ;
#40488=CARTESIAN_POINT ( 'NONE',  ( 7.188101187499999156, -13.25000000204838280, 2.977408999572654924 ) ) ;
#40491=VECTOR ( 'NONE', #72360, 1000.000000000000000 ) ;
#40539=CARTESIAN_POINT ( 'NONE',  ( -5.082755093536325042, -11.46875000204838635, -5.082755093536325930 ) ) ;
#40546=CARTESIAN_POINT ( 'NONE',  ( 6.797283463257937974, -29.92009708584722461, -3.368226723814712109 ) ) ;
#40549=CARTESIAN_POINT ( 'NONE',  ( -1.320432766682874540E-15, -25.90625000204838813, 7.188101187500000044 ) ) ;
#40565=CARTESIAN_POINT ( 'NONE',  ( -7.934914944860279817, 88.86845647200112808, -1.051261972695690439 ) ) ;
#40568=LINE ( 'NONE', #24431, #28047 ) ;
#40578=CARTESIAN_POINT ( 'NONE',  ( -8.000000000000000000, -25.43750000409677270, -9.797174393178825657E-16 ) ) ;
#40591=CARTESIAN_POINT ( 'NONE',  ( 5.082755093536325930, -25.34375000204838813, -5.082755093536325042 ) ) ;
#40603=CARTESIAN_POINT ( 'NONE',  ( 4.401442555609581635E-16, -15.78125000204838635, -7.188101187500000044 ) ) ;
#40615=CARTESIAN_POINT ( 'NONE',  ( -5.082755093536325042, -29.09375000204838813, -5.082755093536325930 ) ) ;
#40623=CARTESIAN_POINT ( 'NONE',  ( -2.918503601030651318, 15.30040232763897023, 9.571198553004045095 ) ) ;
#40664=CARTESIAN_POINT ( 'NONE',  ( 7.344361273354515163, 87.44560530588523761, -3.175733139645585457 ) ) ;
#40673=CARTESIAN_POINT ( 'NONE',  ( 7.188101187499999156, -19.25000000204838813, 2.977408999572654924 ) ) ;
#40690=FACE_OUTER_BOUND ( 'NONE', #92035, .T. ) ;
#40692=CARTESIAN_POINT ( 'NONE',  ( -3.313708498984765161, -19.15625000409677270, 7.999999999999998224 ) ) ;
#40706=ORIENTED_EDGE ( 'NONE', *, *, #83989, .T. ) ;
#40727=VECTOR ( 'NONE', #61117, 1000.000000000000000 ) ;
#40731=CARTESIAN_POINT ( 'NONE',  ( 3.368226723814772505, -29.92009708584722461, 6.797283463257880243 ) ) ;
#40741=CARTESIAN_POINT ( 'NONE',  ( 3.313708498984762052, -24.40625000409677270, -8.000000000000000000 ) ) ;
#40743=DIRECTION ( 'NONE',  ( 0.000000000000000000, 0.000000000000000000, 1.000000000000000000 ) ) ;
#40746=CARTESIAN_POINT ( 'NONE',  ( -3.884543032214529124, 15.13241195026090047, -9.216463528758191970 ) ) ;
#40776=CARTESIAN_POINT ( 'NONE',  ( -7.002619243997878939, 31.05007318013818463, -3.868708944012996920 ) ) ;
#40786=CARTESIAN_POINT ( 'NONE',  ( -7.782059566932863603, -29.99999999999999289, 1.004593303788806846 ) ) ;
#40815=FILL_AREA_STYLE_COLOUR ( '', #42646 ) ;
#40836=VERTEX_POINT ( 'NONE', #98483 ) ;
#40843=CARTESIAN_POINT ( 'NONE',  ( 9.797936955406314041, 108.4667168977048135, -2.012343231877594896 ) ) ;
#40866=CARTESIAN_POINT ( 'NONE',  ( -1.469576158976823947E-15, -11.37499999999999289, 8.000000000000000000 ) ) ;
#40872=CARTESIAN_POINT ( 'NONE',  ( -7.999885325681428405, 101.0002293487006426, 0.2682325777720032667 ) ) ;
#40898=CARTESIAN_POINT ( 'NONE',  ( 10.00000000000027178, 14.99999999999986500, -3.082707893549384792 ) ) ;
#40905=CARTESIAN_POINT ( 'NONE',  ( -7.414580834929599185, 82.35343719718518685, 3.010264818013834276 ) ) ;
#40913=CARTESIAN_POINT ( 'NONE',  ( -8.000000000000001776, -29.65625000000000000, 3.313708498984759387 ) ) ;
#40934=CARTESIAN_POINT ( 'NONE',  ( -2.977408999572654480, -30.12500000204838813, 7.188101187499999156 ) ) ;
#40997=CARTESIAN_POINT ( 'NONE',  ( 7.999999999999998224, -32.09374999999999289, 3.313708498984766493 ) ) ;
#41005=DIRECTION ( 'NONE',  ( 0.000000000000000000, 1.000000000000000000, 0.000000000000000000 ) ) ;
#41024=CARTESIAN_POINT ( 'NONE',  ( -1.320432766682874540E-15, -12.03125000204838635, 7.188101187500000044 ) ) ;
#41076=CARTESIAN_POINT ( 'NONE',  ( -5.082755093536325042, -14.46875000204838457, -5.082755093536325930 ) ) ;
#41081=VERTEX_POINT ( 'NONE', #54172 ) ;
#41085=CARTESIAN_POINT ( 'NONE',  ( -2.977408999572650039, -22.06250000204838813, -7.188101187500001821 ) ) ;
#41104=CARTESIAN_POINT ( 'NONE',  ( -7.002619243997878051, 86.05007318013815620, -3.868708944012997808 ) ) ;
#41126=FACE_OUTER_BOUND ( 'NONE', #99414, .T. ) ;
#41127=CARTESIAN_POINT ( 'NONE',  ( 9.798380800342661345, 26.53199345684497956, -2.010350564680329910 ) ) ;
#41129=CARTESIAN_POINT ( 'NONE',  ( -5.082755093536326818, -26.09375000204838813, 5.082755093536325042 ) ) ;
#41130=CARTESIAN_POINT ( 'NONE',  ( 9.165151389911679658, 105.0000000000000000, 4.000000000000001776 ) ) ;
#41140=CARTESIAN_POINT ( 'NONE',  ( 9.699121749566359085, 88.17668760275819295, 2.444499528233560426 ) ) ;
#41144=CARTESIAN_POINT ( 'NONE',  ( -2.977408999572650039, -11.18750000204838457, -7.188101187500000933 ) ) ;
#41155=LINE ( 'NONE', #16887, #55059 ) ;
#41156=CARTESIAN_POINT ( 'NONE',  ( -7.188101187500001821, -29.00000000204838813, -2.977408999572651371 ) ) ;
#41200=CARTESIAN_POINT ( 'NONE',  ( 7.897196874019792645, 88.79127204167808429, -1.302055520192086702 ) ) ;
#41209=CARTESIAN_POINT ( 'NONE',  ( 5.082755093536325930, -21.96875000204838457, -5.082755093536325042 ) ) ;
#41234=DIRECTION ( 'NONE',  ( -0.4165977904505313578, 0.000000000000000000, -0.9090909090909089496 ) ) ;
#41243=DIRECTION ( 'NONE',  ( 0.000000000000000000, 0.000000000000000000, -1.000000000000000000 ) ) ;
#41273=CARTESIAN_POINT ( 'NONE',  ( 8.000000000000000000, -21.68750000409676915, 0.000000000000000000 ) ) ;
#41312=CARTESIAN_POINT ( 'NONE',  ( -7.414346147792000075, 32.64589157662263830, -3.010818766110528344 ) ) ;
#41328=CARTESIAN_POINT ( 'NONE',  ( -1.469576158976823947E-15, -21.87499999999999289, 8.000000000000000000 ) ) ;
#41380=CARTESIAN_POINT ( 'NONE',  ( 9.989113211954169458, 108.9729927354899530, 0.5334031035448967284 ) ) ;
#41398=CARTESIAN_POINT ( 'NONE',  ( -8.000000000000001776, -10.15624999999999112, 3.313708498984758943 ) ) ;
#41432=CARTESIAN_POINT ( 'NONE',  ( -6.928203230275510549, 85.00000000000000000, 4.000000000000000000 ) ) ;
#41453=EDGE_LOOP ( 'NONE', ( #85243, #8196, #7158, #93076 ) ) ;
#41463=CARTESIAN_POINT ( 'NONE',  ( -2.977408999572654480, -31.62500000204838813, 7.188101187499999156 ) ) ;
#41524=CARTESIAN_POINT ( 'NONE',  ( -5.656854249492381470, -28.06249999999999645, 5.656854249492379694 ) ) ;
#41551=CARTESIAN_POINT ( 'NONE',  ( 5.082755093536324154, -14.84375000204838457, 5.082755093536326818 ) ) ;
#41609=CARTESIAN_POINT ( 'NONE',  ( 5.082755093536325930, -16.34375000204838813, -5.082755093536325042 ) ) ;
#41617=CARTESIAN_POINT ( 'NONE',  ( 5.082755093536325930, -19.34375000204838457, -5.082755093536325042 ) ) ;
#41648=CARTESIAN_POINT ( 'NONE',  ( 9.999999999999998224, 15.00000000000000000, -1.734723475976806897E-15 ) ) ;
#41656=CARTESIAN_POINT ( 'NONE',  ( 5.082755093536324154, -16.71875000204838813, 5.082755093536326818 ) ) ;
#41663=CARTESIAN_POINT ( 'NONE',  ( 9.948181520647857212, 88.86892802760380050, 1.049088206181487459 ) ) ;
#41677=CARTESIAN_POINT ( 'NONE',  ( -5.656854249492379694, -19.43749999999999289, -5.656854249492380582 ) ) ;
#41682=CARTESIAN_POINT ( 'NONE',  ( 5.082755093536324154, -32.84375000204838813, 5.082755093536326818 ) ) ;
#41730=CARTESIAN_POINT ( 'NONE',  ( 7.150931910075643216, 86.78625798522261903, -3.588457848165357067 ) ) ;
#41732=ORIENTED_EDGE ( 'NONE', *, *, #98234, .T. ) ;
#41738=CARTESIAN_POINT ( 'NONE',  ( 2.977408999572651815, -10.43750000204838457, 7.188101187500000933 ) ) ;
#41767=EDGE_CURVE ( 'NONE', #27681, #45098, #39814, .T. ) ;
#41794=CARTESIAN_POINT ( 'NONE',  ( 7.188101187500000044, -26.65625000204838813, 0.000000000000000000 ) ) ;
#41800=CARTESIAN_POINT ( 'NONE',  ( -8.000000000000001776, -23.84375000409677270, 3.313708498984758943 ) ) ;
#41807=( GEOMETRIC_REPRESENTATION_CONTEXT ( 3 ) GLOBAL_UNCERTAINTY_ASSIGNED_CONTEXT ( ( #44561 ) ) GLOBAL_UNIT_ASSIGNED_CONTEXT ( ( #7305, #47764, #79615 ) ) REPRESENTATION_CONTEXT ( 'NONE', 'WORKASPACE' ) );
#41842=CARTESIAN_POINT ( 'NONE',  ( -7.934883677559682269, 33.86839177937552137, 1.051380792122687646 ) ) ;
#41859=ORIENTED_EDGE ( 'NONE', *, *, #81717, .F. ) ;
#41896=EDGE_CURVE ( 'NONE', #81173, #102469, #79166, .T. ) ;
#41897=CARTESIAN_POINT ( 'NONE',  ( 0.000000000000000000, -30.00000000000000000, 8.000000000000000000 ) ) ;
#41920=AXIS2_PLACEMENT_3D ( 'NONE', #52520, #5049, #85436 ) ;
#41921=LINE ( 'NONE', #11132, #39427 ) ;
#41932=CARTESIAN_POINT ( 'NONE',  ( -7.551892080562057963, 101.9901229746061802, 2.647003822403975803 ) ) ;
#41941=CARTESIAN_POINT ( 'NONE',  ( 5.656854249492380582, -18.31249999999999289, -5.656854249492379694 ) ) ;
#41973=ORIENTED_EDGE ( 'NONE', *, *, #67216, .F. ) ;
#41979=ORIENTED_EDGE ( 'NONE', *, *, #45267, .T. ) ;
#41986=CARTESIAN_POINT ( 'NONE',  ( -8.000000000000001776, -28.15624999999999645, 3.313708498984759387 ) ) ;
#41995=CARTESIAN_POINT ( 'NONE',  ( -5.082755093536326818, -31.71875000204838457, 5.082755093536325042 ) ) ;
#42054=CARTESIAN_POINT ( 'NONE',  ( -3.313708498984765161, -26.46874999999999645, 7.999999999999998224 ) ) ;
#42068=AXIS2_PLACEMENT_3D ( 'NONE', #74951, #49624, #67423 ) ;
#42072=CARTESIAN_POINT ( 'NONE',  ( 7.344361273354512498, 107.4456053058852518, -3.175733139645587677 ) ) ;
#42075=EDGE_CURVE ( 'NONE', #10653, #81483, #106396, .T. ) ;
#42079=CARTESIAN_POINT ( 'NONE',  ( -7.188101187500002709, -15.31250000204838457, 2.977408999572648707 ) ) ;
#42093=DIRECTION ( 'NONE',  ( 1.000000000000000000, 0.000000000000000000, 0.000000000000000000 ) ) ;
#42130=CARTESIAN_POINT ( 'NONE',  ( 7.188101187500000933, -16.43750000204838813, -2.977408999572650483 ) ) ;
#42137=CARTESIAN_POINT ( 'NONE',  ( 7.188101187500000044, -19.53125000204838457, 0.000000000000000000 ) ) ;
#42165=CARTESIAN_POINT ( 'NONE',  ( 9.090909090909089940, 16.00000000000000000, -4.165977904505312246 ) ) ;
#42179=CARTESIAN_POINT ( 'NONE',  ( 9.253583916535172094, 28.70196091994965570, 3.792462592445553948 ) ) ;
#42180=CARTESIAN_POINT ( 'NONE',  ( -2.977408999572654480, -21.50000000204839168, 7.188101187499999156 ) ) ;
#42191=CARTESIAN_POINT ( 'NONE',  ( 9.381394091586569672, 87.01349605581610547, 3.465950112474255551 ) ) ;
#42206=ADVANCED_FACE ( 'NONE', ( #78890 ), #56177, .T. ) ;
#42208=CARTESIAN_POINT ( 'NONE',  ( -7.188101187500001821, -32.00000000204838813, -2.977408999572651371 ) ) ;
#42251=CARTESIAN_POINT ( 'NONE',  ( 7.619753052866894194, 88.17451502807173824, -2.447276542590444137 ) ) ;
#42255=ORIENTED_EDGE ( 'NONE', *, *, #100036, .F. ) ;
#42262=CARTESIAN_POINT ( 'NONE',  ( 7.188101187500000044, -13.15625000204838280, 0.000000000000000000 ) ) ;
#42289=VERTEX_POINT ( 'NONE', #33029 ) ;
#42302=CARTESIAN_POINT ( 'NONE',  ( 7.414346147791996522, 82.35410842337738302, -3.010818766110532785 ) ) ;
#42320=CARTESIAN_POINT ( 'NONE',  ( 2.977408999572652260, -25.43750000204838457, 7.188101187500000044 ) ) ;
#42325=SHAPE_REPRESENTATION_RELATIONSHIP ( 'NONE' , 'NONE' ,  #55690, #39669 ) ;
#42333=CARTESIAN_POINT ( 'NONE',  ( 4.898587196589412829E-16, -22.81250000409677270, -8.000000000000000000 ) ) ;
#42343=CARTESIAN_POINT ( 'NONE',  ( 0.000000000000000000, 15.00000000000000000, -9.999999999999998224 ) ) ;
#42367=AXIS2_PLACEMENT_3D ( 'NONE', #72509, #56301, #89769 ) ;
#42461=CARTESIAN_POINT ( 'NONE',  ( -7.151597709147946347, 103.2107073494778575, 3.587174531012139678 ) ) ;
#42489=EDGE_CURVE ( 'NONE', #94793, #59320, #101238, .T. ) ;
#42493=( NAMED_UNIT ( * ) SI_UNIT ( $, .STERADIAN. ) SOLID_ANGLE_UNIT ( ) );
#42495=CARTESIAN_POINT ( 'NONE',  ( -7.344361273354514275, 82.55439469411476239, -3.175733139645586345 ) ) ;
#42534=COLOUR_RGB ( '', 0.09019608, 0.27058824, 0.51372549) ;
#42582=CARTESIAN_POINT ( 'NONE',  ( 4.898587196589412829E-16, -27.12499999999999645, -8.000000000000000000 ) ) ;
#42596=DIRECTION ( 'NONE',  ( 0.000000000000000000, 0.000000000000000000, 1.000000000000000000 ) ) ;
#42608=CARTESIAN_POINT ( 'NONE',  ( -9.482856158761270748, 87.44307115854722667, 3.177891129109650770 ) ) ;
#42628=CARTESIAN_POINT ( 'NONE',  ( -10.00000000000000000, 0.000000000000000000, 10.00000000000000000 ) ) ;
#42646=COLOUR_RGB ( '', 0.08235294, 0.09019608, 0.10196078) ;
#42649=EDGE_LOOP ( 'NONE', ( #99219, #41979 ) ) ;
#42675=CARTESIAN_POINT ( 'NONE',  ( 7.188101187500001821, -19.43750000204838457, -2.977408999572650483 ) ) ;
#42701=CARTESIAN_POINT ( 'NONE',  ( 9.380169522195144438, 15.95824666716552009, -3.484756791224365990 ) ) ;
#42720=CARTESIAN_POINT ( 'NONE',  ( 4.401442555609581635E-16, -20.65625000204838813, -7.188101187500000044 ) ) ;
#42743=CYLINDRICAL_SURFACE ( 'NONE', #25873, 8.000000000000000000 ) ;
#42746=CARTESIAN_POINT ( 'NONE',  ( 2.977408999572651815, -29.93750000204839523, 7.188101187500000933 ) ) ;
#42797=CARTESIAN_POINT ( 'NONE',  ( 4.401442555609581635E-16, -25.15625000204838813, -7.188101187500000044 ) ) ;
#42803=CARTESIAN_POINT ( 'NONE',  ( -7.188101187500000044, -15.40625000204838635, -8.802885111219163269E-16 ) ) ;
#42837=VERTEX_POINT ( 'NONE', #38094 ) ;
#42839=ORIENTED_EDGE ( 'NONE', *, *, #56547, .T. ) ;
#42862=CARTESIAN_POINT ( 'NONE',  ( -2.977408999572650039, -24.68750000204838813, -7.188101187500000933 ) ) ;
#42870=CARTESIAN_POINT ( 'NONE',  ( -8.000000000000000000, -25.43750000409677270, -9.797174393178825657E-16 ) ) ;
#42879=CARTESIAN_POINT ( 'NONE',  ( -2.701558353794590861, 15.00000000000000000, -9.999999999999998224 ) ) ;
#42935=CARTESIAN_POINT ( 'NONE',  ( -3.313708498984688333, -21.96874999999999289, 8.000000000000074607 ) ) ;
#43001=AXIS2_PLACEMENT_3D ( 'NONE', #91173, #41005, #16728 ) ;
#43005=CARTESIAN_POINT ( 'NONE',  ( 8.000000000000000000, -10.99999999999999289, 0.000000000000000000 ) ) ;
#43038=CARTESIAN_POINT ( 'NONE',  ( -9.999945253488242258, 108.9998631337053467, -0.2662901834230876896 ) ) ;
#43042=EDGE_CURVE ( 'NONE', #28854, #60867, #104883, .T. ) ;
#43052=FACE_BOUND ( 'NONE', #69935, .T. ) ;
#43065=CARTESIAN_POINT ( 'NONE',  ( -5.656854249492379694, -28.43749999999999289, -5.656854249492380582 ) ) ;
#43079=CARTESIAN_POINT ( 'NONE',  ( 8.000000000000000000, -27.40624999999999645, -3.313708498984761164 ) ) ;
#43126=CARTESIAN_POINT ( 'NONE',  ( -8.000000000000000000, -29.74999999999999645, -9.797174393178825657E-16 ) ) ;
#43129=DIRECTION ( 'NONE',  ( -0.4165977904505304696, -3.915074853572114378E-16, 0.9090909090909092827 ) ) ;
#43138=EDGE_CURVE ( 'NONE', #33789, #49838, #59078, .T. ) ;
#43154=CARTESIAN_POINT ( 'NONE',  ( -9.989285784994814676, 88.97342427445701674, 0.5301777604595948601 ) ) ;
#43168=CARTESIAN_POINT ( 'NONE',  ( 0.000000000000000000, -30.00000000000000000, 0.000000000000000000 ) ) ;
#43171=ADVANCED_FACE ( 'NONE', ( #43422 ), #102181, .T. ) ;
#43188=EDGE_LOOP ( 'NONE', ( #38821, #62256 ) ) ;
#43214=CARTESIAN_POINT ( 'NONE',  ( 2.977408999572651815, -22.81250000204838813, 7.188101187500000933 ) ) ;
#43254=CARTESIAN_POINT ( 'NONE',  ( 9.221249107921748234, 28.95178628501513529, 3.869340886054257300 ) ) ;
#43255=CARTESIAN_POINT ( 'NONE',  ( 5.082755093536325930, -22.34375000204838457, -5.082755093536325042 ) ) ;
#43279=CARTESIAN_POINT ( 'NONE',  ( -5.082755093536325042, -27.59375000204838457, -5.082755093536325930 ) ) ;
#43334=CARTESIAN_POINT ( 'NONE',  ( -2.977408999572650039, -23.56250000204838813, -7.188101187500000933 ) ) ;
#43336=ORIENTED_EDGE ( 'NONE', *, *, #98052, .T. ) ;
#43343=CARTESIAN_POINT ( 'NONE',  ( -7.188101187500002709, -12.31250000204838635, 2.977408999572648707 ) ) ;
#43402=CARTESIAN_POINT ( 'NONE',  ( -2.977408999572654480, -22.62500000204838813, 7.188101187499999156 ) ) ;
#43411=MECHANICAL_DESIGN_GEOMETRIC_PRESENTATION_REPRESENTATION('',(#95079),#31355);
#43413=CARTESIAN_POINT ( 'NONE',  ( -8.000000000000000000, -14.93750000409677092, -9.797174393178825657E-16 ) ) ;
#43417=CARTESIAN_POINT ( 'NONE',  ( 9.537927238823506570, 32.64626857118177838, -3.010735687602430044 ) ) ;
#43422=FACE_OUTER_BOUND ( 'NONE', #4519, .T. ) ;
#43472=CARTESIAN_POINT ( 'NONE',  ( 0.7060372491588029487, 15.23416508904654521, 9.999999999999998224 ) ) ;
#43496=VERTEX_POINT ( 'NONE', #57326 ) ;
#43501=CARTESIAN_POINT ( 'NONE',  ( 1.400734872026642375, 15.45478884909084272, 9.907647895771706459 ) ) ;
#43511=CARTESIAN_POINT ( 'NONE',  ( 4.898587196589412829E-16, -15.12499999999999289, -8.000000000000000000 ) ) ;
#43545=ORIENTED_EDGE ( 'NONE', *, *, #10358, .T. ) ;
#43546=CYLINDRICAL_SURFACE ( 'NONE', #37769, 4.000000000000000000 ) ;
#43548=CYLINDRICAL_SURFACE ( 'NONE', #4189, 4.000000000000001776 ) ;
#43563=CARTESIAN_POINT ( 'NONE',  ( -9.483056940782027766, 107.4438779010658038, -3.177305548492606047 ) ) ;
#43571=ORIENTED_EDGE ( 'NONE', *, *, #10371, .T. ) ;
#43583=STYLED_ITEM ( 'NONE', ( #54260 ), #83666 ) ;
#43616=AXIS2_PLACEMENT_3D ( 'NONE', #94241, #2018, #34966 ) ;
#43630=CARTESIAN_POINT ( 'NONE',  ( 8.000000000000000000, -29.09375000409677270, -3.313708498984761164 ) ) ;
#43638=EDGE_CURVE ( 'NONE', #82728, #71070, #43813, .T. ) ;
#43650=CARTESIAN_POINT ( 'NONE',  ( 3.313708498984762052, -27.21874999999999645, -8.000000000000000000 ) ) ;
#43670=CARTESIAN_POINT ( 'NONE',  ( 7.934203308536662114, 108.8670034001779783, 1.057099537198549655 ) ) ;
#43698=CARTESIAN_POINT ( 'NONE',  ( 9.797174393178825657E-16, -30.00000000000000000, -8.000000000000000000 ) ) ;
#43730=CARTESIAN_POINT ( 'NONE',  ( -2.977408999572650039, -10.06250000204838457, -7.188101187500000933 ) ) ;
#43739=CARTESIAN_POINT ( 'NONE',  ( -5.082755093536325042, -15.96875000204838635, -5.082755093536325930 ) ) ;
#43756=FACE_OUTER_BOUND ( 'NONE', #20028, .T. ) ;
#43780=CARTESIAN_POINT ( 'NONE',  ( 7.188101187499999156, -19.62500000204838457, 2.977408999572654924 ) ) ;
#43803=CARTESIAN_POINT ( 'NONE',  ( -7.188101187500000044, -22.90625000204838457, -8.802885111219163269E-16 ) ) ;
#43813=LINE ( 'NONE', #92352, #87482 ) ;
#43822=CARTESIAN_POINT ( 'NONE',  ( 9.918579450955565591, 101.2069608703131252, 1.297207292923863164 ) ) ;
#43857=CARTESIAN_POINT ( 'NONE',  ( 2.977408999572650927, -28.25000000204838813, -7.188101187500000933 ) ) ;
#43866=CARTESIAN_POINT ( 'NONE',  ( -2.977408999572650039, -11.18750000204838457, -7.188101187500001821 ) ) ;
#43883=CARTESIAN_POINT ( 'NONE',  ( -1.469576158976823947E-15, -23.56250000409677270, 8.000000000000000000 ) ) ;
#43925=CARTESIAN_POINT ( 'NONE',  ( -7.188101187500000933, -27.50000000204838457, -2.977408999572651371 ) ) ;
#43931=( LENGTH_UNIT ( ) NAMED_UNIT ( * ) SI_UNIT ( .MILLI., .METRE. ) );
#43937=CARTESIAN_POINT ( 'NONE',  ( -3.313708498984760720, -16.71875000409677270, -8.000000000000000000 ) ) ;
#43978=CARTESIAN_POINT ( 'NONE',  ( -1.469576158976823947E-15, -29.37499999999999645, 8.000000000000000000 ) ) ;
#43999=CARTESIAN_POINT ( 'NONE',  ( -2.977408999572650039, -30.68750000204839168, -7.188101187500001821 ) ) ;
#44006=CARTESIAN_POINT ( 'NONE',  ( -3.313708498984760276, -18.03124999999999645, -8.000000000000000000 ) ) ;
#44075=CARTESIAN_POINT ( 'NONE',  ( 9.907626560209529032, 15.45483377860037244, 1.400881274228120477 ) ) ;
#44077=CARTESIAN_POINT ( 'NONE',  ( 0.000000000000000000, -30.00000000000000000, 8.000000000000000000 ) ) ;
#44087=B_SPLINE_CURVE_WITH_KNOTS ( 'NONE', 3,
 ( #46814, #79711, #102934, #29100, #71091, #105577, #8476, #50000, #82369, #9003, #16037, #91016, #106637, #16576, #48918, #41380, #7403, #32786, #74271, #48396, #65660, #40316, #40843, #73737, #74795, #32243, #81812, #98542, #33314, #24693, #83431, #57541, #65123, #66186 ),
 .UNSPECIFIED., .F., .F.,
 ( 4, 2, 2, 2, 2, 2, 2, 2, 2, 2, 2, 2, 2, 2, 2, 2, 4 ),
 ( 0.01263889472610568374, 0.01342810546992895954, 0.01421731621375223534, 0.01500652695757551114, 0.01579573770139878694, 0.01658494844522206274, 0.01737415918904533854, 0.01816336993286861434, 0.01895258067669189361, 0.01974179142051516594, 0.02053100216433844522, 0.02132021290816171755, 0.02210942365198499682, 0.02289863439580827262, 0.02368784513963154842, 0.02447705588345482769, 0.02526626662727810002 ),
 .UNSPECIFIED. ) ;
#44102=CARTESIAN_POINT ( 'NONE',  ( -9.798380800342661345, 108.4680065431550275, -2.010350564680323249 ) ) ;
#44194=CARTESIAN_POINT ( 'NONE',  ( 4.898587196589412829E-16, -18.12499999999999645, -8.000000000000000000 ) ) ;
#44244=CARTESIAN_POINT ( 'NONE',  ( -8.000000000000001776, -11.65624999999999289, 3.313708498984759387 ) ) ;
#44264=CARTESIAN_POINT ( 'NONE',  ( -9.381394091586566120, 102.9865039441838519, 3.465950112474256883 ) ) ;
#44281=CARTESIAN_POINT ( 'NONE',  ( 2.977408999572651815, -13.81250000204838280, 7.188101187500000933 ) ) ;
#44292=CARTESIAN_POINT ( 'NONE',  ( 5.656854249492378806, -14.18749999999999112, 5.656854249492381470 ) ) ;
#44318=CARTESIAN_POINT ( 'NONE',  ( 9.165151389911679658, 30.00000000000000000, 4.000000000000000000 ) ) ;
#44319=CARTESIAN_POINT ( 'NONE',  ( -5.082755093536326818, -11.09375000204838457, 5.082755093536325042 ) ) ;
#44322=CARTESIAN_POINT ( 'NONE',  ( -3.313708498984803352, -11.65625000409677270, 7.999999999999960032 ) ) ;
#44334=CARTESIAN_POINT ( 'NONE',  ( 3.313708498984781592, -29.28124999999999645, 7.999999999999979572 ) ) ;
#44346=CARTESIAN_POINT ( 'NONE',  ( 2.977408999572651815, -25.43750000204838813, 7.188101187500000933 ) ) ;
#44397=VERTEX_POINT ( 'NONE', #398 ) ;
#44399=CARTESIAN_POINT ( 'NONE',  ( -7.188101187500002709, -23.18750000204838813, 2.977408999572647819 ) ) ;
#44409=CARTESIAN_POINT ( 'NONE',  ( 2.977408999572650927, -29.75000000204838813, -7.188101187500001821 ) ) ;
#44428=FACE_OUTER_BOUND ( 'NONE', #38760, .T. ) ;
#44465=CARTESIAN_POINT ( 'NONE',  ( -7.188101187500002709, -18.31250000204838457, 2.977408999572647819 ) ) ;
#44470=CARTESIAN_POINT ( 'NONE',  ( 0.000000000000000000, -30.00000000000000000, 0.000000000000000000 ) ) ;
#44471=AXIS2_PLACEMENT_3D ( 'NONE', #22762, #54539, #39982 ) ;
#44478=CARTESIAN_POINT ( 'NONE',  ( -8.000000000000000000, -17.93750000409676915, -9.797174393178825657E-16 ) ) ;
#44541=CARTESIAN_POINT ( 'NONE',  ( 2.977408999572651815, -23.93750000204838457, 7.188101187500000933 ) ) ;
#44545=CARTESIAN_POINT ( 'NONE',  ( 2.918503601030405736, 15.30040232763797903, 9.571198553003400278 ) ) ;
#44552=CYLINDRICAL_SURFACE ( 'NONE', #80479, 4.000000000000000000 ) ;
#44561=UNCERTAINTY_MEASURE_WITH_UNIT (LENGTH_MEASURE( 1.000000000000000082E-05 ), #7305, 'distance_accuracy_value', 'NONE');
#44595=CARTESIAN_POINT ( 'NONE',  ( 4.898587196589412829E-16, -10.81250000409677092, -8.000000000000000000 ) ) ;
#44600=ORIENTED_EDGE ( 'NONE', *, *, #27926, .T. ) ;
#44646=CARTESIAN_POINT ( 'NONE',  ( -9.948513602187995630, 108.8697794334385804, 1.045942665286139217 ) ) ;
#44667=VERTEX_POINT ( 'NONE', #25429 ) ;
#44670=DIRECTION ( 'NONE',  ( -0.000000000000000000, 1.000000000000000000, -0.000000000000000000 ) ) ;
#44687=ORIENTED_EDGE ( 'NONE', *, *, #80384, .F. ) ;
#44734=CARTESIAN_POINT ( 'NONE',  ( 3.313708498984762496, -23.28124999999999645, 7.999999999999998224 ) ) ;
#44760=CARTESIAN_POINT ( 'NONE',  ( -5.082755093536325042, -9.593750002048384573, -5.082755093536325930 ) ) ;
#44785=CARTESIAN_POINT ( 'NONE',  ( -8.000000000000001776, -25.15624999999999289, 3.313708498984759387 ) ) ;
#44800=EDGE_CURVE ( 'NONE', #40836, #99482, #36190, .T. ) ;
#44801=SURFACE_STYLE_FILL_AREA ( #11873 ) ;
#44805=CARTESIAN_POINT ( 'NONE',  ( -9.843481099141461854, 101.4079544384661347, -1.779148000612192915 ) ) ;
#44819=CARTESIAN_POINT ( 'NONE',  ( 4.898587196589412829E-16, -18.31250000409676915, -8.000000000000000000 ) ) ;
#44824=CARTESIAN_POINT ( 'NONE',  ( -7.188101187500002709, -17.18750000204838813, 2.977408999572648707 ) ) ;
#44863=CARTESIAN_POINT ( 'NONE',  ( -1.320432766682874540E-15, -12.40625000204838635, 7.188101187500000044 ) ) ;
#44873=CARTESIAN_POINT ( 'NONE',  ( 9.221346651730840449, 86.04834020068338418, -3.869102247876031520 ) ) ;
#44874=EDGE_CURVE ( 'NONE', #53794, #61442, #75699, .T. ) ;
#44890=CARTESIAN_POINT ( 'NONE',  ( 4.582575694955839829, 15.00000000000000000, 10.00000000000000000 ) ) ;
#44894=CARTESIAN_POINT ( 'NONE',  ( -7.188101187500000044, -25.90625000204838813, -8.802885111219163269E-16 ) ) ;
#44895=CARTESIAN_POINT ( 'NONE',  ( 4.898587196589412829E-16, -28.62499999999999289, -8.000000000000000000 ) ) ;
#44906=CARTESIAN_POINT ( 'NONE',  ( 8.000000000000000000, -21.59375000409677625, -3.313708498984761164 ) ) ;
#44911=CARTESIAN_POINT ( 'NONE',  ( 9.948561005166130400, 101.1300972625180066, -1.045755304005130837 ) ) ;
#44943=EDGE_LOOP ( 'NONE', ( #6564, #70588 ) ) ;
#44945=CARTESIAN_POINT ( 'NONE',  ( 5.082755093536324154, -24.21875000204838813, 5.082755093536326818 ) ) ;
#44948=VERTEX_POINT ( 'NONE', #69586 ) ;
#44954=CARTESIAN_POINT ( 'NONE',  ( 5.082755093536325930, -31.34375000204838457, -5.082755093536325042 ) ) ;
#44959=CARTESIAN_POINT ( 'NONE',  ( -7.618844049274130725, 108.1723589892945938, 2.450177051822847840 ) ) ;
#44988=EDGE_CURVE ( 'NONE', #96386, #24908, #86760, .T. ) ;
#44994=CARTESIAN_POINT ( 'NONE',  ( -5.082755093536325042, -32.46875000204838813, -5.082755093536325930 ) ) ;
#45009=CARTESIAN_POINT ( 'NONE',  ( -7.188101187500000044, -16.90625000204838813, -8.802885111219163269E-16 ) ) ;
#45018=CARTESIAN_POINT ( 'NONE',  ( -9.918325909156568088, 81.20764768292566771, 1.298699613733151237 ) ) ;
#45021=CARTESIAN_POINT ( 'NONE',  ( -8.000000000000001776, -20.84375000409677270, 3.313708498984758943 ) ) ;
#45036=ORIENTED_EDGE ( 'NONE', *, *, #13889, .T. ) ;
#45053=FACE_OUTER_BOUND ( 'NONE', #47490, .T. ) ;
#45080=CARTESIAN_POINT ( 'NONE',  ( 2.977408999572650927, -26.37500000204838457, -7.188101187500001821 ) ) ;
#45083=DIRECTION ( 'NONE',  ( -1.000000000000000000, 0.000000000000000000, 1.734723475976807094E-16 ) ) ;
#45098=VERTEX_POINT ( 'NONE', #106703 ) ;
#45111=CARTESIAN_POINT ( 'NONE',  ( 0.7016502453916999560, 15.23274035658503145, 9.981544566921638051 ) ) ;
#45143=B_SPLINE_CURVE_WITH_KNOTS ( 'NONE', 3,
 ( #41432, #66236, #25839, #83481, #50049, #99121, #927, #67322, #40905, #98598, #1487, #25286, #59232, #32838, #92105, #58143, #57594, #9054, #75928, #82959, #90516, #49518, #99669, #91071, #57072, #33912, #42495, #34452, #66781, #24223, #58695, #17706, #18248, #100202 ),
 .UNSPECIFIED., .F., .F.,
 ( 4, 2, 2, 2, 2, 2, 2, 2, 2, 2, 2, 2, 2, 2, 2, 2, 4 ),
 ( 0.01272238763756221129, 0.01351613129786392864, 0.01430987495816564599, 0.01510361861846736334, 0.01589736227876908242, 0.01669110593907079804, 0.01748484959937251712, 0.01827859325967423620, 0.01907233691997595182, 0.01986608058027767090, 0.02065982424057938999, 0.02145356790088110560, 0.02224731156118282122, 0.02304105522148454030, 0.02383479888178625938, 0.02462854254208797500, 0.02542228620238969408 ),
 .UNSPECIFIED. ) ;
#45172=FACE_BOUND ( 'NONE', #53081, .T. ) ;
#45178=CARTESIAN_POINT ( 'NONE',  ( -9.380871178326117388, 107.0111637979832580, 3.467392232194204116 ) ) ;
#45264=CARTESIAN_POINT ( 'NONE',  ( -1.469576158976823947E-15, -20.37499999999999289, 8.000000000000000000 ) ) ;
#45267=EDGE_CURVE ( 'NONE', #99488, #49442, #39445, .T. ) ;
#45314=CARTESIAN_POINT ( 'NONE',  ( -9.333555687487613994, 28.21897303391028800, 3.591168747312690979 ) ) ;
#45328=B_SPLINE_CURVE_WITH_KNOTS ( 'NONE', 3,
 ( #5083, #104290, #87075, #105367, #30440, #15288, #89186, #22358, #88130, #96229, #13148, #14212, #104839, #63861, #46077, #29908, #22883, #88650, #38015, #70876, #82135, #33097, #17428, #57853, #15819, #81587, #48699, #74575, #83205, #99369, #98843, #105881, #56795, #75095 ),
 .UNSPECIFIED., .F., .F.,
 ( 4, 2, 2, 2, 2, 2, 2, 2, 2, 2, 2, 2, 2, 2, 2, 2, 4 ),
 ( 0.000000000000000000, 0.0007899309203816213881, 0.001579861840763242776, 0.002369792761144844974, 0.003159723681526447822, 0.003949654601908049803, 0.004739585522289651784, 0.005529516442671255499, 0.006319447363052857480, 0.007109378283434458594, 0.007899309203816059707, 0.008689240124197661688, 0.009479171044579263669, 0.01026910196496086738, 0.01105903288534246763, 0.01184896380572406961, 0.01263889472610566986 ),
 .UNSPECIFIED. ) ;
#45334=CARTESIAN_POINT ( 'NONE',  ( -9.646032546913144046, 101.9871967152563172, 2.644051433538248119 ) ) ;
#45336=CARTESIAN_POINT ( 'NONE',  ( 4.397168787612283580, 15.00000000000000000, -9.999999999999998224 ) ) ;
#45351=CARTESIAN_POINT ( 'NONE',  ( -5.082755093536326818, -14.09375000204838457, 5.082755093536325042 ) ) ;
#45362=CARTESIAN_POINT ( 'NONE',  ( 8.000000000000000000, -13.99999999999999112, 0.000000000000000000 ) ) ;
#45391=CARTESIAN_POINT ( 'NONE',  ( -7.188101187500001821, -12.87500000204838813, -2.977408999572651371 ) ) ;
#45401=CARTESIAN_POINT ( 'NONE',  ( 9.165151389911681434, 85.00000000000001421, -4.000000000000000000 ) ) ;
#45421=CARTESIAN_POINT ( 'NONE',  ( -7.188101187500001821, -27.50000000204838813, -2.977408999572651371 ) ) ;
#45470=EDGE_CURVE ( 'NONE', #62602, #32259, #21573, .T. ) ;
#45471=CARTESIAN_POINT ( 'NONE',  ( 2.977408999572650927, -19.25000000204838457, -7.188101187500000933 ) ) ;
#45481=CARTESIAN_POINT ( 'NONE',  ( -7.188101187500002709, -9.312500002048384573, 2.977408999572648707 ) ) ;
#45515=ORIENTED_EDGE ( 'NONE', *, *, #44874, .F. ) ;
#45524=CARTESIAN_POINT ( 'NONE',  ( -2.977408999572650039, -31.06250000204838813, -7.188101187500001821 ) ) ;
#45529=ORIENTED_EDGE ( 'NONE', *, *, #69423, .F. ) ;
#45538=CARTESIAN_POINT ( 'NONE',  ( 5.082755093536324154, -19.34375000204838457, 5.082755093536326818 ) ) ;
#45543=CARTESIAN_POINT ( 'NONE',  ( -9.843481099141461854, 81.40795443846614887, -1.779148000612192915 ) ) ;
#45546=CARTESIAN_POINT ( 'NONE',  ( 4.898587196589412829E-16, -15.31250000409677092, -8.000000000000000000 ) ) ;
#45548=SURFACE_SIDE_STYLE ('',( #5598 ) ) ;
#45579=DIRECTION ( 'NONE',  ( -0.000000000000000000, 1.000000000000000000, -0.000000000000000000 ) ) ;
#45608=CARTESIAN_POINT ( 'NONE',  ( 2.977408999572650927, -27.87500000204838457, -7.188101187500001821 ) ) ;
#45627=CYLINDRICAL_SURFACE ( 'NONE', #93166, 8.000000000000000000 ) ;
#45637=VERTEX_POINT ( 'NONE', #1371 ) ;
#45648=ADVANCED_FACE ( 'NONE', ( #8948 ), #1913, .T. ) ;
#45650=CARTESIAN_POINT ( 'NONE',  ( -0.7016502453916991788, 15.23274035658503145, -9.981544566921638051 ) ) ;
#45659=CARTESIAN_POINT ( 'NONE',  ( -10.00000000000000355, 0.000000000000000000, -10.00000000000000000 ) ) ;
#45698=ORIENTED_EDGE ( 'NONE', *, *, #39704, .F. ) ;
#45710=COLOUR_RGB ( '', 0.40784314, 0.44705882, 0.49803922) ;
#45711=EDGE_LOOP ( 'NONE', ( #57276, #75933, #30122, #63553 ) ) ;
#45774=CARTESIAN_POINT ( 'NONE',  ( -8.000000000000000000, -10.43750000409677092, -9.797174393178825657E-16 ) ) ;
#45782=CARTESIAN_POINT ( 'NONE',  ( -5.656854249492381470, -19.06249999999999289, 5.656854249492379694 ) ) ;
#45801=AXIS2_PLACEMENT_3D ( 'NONE', #31696, #97453, #32220 ) ;
#45805=ADVANCED_FACE ( 'NONE', ( #4597 ), #62838, .T. ) ;
#45808=EDGE_CURVE ( 'NONE', #90586, #53794, #54177, .T. ) ;
#45813=CARTESIAN_POINT ( 'NONE',  ( 9.090909090909086387, 15.00000000000000000, -4.165977904505313134 ) ) ;
#45837=CARTESIAN_POINT ( 'NONE',  ( -9.537927238823508347, 27.35373142881821096, -3.010735687602430488 ) ) ;
#45838=CARTESIAN_POINT ( 'NONE',  ( -5.656854249492381470, -26.56249999999999645, 5.656854249492379694 ) ) ;
#45853=CARTESIAN_POINT ( 'NONE',  ( -9.381593208289373820, 102.9856136188049334, -3.465401811657803588 ) ) ;
#45868=CARTESIAN_POINT ( 'NONE',  ( -7.188101187500002709, -12.68750000204838635, 2.977408999572648707 ) ) ;
#45888=VECTOR ( 'NONE', #28013, 1000.000000000000000 ) ;
#45908=CARTESIAN_POINT ( 'NONE',  ( -7.986711519608433285, 26.02638096376566068, -0.5300249774147565152 ) ) ;
#45914=CARTESIAN_POINT ( 'NONE',  ( -5.082755093536326818, -12.59375000204838635, 5.082755093536325042 ) ) ;
#45928=CARTESIAN_POINT ( 'NONE',  ( 5.656854249492380582, -28.81249999999999289, -5.656854249492379694 ) ) ;
#45938=CARTESIAN_POINT ( 'NONE',  ( 0.000000000000000000, 0.000000000000000000, 0.000000000000000000 ) ) ;
#45940=CARTESIAN_POINT ( 'NONE',  ( -1.320432766682874540E-15, -21.03125000204838457, 7.188101187500000044 ) ) ;
#45992=CARTESIAN_POINT ( 'NONE',  ( -10.00000000000000355, 85.00000000000000000, 4.000000000000000000 ) ) ;
#45993=CARTESIAN_POINT ( 'NONE',  ( 5.082755093536324154, -21.21875000204838813, 5.082755093536326818 ) ) ;
#46003=CARTESIAN_POINT ( 'NONE',  ( 2.977408999572650927, -34.25000000204838813, -7.188101187500001821 ) ) ;
#46038=EDGE_LOOP ( 'NONE', ( #89998, #81554 ) ) ;
#46043=CARTESIAN_POINT ( 'NONE',  ( 5.082755093536325930, -29.84375000204838813, -5.082755093536325042 ) ) ;
#46058=CARTESIAN_POINT ( 'NONE',  ( 4.401442555609581635E-16, -20.28125000204838813, -7.188101187500000044 ) ) ;
#46069=CARTESIAN_POINT ( 'NONE',  ( 7.999999999999998224, -14.28125000409677092, 3.313708498984766493 ) ) ;
#46071=CARTESIAN_POINT ( 'NONE',  ( 9.373884331925060209, 15.95332971149351842, 3.487646406148156242 ) ) ;
#46077=CARTESIAN_POINT ( 'NONE',  ( -9.948561005166130400, 33.86990273748199343, -1.045755304005141273 ) ) ;
#46132=CARTESIAN_POINT ( 'NONE',  ( -7.188101187500000044, -27.40625000204838813, -8.802885111219163269E-16 ) ) ;
#46134=CARTESIAN_POINT ( 'NONE',  ( 4.898587196589412829E-16, -19.81250000409677270, -8.000000000000000000 ) ) ;
#46150=UNCERTAINTY_MEASURE_WITH_UNIT (LENGTH_MEASURE( 1.000000000000000082E-05 ), #17074, 'distance_accuracy_value', 'NONE');
#46189=ORIENTED_EDGE ( 'NONE', *, *, #10896, .F. ) ;
#46197=CARTESIAN_POINT ( 'NONE',  ( 4.898587196589412829E-16, -33.31250000409677625, -8.000000000000000000 ) ) ;
#46219=CARTESIAN_POINT ( 'NONE',  ( -10.00000000000000000, 15.00000000000000000, 2.701558353794764056 ) ) ;
#46251=CARTESIAN_POINT ( 'NONE',  ( 8.000000000000000000, -14.09375000409676915, -3.313708498984761164 ) ) ;
#46284=ORIENTED_EDGE ( 'NONE', *, *, #93988, .T. ) ;
#46314=CARTESIAN_POINT ( 'NONE',  ( 5.656854249492378806, -18.68749999999999289, 5.656854249492381470 ) ) ;
#46322=CIRCLE ( 'NONE', #29130, 8.000000000000000000 ) ;
#46336=VECTOR ( 'NONE', #902, 1000.000000000000000 ) ;
#46341=FILL_AREA_STYLE_COLOUR ( '', #73302 ) ;
#46364=CARTESIAN_POINT ( 'NONE',  ( -9.221216839714866609, 28.95240251831025446, 3.869414262756994294 ) ) ;
#46378=CARTESIAN_POINT ( 'NONE',  ( -10.00000000000000000, 15.00000000000000000, -1.544939622599426743 ) ) ;
#46410=CARTESIAN_POINT ( 'NONE',  ( 3.313708498984722972, -24.21874999999998934, -8.000000000000040856 ) ) ;
#46427=CARTESIAN_POINT ( 'NONE',  ( 3.313708498984762496, -17.46875000409676915, 7.999999999999998224 ) ) ;
#46433=CARTESIAN_POINT ( 'NONE',  ( 7.934203308536660337, 33.86700340017797117, 1.057099537198553652 ) ) ;
#46441=CARTESIAN_POINT ( 'NONE',  ( 2.977408999572650927, -13.25000000204838280, -7.188101187500001821 ) ) ;
#46468=CARTESIAN_POINT ( 'NONE',  ( 2.977408999572650927, -20.37500000204838457, -7.188101187500001821 ) ) ;
#46496=CARTESIAN_POINT ( 'NONE',  ( -6.928203230275510549, 85.00000000000000000, -4.000000000000000000 ) ) ;
#46511=CARTESIAN_POINT ( 'NONE',  ( 2.977408999572652260, -16.81250000204838813, 7.188101187500000044 ) ) ;
#46521=CARTESIAN_POINT ( 'NONE',  ( 5.082755093536325930, -34.34375000204838813, -5.082755093536325042 ) ) ;
#46528=CARTESIAN_POINT ( 'NONE',  ( -7.212408192734267587, 107.0151708932036883, -3.465038817813882233 ) ) ;
#46563=CARTESIAN_POINT ( 'NONE',  ( -5.082755093536326818, -30.59375000204838813, 5.082755093536325042 ) ) ;
#46576=CARTESIAN_POINT ( 'NONE',  ( -1.320432766682874540E-15, -18.03125000204838457, 7.188101187500000044 ) ) ;
#46586=CARTESIAN_POINT ( 'NONE',  ( 3.313708498984762052, -9.406250004096769146, -8.000000000000000000 ) ) ;
#46589=CARTESIAN_POINT ( 'NONE',  ( 10.00000000000003730, 14.99999999999998934, 4.210530276628143831 ) ) ;
#46616=CARTESIAN_POINT ( 'NONE',  ( -9.165151389911681434, 30.00000000000000000, -4.000000000000000000 ) ) ;
#46646=CARTESIAN_POINT ( 'NONE',  ( 7.188101187500000044, -25.15625000204838813, 0.000000000000000000 ) ) ;
#46647=CARTESIAN_POINT ( 'NONE',  ( 3.313708498984800688, -20.46875000409677270, 7.999999999999960032 ) ) ;
#46666=CARTESIAN_POINT ( 'NONE',  ( -4.582575694955840717, 16.00000000000000000, -10.00000000000000000 ) ) ;
#46675=CIRCLE ( 'NONE', #129, 8.000000000000000000 ) ;
#46716=CARTESIAN_POINT ( 'NONE',  ( -8.000000000000000000, -31.43750000409677270, -9.797174393178825657E-16 ) ) ;
#46739=CARTESIAN_POINT ( 'NONE',  ( -9.999999999999998224, 15.00000000000000000, 1.836970198721029589E-15 ) ) ;
#46773=CARTESIAN_POINT ( 'NONE',  ( -1.469576158976823947E-15, -13.06250000409676915, 8.000000000000000000 ) ) ;
#46791=FACE_OUTER_BOUND ( 'NONE', #71310, .T. ) ;
#46814=CARTESIAN_POINT ( 'NONE',  ( 9.165151389911679658, 105.0000000000000000, 4.000000000000001776 ) ) ;
#46827=CARTESIAN_POINT ( 'NONE',  ( 4.898587196589412829E-16, -10.81250000409677092, -8.000000000000000000 ) ) ;
#46835=CARTESIAN_POINT ( 'NONE',  ( 8.000000000000000000, -16.99999999999999289, 0.000000000000000000 ) ) ;
#46857=EDGE_CURVE ( 'NONE', #61442, #82593, #90836, .T. ) ;
#46878=CARTESIAN_POINT ( 'NONE',  ( -9.482945380845299255, 27.55666941221070232, 3.177595346755240691 ) ) ;
#46947=CARTESIAN_POINT ( 'NONE',  ( 7.801777176595948937, 33.58827985812632733, -1.786991866639921822 ) ) ;
#46955=CARTESIAN_POINT ( 'NONE',  ( 4.898587196589412829E-16, -30.12499999999999645, -8.000000000000000000 ) ) ;
#46982=CARTESIAN_POINT ( 'NONE',  ( -7.188101187500001821, -21.50000000204839168, -2.977408999572651371 ) ) ;
#46990=AXIS2_PLACEMENT_3D ( 'NONE', #90866, #74654, #50909 ) ;
#47027=CARTESIAN_POINT ( 'NONE',  ( 2.977408999572650927, -20.75000000204839523, -7.188101187500000933 ) ) ;
#47033=VERTEX_POINT ( 'NONE', #74903 ) ;
#47034=FACE_OUTER_BOUND ( 'NONE', #33930, .T. ) ;
#47039=CARTESIAN_POINT ( 'NONE',  ( 5.082755093536325930, -28.34375000204838813, -5.082755093536325042 ) ) ;
#47046=DIRECTION ( 'NONE',  ( -0.000000000000000000, 1.000000000000000000, -0.000000000000000000 ) ) ;
#47080=CARTESIAN_POINT ( 'NONE',  ( -5.082755093536325042, -26.46875000204838813, -5.082755093536325930 ) ) ;
#47094=CARTESIAN_POINT ( 'NONE',  ( 7.188101187500000044, -11.65625000204838635, 0.000000000000000000 ) ) ;
#47102=CARTESIAN_POINT ( 'NONE',  ( -9.842984802582135373, 81.40930409524348477, 1.781981959250507952 ) ) ;
#47105=CARTESIAN_POINT ( 'NONE',  ( -8.000000000000000000, -9.031250004096769146, -3.313708498984762496 ) ) ;
#47107=CARTESIAN_POINT ( 'NONE',  ( 9.090909090909084611, 14.99999999999999645, 4.165977904505316687 ) ) ;
#47111=CARTESIAN_POINT ( 'NONE',  ( -9.165151389911684987, 85.26735155607116212, -4.000000000000000000 ) ) ;
#47112=( NAMED_UNIT ( * ) SI_UNIT ( $, .STERADIAN. ) SOLID_ANGLE_UNIT ( ) );
#47130=CARTESIAN_POINT ( 'NONE',  ( -9.165151389911681434, 84.99999999999998579, -4.000000000000000000 ) ) ;
#47168=CARTESIAN_POINT ( 'NONE',  ( 7.188101187499999156, -20.75000000204839523, 2.977408999572654924 ) ) ;
#47207=CARTESIAN_POINT ( 'NONE',  ( -8.000000000000000000, -16.43750000409677270, -9.797174393178825657E-16 ) ) ;
#47235=CARTESIAN_POINT ( 'NONE',  ( -1.469576158976823947E-15, -31.06250000409677270, 8.000000000000000000 ) ) ;
#47242=CARTESIAN_POINT ( 'NONE',  ( -4.165977904505308693, 15.00000000000000000, -9.090909090909091717 ) ) ;
#47245=CARTESIAN_POINT ( 'NONE',  ( -8.000000000000000000, -10.34374999999999112, -3.313708498984762496 ) ) ;
#47257=CARTESIAN_POINT ( 'NONE',  ( -10.00000000000000000, 15.00000000000000000, 3.648665620917489250 ) ) ;
#47280=CARTESIAN_POINT ( 'NONE',  ( -2.440247554416620890, -29.99999999999999289, 6.972723154969403758 ) ) ;
#47292=CARTESIAN_POINT ( 'NONE',  ( 7.999999999999998224, -12.78125000409676915, 3.313708498984766049 ) ) ;
#47362=UNCERTAINTY_MEASURE_WITH_UNIT (LENGTH_MEASURE( 1.000000000000000082E-05 ), #81869, 'distance_accuracy_value', 'NONE');
#47364=CARTESIAN_POINT ( 'NONE',  ( 7.999999999999998224, -15.59374999999999289, 3.313708498984766493 ) ) ;
#47385=CARTESIAN_POINT ( 'NONE',  ( 9.999999999999957367, 15.00000000000001066, -3.836411046841929018 ) ) ;
#47421=CARTESIAN_POINT ( 'NONE',  ( -9.999999999999998224, 15.00000000000000000, 1.785846837348918736E-15 ) ) ;
#47475=CARTESIAN_POINT ( 'NONE',  ( 7.744329845603316720, 33.46288230153454890, -2.018701143083232008 ) ) ;
#47476=CARTESIAN_POINT ( 'NONE',  ( -7.151597709147948123, 28.21070734947783976, 3.587174531012139678 ) ) ;
#47483=CARTESIAN_POINT ( 'NONE',  ( 7.999999999999998224, -33.59374999999999289, 3.313708498984766493 ) ) ;
#47490=EDGE_LOOP ( 'NONE', ( #5801, #76547, #7799, #46189 ) ) ;
#47499=LINE ( 'NONE', #81773, #77933 ) ;
#47512=CARTESIAN_POINT ( 'NONE',  ( -5.082755093536325042, -17.09375000204838813, -5.082755093536325930 ) ) ;
#47518=EDGE_CURVE ( 'NONE', #14808, #57343, #15498, .T. ) ;
#47520=CIRCLE ( 'NONE', #42367, 1.000000000000000888 ) ;
#47535=DIRECTION ( 'NONE',  ( 0.4165977904505306917, 0.000000000000000000, -0.9090909090909092827 ) ) ;
#47560=CARTESIAN_POINT ( 'NONE',  ( -5.082755093536326818, -18.59375000204838457, 5.082755093536325042 ) ) ;
#47570=CARTESIAN_POINT ( 'NONE',  ( -5.082755093536326818, -29.09375000204838813, 5.082755093536325042 ) ) ;
#47594=EDGE_CURVE ( 'NONE', #71772, #37759, #8339, .T. ) ;
#47609=CARTESIAN_POINT ( 'NONE',  ( -7.188101187500001821, -24.87500000204838457, -2.977408999572651371 ) ) ;
#47620=CARTESIAN_POINT ( 'NONE',  ( -7.188101187500002709, -12.31250000204838635, 2.977408999572647819 ) ) ;
#47621=CARTESIAN_POINT ( 'NONE',  ( 6.928203230275510549, 30.00000000000000355, -4.000000000000000000 ) ) ;
#47633=CARTESIAN_POINT ( 'NONE',  ( -1.469576158976823947E-15, -10.06250000409677092, 8.000000000000000000 ) ) ;
#47636=CARTESIAN_POINT ( 'NONE',  ( 9.999999999997889688, 15.11700796859310714, 0.7408669144238181348 ) ) ;
#47655=CARTESIAN_POINT ( 'NONE',  ( 8.000000000000000000, -9.687500004096769146, 0.000000000000000000 ) ) ;
#47696=CARTESIAN_POINT ( 'NONE',  ( 2.977408999572651815, -20.93750000204838457, 7.188101187500000933 ) ) ;
#47698=CARTESIAN_POINT ( 'NONE',  ( 9.948513602187992078, 81.13022056656140535, 1.045942665286136108 ) ) ;
#47706=DIRECTION ( 'NONE',  ( -0.000000000000000000, 1.000000000000000000, -0.000000000000000000 ) ) ;
#47745=AXIS2_PLACEMENT_3D ( 'NONE', #96012, #63110, #21617 ) ;
#47757=CARTESIAN_POINT ( 'NONE',  ( 4.898587196589412829E-16, -30.31250000409677270, -8.000000000000000000 ) ) ;
#47762=CARTESIAN_POINT ( 'NONE',  ( 9.989113211954165905, 33.97299273548994591, 0.5334031035449001701 ) ) ;
#47764=( NAMED_UNIT ( * ) PLANE_ANGLE_UNIT ( ) SI_UNIT ( $, .RADIAN. ) );
#47770=VECTOR ( 'NONE', #63901, 1000.000000000000000 ) ;
#47841=ORIENTED_EDGE ( 'NONE', *, *, #97861, .F. ) ;
#47878=DIRECTION ( 'NONE',  ( 1.000000000000000000, 0.000000000000000000, 0.000000000000000000 ) ) ;
#47882=CARTESIAN_POINT ( 'NONE',  ( 5.656854249492380582, -13.81249999999999112, -5.656854249492379694 ) ) ;
#47905=ORIENTED_EDGE ( 'NONE', *, *, #93960, .F. ) ;
#47944=CARTESIAN_POINT ( 'NONE',  ( -9.999999999999998224, 15.23416508905776112, -0.7060372491550682694 ) ) ;
#48008=CARTESIAN_POINT ( 'NONE',  ( 4.401442555609581635E-16, -10.15625000204838457, -7.188101187500000044 ) ) ;
#48034=CARTESIAN_POINT ( 'NONE',  ( 5.082755093536324154, -17.84375000204838457, 5.082755093536326818 ) ) ;
#48064=VECTOR ( 'NONE', #67577, 1000.000000000000000 ) ;
#48086=CARTESIAN_POINT ( 'NONE',  ( 7.188101187500000044, -12.03125000204838635, 0.000000000000000000 ) ) ;
#48089=CARTESIAN_POINT ( 'NONE',  ( 7.144701066121058375, -30.00000000000003553, 0.9176209997231349336 ) ) ;
#48095=CARTESIAN_POINT ( 'NONE',  ( -2.977408999572654480, -27.50000000204838813, 7.188101187499999156 ) ) ;
#48100=CARTESIAN_POINT ( 'NONE',  ( -6.928203230275508773, 105.0000000000000000, 4.000000000000001776 ) ) ;
#48101=CARTESIAN_POINT ( 'NONE',  ( 0.000000000000000000, -30.00000000000000000, 0.000000000000000000 ) ) ;
#48120=PLANE ( 'NONE',  #60101 ) ;
#48139=CARTESIAN_POINT ( 'NONE',  ( -7.188101187500001821, -26.37500000204838457, -2.977408999572651371 ) ) ;
#48152=CARTESIAN_POINT ( 'NONE',  ( -5.082755093536326818, -13.71875000204838457, 5.082755093536325042 ) ) ;
#48153=CARTESIAN_POINT ( 'NONE',  ( 7.986452802927061612, 26.02690242308113966, 0.5332468218996363474 ) ) ;
#48165=CARTESIAN_POINT ( 'NONE',  ( 4.898587196589412829E-16, -10.81250000409677092, -8.000000000000000000 ) ) ;
#48170=CARTESIAN_POINT ( 'NONE',  ( -9.645512969475857901, 88.01103150675727704, -2.645801731561387538 ) ) ;
#48183=CARTESIAN_POINT ( 'NONE',  ( 3.313708498984799800, -9.406250004096770923, -7.999999999999961808 ) ) ;
#48200=ORIENTED_EDGE ( 'NONE', *, *, #96434, .F. ) ;
#48216=CARTESIAN_POINT ( 'NONE',  ( 6.928203230275510549, 85.00000000000000000, -4.000000000000000000 ) ) ;
#48225=CARTESIAN_POINT ( 'NONE',  ( 2.977408999572651815, -16.43750000204838457, 7.188101187500000933 ) ) ;
#48272=CARTESIAN_POINT ( 'NONE',  ( -1.469576158976823947E-15, -22.06250000409676915, 8.000000000000000000 ) ) ;
#48284=ORIENTED_EDGE ( 'NONE', *, *, #68061, .T. ) ;
#48290=CARTESIAN_POINT ( 'NONE',  ( -3.313708498984765161, -32.65625000409677625, 7.999999999999998224 ) ) ;
#48295=CARTESIAN_POINT ( 'NONE',  ( 9.797372177749753774, 33.46509494847563815, 2.014953862275838503 ) ) ;
#48297=SURFACE_STYLE_FILL_AREA ( #62926 ) ;
#48300=CARTESIAN_POINT ( 'NONE',  ( -5.656854249492379694, -10.43749999999999112, -5.656854249492380582 ) ) ;
#48348=VERTEX_POINT ( 'NONE', #36909 ) ;
#48362=LINE ( 'NONE', #95880, #60669 ) ;
#48372=FACE_OUTER_BOUND ( 'NONE', #21903, .T. ) ;
#48396=CARTESIAN_POINT ( 'NONE',  ( 9.948688207305192321, 108.8702314949018444, -1.044946705213434024 ) ) ;
#48417=CARTESIAN_POINT ( 'NONE',  ( 7.999999999999998224, -12.59374999999999467, 3.313708498984766493 ) ) ;
#48419=CARTESIAN_POINT ( 'NONE',  ( -6.928203230275511437, 104.7352073274642805, 4.000000000000001776 ) ) ;
#48426=CARTESIAN_POINT ( 'NONE',  ( 3.484792534604217007, 15.95825086476136967, -9.380155525692146057 ) ) ;
#48444=CARTESIAN_POINT ( 'NONE',  ( 9.216463528758916723, 15.13241195026071928, -3.884543032214160085 ) ) ;
#48489=CARTESIAN_POINT ( 'NONE',  ( 7.999999999999998224, -27.59374999999999289, 3.313708498984766049 ) ) ;
#48490=ORIENTED_EDGE ( 'NONE', *, *, #72882, .F. ) ;
#48497=CARTESIAN_POINT ( 'NONE',  ( -7.188101187500000044, -11.28125000204838457, -8.802885111219163269E-16 ) ) ;
#48536=ORIENTED_EDGE ( 'NONE', *, *, #56547, .F. ) ;
#48542=CARTESIAN_POINT ( 'NONE',  ( -8.000000000000000000, -31.34374999999999645, -3.313708498984762496 ) ) ;
#48565=CARTESIAN_POINT ( 'NONE',  ( -7.188101187500000044, -12.40625000204838635, -8.802885111219163269E-16 ) ) ;
#48597=ORIENTED_EDGE ( 'NONE', *, *, #66044, .T. ) ;
#48616=CARTESIAN_POINT ( 'NONE',  ( -7.188101187500000044, -14.28125000204838457, -8.802885111219163269E-16 ) ) ;
#48624=CARTESIAN_POINT ( 'NONE',  ( -7.188101187500000044, -29.28125000204838813, -8.802885111219163269E-16 ) ) ;
#48650=CARTESIAN_POINT ( 'NONE',  ( -1.469576158976823947E-15, -25.06250000409677270, 8.000000000000000000 ) ) ;
#48666=CARTESIAN_POINT ( 'NONE',  ( 7.188101187500000044, -25.53125000204838813, 0.000000000000000000 ) ) ;
#48671=DIRECTION ( 'NONE',  ( -0.000000000000000000, 1.000000000000000000, -0.000000000000000000 ) ) ;
#48679=CARTESIAN_POINT ( 'NONE',  ( -7.188101187500000933, -12.50000000204838813, -2.977408999572651371 ) ) ;
#48680=CARTESIAN_POINT ( 'NONE',  ( 8.000086790516061086, 25.99982641893993929, 0.2639471549312826792 ) ) ;
#48692=CARTESIAN_POINT ( 'NONE',  ( 4.401442555609581635E-16, -29.28125000204838813, -7.188101187500000044 ) ) ;
#48696=CARTESIAN_POINT ( 'NONE',  ( -8.000000000000000000, -16.34374999999999289, -3.313708498984762496 ) ) ;
#48699=CARTESIAN_POINT ( 'NONE',  ( -9.482856158761276077, 32.44307115854724799, 3.177891129109638779 ) ) ;
#48702=CARTESIAN_POINT ( 'NONE',  ( -0.7060372491586903720, 15.23416508904650968, 9.999999999999998224 ) ) ;
#48739=CARTESIAN_POINT ( 'NONE',  ( 7.999885325681428405, 88.99977065129938580, 0.2682325777720055426 ) ) ;
#48748=CARTESIAN_POINT ( 'NONE',  ( 7.188101187499999156, -16.25000000204838813, 2.977408999572654924 ) ) ;
#48751=CARTESIAN_POINT ( 'NONE',  ( 9.176855344542989457, 84.47039573022591696, -3.973472207155925862 ) ) ;
#48814=CARTESIAN_POINT ( 'NONE',  ( -1.469576158976823947E-15, -25.06250000409677270, 8.000000000000000000 ) ) ;
#48910=DIRECTION ( 'NONE',  ( -0.000000000000000000, 1.000000000000000000, -0.000000000000000000 ) ) ;
#48918=CARTESIAN_POINT ( 'NONE',  ( 9.948181520647857212, 108.8689280276037863, 1.049088206181482574 ) ) ;
#48940=CARTESIAN_POINT ( 'NONE',  ( -8.000000000000000000, -11.84374999999999289, -3.313708498984762496 ) ) ;
#48948=CARTESIAN_POINT ( 'NONE',  ( 1.749942564367553022, 15.56091200510339512, -9.852211596319794040 ) ) ;
#48971=FILL_AREA_STYLE ('',( #75389 ) ) ;
#48989=CARTESIAN_POINT ( 'NONE',  ( -9.852235012526417535, 15.56087475005695353, 1.749814335632529749 ) ) ;
#48991=EDGE_CURVE ( 'NONE', #40836, #96386, #38552, .T. ) ;
#49007=CARTESIAN_POINT ( 'NONE',  ( 7.188101187500001821, -29.56250000204838813, -2.977408999572650483 ) ) ;
#49010=CARTESIAN_POINT ( 'NONE',  ( 2.563280883360062656, 15.30085158941011159, -9.673800154115147265 ) ) ;
#49015=CARTESIAN_POINT ( 'NONE',  ( -1.469576158976823947E-15, -27.87499999999999645, 8.000000000000000000 ) ) ;
#49048=CARTESIAN_POINT ( 'NONE',  ( 5.656854249492378806, -15.68749999999999289, 5.656854249492381470 ) ) ;
#49050=CARTESIAN_POINT ( 'NONE',  ( -10.00000000000000355, 105.0000000000000000, -4.000000000000001776 ) ) ;
#49070=CARTESIAN_POINT ( 'NONE',  ( 5.656854249492378806, -32.18749999999999289, 5.656854249492381470 ) ) ;
#49091=CARTESIAN_POINT ( 'NONE',  ( -2.977408999572654480, -13.62500000204838457, 7.188101187499999156 ) ) ;
#49105=ORIENTED_EDGE ( 'NONE', *, *, #73497, .T. ) ;
#49128=ORIENTED_EDGE ( 'NONE', *, *, #86312, .F. ) ;
#49145=CARTESIAN_POINT ( 'NONE',  ( 5.082755093536324154, -12.21875000204838635, 5.082755093536326818 ) ) ;
#49148=CARTESIAN_POINT ( 'NONE',  ( 7.186686048019178763, -30.00000000000000355, -0.4953821823922022194 ) ) ;
#49154=CARTESIAN_POINT ( 'NONE',  ( -5.082755093536325042, -26.46875000204838813, -5.082755093536325930 ) ) ;
#49170=CARTESIAN_POINT ( 'NONE',  ( -8.000086790516061086, 89.00017358106009624, 0.2639471549312795151 ) ) ;
#49184=CARTESIAN_POINT ( 'NONE',  ( -5.656854249492379694, -25.62500000409677270, -5.656854249492380582 ) ) ;
#49199=CARTESIAN_POINT ( 'NONE',  ( 9.483056940782024213, 27.55612209893422815, -3.177305548492607379 ) ) ;
#49200=CARTESIAN_POINT ( 'NONE',  ( -7.188101187500000044, -27.78125000204838813, -8.802885111219163269E-16 ) ) ;
#49206=CARTESIAN_POINT ( 'NONE',  ( 0.000000000000000000, -30.00000000000000000, 0.000000000000000000 ) ) ;
#49215=CARTESIAN_POINT ( 'NONE',  ( 7.188101187500000044, -13.15625000204838280, 0.000000000000000000 ) ) ;
#49223=CARTESIAN_POINT ( 'NONE',  ( -3.313708498984798467, -19.53124999999999289, -7.999999999999961808 ) ) ;
#49225=CARTESIAN_POINT ( 'NONE',  ( -1.320432766682874540E-15, -30.03125000204838813, 7.188101187500000044 ) ) ;
#49236=( BOUNDED_CURVE ( )  B_SPLINE_CURVE ( 1, ( #66991, #58903 ),
 .UNSPECIFIED., .F., .F. ) 
 B_SPLINE_CURVE_WITH_KNOTS ( ( 2, 2 ),
 ( 0.000000000000000000, 1.000000000000000000 ),
 .UNSPECIFIED. ) 
 CURVE ( )  GEOMETRIC_REPRESENTATION_ITEM ( )  RATIONAL_B_SPLINE_CURVE ( ( 0.9660719911213342392, 0.9660719911213342392 ) ) 
 REPRESENTATION_ITEM ( '' )  );
#49265=ORIENTED_EDGE ( 'NONE', *, *, #7820, .F. ) ;
#49284=CARTESIAN_POINT ( 'NONE',  ( 2.977408999572650927, -21.87500000204838813, -7.188101187500001821 ) ) ;
#49351=CARTESIAN_POINT ( 'NONE',  ( 4.898587196589412829E-16, -24.31250000409677270, -8.000000000000000000 ) ) ;
#49375=AXIS2_PLACEMENT_3D ( 'NONE', #37485, #88648, #39051 ) ;
#49392=CARTESIAN_POINT ( 'NONE',  ( -7.045965687440314262, 31.30392463786035151, 3.790395326974318913 ) ) ;
#49418=CARTESIAN_POINT ( 'NONE',  ( 3.997425403568278579, 15.99999999372935022, 9.168149550320896068 ) ) ;
#49437=CARTESIAN_POINT ( 'NONE',  ( -8.000000000000001776, -28.34375000409677270, 3.313708498984759387 ) ) ;
#49442=VERTEX_POINT ( 'NONE', #92971 ) ;
#49483=CARTESIAN_POINT ( 'NONE',  ( 7.999999999999998224, -11.09374999999999289, 3.313708498984766493 ) ) ;
#49518=CARTESIAN_POINT ( 'NONE',  ( -7.801777176595949825, 81.41172014187367267, -1.786991866639916715 ) ) ;
#49551=CARTESIAN_POINT ( 'NONE',  ( -7.188101187500000044, -28.90625000204838813, -8.802885111219163269E-16 ) ) ;
#49589=CARTESIAN_POINT ( 'NONE',  ( 7.999999999999998224, -29.28125000409677270, 3.313708498984766049 ) ) ;
#49611=CARTESIAN_POINT ( 'NONE',  ( -1.469576158976823947E-15, -24.87499999999999289, 8.000000000000000000 ) ) ;
#49620=CARTESIAN_POINT ( 'NONE',  ( -8.000000000000000000, -8.937500004096769146, -9.797174393178825657E-16 ) ) ;
#49624=DIRECTION ( 'NONE',  ( 0.000000000000000000, 1.000000000000000000, 0.000000000000000000 ) ) ;
#49636=CARTESIAN_POINT ( 'NONE',  ( 2.977408999572651815, -11.93750000204838457, 7.188101187500000933 ) ) ;
#49663=EDGE_CURVE ( 'NONE', #89014, #10653, #78380, .T. ) ;
#49690=CARTESIAN_POINT ( 'NONE',  ( 7.188101187499999156, -15.12500000204838457, 2.977408999572654924 ) ) ;
#49701=CARTESIAN_POINT ( 'NONE',  ( -5.082755093536325042, -21.96875000204838457, -5.082755093536325930 ) ) ;
#49739=CARTESIAN_POINT ( 'NONE',  ( 9.698972129396510766, 26.82370287258062191, -2.445345647270328993 ) ) ;
#49740=CARTESIAN_POINT ( 'NONE',  ( -1.320432766682874540E-15, -21.40625000204838457, 7.188101187500000044 ) ) ;
#49756=CARTESIAN_POINT ( 'NONE',  ( 7.896571385775229324, 26.21002000654247155, 1.305932416347440173 ) ) ;
#49767=DIRECTION ( 'NONE',  ( -0.000000000000000000, 1.000000000000000000, -0.000000000000000000 ) ) ;
#49769=CARTESIAN_POINT ( 'NONE',  ( -7.188101187500001821, -30.50000000204838813, -2.977408999572651371 ) ) ;
#49817=CARTESIAN_POINT ( 'NONE',  ( 7.934996450857311423, 88.86862456472529459, -1.050865690281773901 ) ) ;
#49827=CARTESIAN_POINT ( 'NONE',  ( -5.082755093536326818, -10.71875000204838457, 5.082755093536325042 ) ) ;
#49832=DIRECTION ( 'NONE',  ( -0.000000000000000000, -1.000000000000000000, -0.000000000000000000 ) ) ;
#49838=VERTEX_POINT ( 'NONE', #76654 ) ;
#49861=CARTESIAN_POINT ( 'NONE',  ( 7.212408192734267587, 82.98482910679631175, -3.465038817813880456 ) ) ;
#49882=CARTESIAN_POINT ( 'NONE',  ( -5.082755093536326818, -28.71875000204838813, 5.082755093536325042 ) ) ;
#49891=CARTESIAN_POINT ( 'NONE',  ( 8.000000000000000000, -24.59375000409677270, -3.313708498984761608 ) ) ;
#49895=CARTESIAN_POINT ( 'NONE',  ( 9.253500431420430772, 31.29771549917707674, 3.792688295761954098 ) ) ;
#49898=CARTESIAN_POINT ( 'NONE',  ( -0.6976587266869073156, -30.00000000000001066, -7.793936262885737598 ) ) ;
#49901=LINE ( 'NONE', #25683, #6044 ) ;
#49927=EDGE_CURVE ( 'NONE', #103221, #11237, #71599, .T. ) ;
#49931=CARTESIAN_POINT ( 'NONE',  ( -7.896165657598945842, 33.78911131371973653, -1.307894402814547385 ) ) ;
#49951=FACE_OUTER_BOUND ( 'NONE', #36556, .T. ) ;
#50000=CARTESIAN_POINT ( 'NONE',  ( 9.482945380845297478, 107.4433305877892764, 3.177595346755246464 ) ) ;
#50020=CARTESIAN_POINT ( 'NONE',  ( -7.414580834929599185, 102.3534371971851726, 3.010264818013836940 ) ) ;
#50030=CARTESIAN_POINT ( 'NONE',  ( 3.313708498984761608, -18.21874999999999645, -8.000000000000000000 ) ) ;
#50049=CARTESIAN_POINT ( 'NONE',  ( -7.045755811259134305, 83.69658396986446292, 3.790843699961853552 ) ) ;
#50085=CARTESIAN_POINT ( 'NONE',  ( 5.082755093536325930, -30.96875000204838813, -5.082755093536325042 ) ) ;
#50100=VERTEX_POINT ( 'NONE', #102275 ) ;
#50142=LINE ( 'NONE', #83050, #83422 ) ;
#50143=CARTESIAN_POINT ( 'NONE',  ( 8.000000000000000000, -28.99999999999999289, 0.000000000000000000 ) ) ;
#50171=CARTESIAN_POINT ( 'NONE',  ( -2.977408999572654480, -15.12500000204838457, 7.188101187499999156 ) ) ;
#50187=EDGE_CURVE ( 'NONE', #77405, #93124, #62370, .T. ) ;
#50226=CARTESIAN_POINT ( 'NONE',  ( 7.188101187500000933, -14.93750000204838457, -2.977408999572650483 ) ) ;
#50233=CARTESIAN_POINT ( 'NONE',  ( -5.082755093536326818, -23.09375000204838457, 5.082755093536325042 ) ) ;
#50273=CARTESIAN_POINT ( 'NONE',  ( -1.320432766682874540E-15, -18.40625000204838457, 7.188101187500000044 ) ) ;
#50274=DIRECTION ( 'NONE',  ( 0.000000000000000000, 1.000000000000000000, 0.000000000000000000 ) ) ;
#50276=EDGE_LOOP ( 'NONE', ( #55802, #96054, #8283, #15336 ) ) ;
#50279=CARTESIAN_POINT ( 'NONE',  ( 9.165151389911679658, 85.00000000000000000, 4.000000000000000000 ) ) ;
#50297=CARTESIAN_POINT ( 'NONE',  ( -2.977408999572650039, -33.68750000204839523, -7.188101187500001821 ) ) ;
#50346=CARTESIAN_POINT ( 'NONE',  ( 0.000000000000000000, 115.0000000000000000, 0.000000000000000000 ) ) ;
#50347=CARTESIAN_POINT ( 'NONE',  ( -7.188101187500002709, -15.31250000204838457, 2.977408999572648707 ) ) ;
#50353=CARTESIAN_POINT ( 'NONE',  ( 4.898587196589412829E-16, -18.12499999999999645, -8.000000000000000000 ) ) ;
#50382=CARTESIAN_POINT ( 'NONE',  ( 7.343637806710344051, 82.55636878099383580, 3.177475076494672646 ) ) ;
#50402=CARTESIAN_POINT ( 'NONE',  ( 7.188101187500000933, -25.06250000204838813, -2.977408999572650483 ) ) ;
#50412=CARTESIAN_POINT ( 'NONE',  ( 3.313708498984762052, -25.90625000409676559, -8.000000000000000000 ) ) ;
#50421=CARTESIAN_POINT ( 'NONE',  ( 0.000000000000000000, 15.00000000000000000, -9.999999999999998224 ) ) ;
#50468=ORIENTED_EDGE ( 'NONE', *, *, #66784, .T. ) ;
#50472=( BOUNDED_CURVE ( )  B_SPLINE_CURVE ( 2, ( #19111, #26144, #58999, #84864, #75698, #26661, #100504, #59540, #51949 ),
 .UNSPECIFIED., .F., .F. ) 
 B_SPLINE_CURVE_WITH_KNOTS ( ( 3, 2, 2, 2, 3 ),
 ( 0.6029411764705882026, 0.6102941176470588758, 0.6176470588235294379, 0.6250000000000000000, 0.6323529411764705621 ),
 .UNSPECIFIED. ) 
 CURVE ( )  GEOMETRIC_REPRESENTATION_ITEM ( )  RATIONAL_B_SPLINE_CURVE ( ( 1.000000000000000000, 0.9238795325112867385, 1.000000000000000000, 0.9238795325112867385, 1.000000000000000000, 0.9238795325112867385, 1.000000000000000000, 0.9238795325112867385, 1.000000000000000000 ) ) 
 REPRESENTATION_ITEM ( '' )  );
#50493=SURFACE_STYLE_FILL_AREA ( #33827 ) ;
#50510=EDGE_LOOP ( 'NONE', ( #58088, #62543, #93313, #7517 ) ) ;
#50564=PRESENTATION_STYLE_ASSIGNMENT (( #17705 ) ) ;
#50570=ORIENTED_EDGE ( 'NONE', *, *, #62176, .F. ) ;
#50598=CARTESIAN_POINT ( 'NONE',  ( 4.401442555609581635E-16, -32.28125000204838813, -7.188101187500000044 ) ) ;
#50630=CARTESIAN_POINT ( 'NONE',  ( 5.656854249492380582, -29.00000000409677270, -5.656854249492379694 ) ) ;
#50649=CARTESIAN_POINT ( 'NONE',  ( -5.656854249492379694, -29.93749999999999645, -5.656854249492380582 ) ) ;
#50700=DIRECTION ( 'NONE',  ( -0.000000000000000000, 1.000000000000000000, -0.000000000000000000 ) ) ;
#50735=CARTESIAN_POINT ( 'NONE',  ( -5.082755093536326818, -9.593750002048384573, 5.082755093536325042 ) ) ;
#50737=CARTESIAN_POINT ( 'NONE',  ( 3.313708498984761608, -18.40625000409676915, -8.000000000000000000 ) ) ;
#50743=CARTESIAN_POINT ( 'NONE',  ( 2.977408999572650927, -20.75000000204839523, -7.188101187500001821 ) ) ;
#50753=PRODUCT_DEFINITION_FORMATION_WITH_SPECIFIED_SOURCE ( 'ANY', '', #38205, .NOT_KNOWN. ) ;
#50778=EDGE_LOOP ( 'NONE', ( #62755, #98557, #2277, #26902 ) ) ;
#50784=CARTESIAN_POINT ( 'NONE',  ( -2.977408999572650039, -22.06250000204838813, -7.188101187500001821 ) ) ;
#50790=PLANE ( 'NONE',  #55142 ) ;
#50793=ORIENTED_EDGE ( 'NONE', *, *, #24209, .T. ) ;
#50815=CARTESIAN_POINT ( 'NONE',  ( 2.977408999572650927, -32.37500000204838813, -7.188101187500001821 ) ) ;
#50878=CARTESIAN_POINT ( 'NONE',  ( 5.082755093536325930, -12.96875000204838280, -5.082755093536325042 ) ) ;
#50884=CARTESIAN_POINT ( 'NONE',  ( -1.469576158976823947E-15, -14.37499999999999112, 8.000000000000000000 ) ) ;
#50896=DIRECTION ( 'NONE',  ( 0.000000000000000000, 0.000000000000000000, -1.000000000000000000 ) ) ;
#50908=VERTEX_POINT ( 'NONE', #41130 ) ;
#50909=DIRECTION ( 'NONE',  ( -0.4165977904505306917, 0.000000000000000000, 0.9090909090909092827 ) ) ;
#50912=CARTESIAN_POINT ( 'NONE',  ( 7.344505440741524893, 82.55381072701295864, -3.175463080953001782 ) ) ;
#50932=CARTESIAN_POINT ( 'NONE',  ( -5.082755093536325042, -27.59375000204838457, -5.082755093536325930 ) ) ;
#50941=CARTESIAN_POINT ( 'NONE',  ( 5.656854249492378806, -26.37500000409677270, 5.656854249492381470 ) ) ;
#50950=CARTESIAN_POINT ( 'NONE',  ( -4.165977904505307805, 16.00000000000000000, -9.090909090909091717 ) ) ;
#50993=CARTESIAN_POINT ( 'NONE',  ( -1.469576158976823947E-15, -20.56250000409676915, 8.000000000000000000 ) ) ;
#51000=CARTESIAN_POINT ( 'NONE',  ( 4.898587196589412829E-16, -22.62499999999999289, -8.000000000000000000 ) ) ;
#51002=CARTESIAN_POINT ( 'NONE',  ( 2.802461721337127898, 15.83563386295778308, 9.606080321247342013 ) ) ;
#51042=ORIENTED_EDGE ( 'NONE', *, *, #88247, .T. ) ;
#51074=( GEOMETRIC_REPRESENTATION_CONTEXT ( 3 ) GLOBAL_UNCERTAINTY_ASSIGNED_CONTEXT ( ( #99855 ) ) GLOBAL_UNIT_ASSIGNED_CONTEXT ( ( #5081, #79491, #47112 ) ) REPRESENTATION_CONTEXT ( 'NONE', 'WORKASPACE' ) );
#51079=CYLINDRICAL_SURFACE ( 'NONE', #89940, 8.000000000000000000 ) ;
#51105=CARTESIAN_POINT ( 'NONE',  ( -9.176855344542985904, 105.5296042697740972, -3.973472207155928970 ) ) ;
#51181=AXIS2_PLACEMENT_3D ( 'NONE', #16772, #64279, #33504 ) ;
#51193=DIRECTION ( 'NONE',  ( 1.000000000000000000, -0.000000000000000000, -0.000000000000000000 ) ) ;
#51194=CARTESIAN_POINT ( 'NONE',  ( 3.313708498984762496, -29.28124999999999645, 7.999999999999998224 ) ) ;
#51218=CARTESIAN_POINT ( 'NONE',  ( 7.188101187499999156, -10.25000000204838813, 2.977408999572654924 ) ) ;
#51283=CARTESIAN_POINT ( 'NONE',  ( 2.977408999572651815, -19.81250000204838813, 7.188101187500000933 ) ) ;
#51301=ORIENTED_EDGE ( 'NONE', *, *, #31116, .F. ) ;
#51326=CARTESIAN_POINT ( 'NONE',  ( 5.082755093536324154, -19.71875000204838457, 5.082755093536326818 ) ) ;
#51334=CARTESIAN_POINT ( 'NONE',  ( -8.000000000000000000, -12.03125000409677270, -3.313708498984762496 ) ) ;
#51358=CARTESIAN_POINT ( 'NONE',  ( -5.082755093536325042, -23.09375000204838457, -5.082755093536325930 ) ) ;
#51374=CARTESIAN_POINT ( 'NONE',  ( 9.220915120640581719, 103.9554511356791267, -3.870126578504840875 ) ) ;
#51411=CARTESIAN_POINT ( 'NONE',  ( -5.082755093536326818, -24.59375000204838813, 5.082755093536325042 ) ) ;
#51419=CARTESIAN_POINT ( 'NONE',  ( -7.188101187500001821, -12.50000000204838990, -2.977408999572651371 ) ) ;
#51478=CARTESIAN_POINT ( 'NONE',  ( -7.188101187500000933, -26.00000000204838457, -2.977408999572651371 ) ) ;
#51486=CARTESIAN_POINT ( 'NONE',  ( 3.313708498984762496, -17.46875000409676559, 7.999999999999998224 ) ) ;
#51495=CARTESIAN_POINT ( 'NONE',  ( 2.909149233950971691, -30.00000000000000711, -7.051612309719152982 ) ) ;
#51526=ADVANCED_FACE ( 'NONE', ( #54648 ), #87582, .F. ) ;
#51567=CARTESIAN_POINT ( 'NONE',  ( 0.000000000000000000, 115.0000000000000000, 0.000000000000000000 ) ) ;
#51606=CARTESIAN_POINT ( 'NONE',  ( -8.000000000000000000, -20.74999999999999289, -9.797174393178825657E-16 ) ) ;
#51614=CARTESIAN_POINT ( 'NONE',  ( -7.046357527897571416, 103.6938434939899594, -3.789683693877208270 ) ) ;
#51643=ORIENTED_EDGE ( 'NONE', *, *, #43138, .F. ) ;
#51733=CARTESIAN_POINT ( 'NONE',  ( 5.656854249492378806, -23.18749999999999289, 5.656854249492381470 ) ) ;
#51734=CARTESIAN_POINT ( 'NONE',  ( -1.469576158976823947E-15, -26.37499999999999645, 8.000000000000000000 ) ) ;
#51754=CARTESIAN_POINT ( 'NONE',  ( 7.801642220026312025, 108.5879682614903174, 1.787233835843584417 ) ) ;
#51799=DIRECTION ( 'NONE',  ( -0.000000000000000000, 1.000000000000000000, -0.000000000000000000 ) ) ;
#51814=CARTESIAN_POINT ( 'NONE',  ( -4.413588872740235480, -9.563952367645422115, 5.751921314332418156 ) ) ;
#51820=CARTESIAN_POINT ( 'NONE',  ( -7.188101187500002709, -21.68750000204838813, 2.977408999572648707 ) ) ;
#51862=CARTESIAN_POINT ( 'NONE',  ( 2.977408999572651815, -16.81250000204838457, 7.188101187500000933 ) ) ;
#51865=CARTESIAN_POINT ( 'NONE',  ( -3.313708498984798467, -12.21875000409676915, -7.999999999999961808 ) ) ;
#51871=ORIENTED_EDGE ( 'NONE', *, *, #68893, .F. ) ;
#51887=CARTESIAN_POINT ( 'NONE',  ( -2.977408999572650039, -26.18750000204838813, -7.188101187500001821 ) ) ;
#51906=MANIFOLD_SOLID_BREP ( 'Fillet1', #60131 ) ;
#51910=CARTESIAN_POINT ( 'NONE',  ( 9.165151389911679658, 105.0000000000000142, -4.000000000000001776 ) ) ;
#51917=CARTESIAN_POINT ( 'NONE',  ( 3.313708498984761608, -25.71874999999999645, -8.000000000000000000 ) ) ;
#51939=CARTESIAN_POINT ( 'NONE',  ( 7.188101187500000933, -23.93750000204838457, -2.977408999572650483 ) ) ;
#51948=CARTESIAN_POINT ( 'NONE',  ( 2.977408999572650927, -11.37500000204838813, -7.188101187500001821 ) ) ;
#51949=CARTESIAN_POINT ( 'NONE',  ( -1.469576158976823947E-15, -17.56250000409676915, 8.000000000000000000 ) ) ;
#51984=CARTESIAN_POINT ( 'NONE',  ( 7.619701877737480977, 81.82557840467232779, -2.447562251315978710 ) ) ;
#52006=CARTESIAN_POINT ( 'NONE',  ( -2.977408999572654480, -24.12500000204838813, 7.188101187499999156 ) ) ;
#52011=EDGE_CURVE ( 'NONE', #99675, #28267, #40035, .T. ) ;
#52019=CARTESIAN_POINT ( 'NONE',  ( -3.313708498984765161, -19.15625000409676915, 7.999999999999998224 ) ) ;
#52067=DIRECTION ( 'NONE',  ( -0.000000000000000000, 1.000000000000000000, -0.000000000000000000 ) ) ;
#52068=CARTESIAN_POINT ( 'NONE',  ( 0.000000000000000000, -30.00000000000000000, 0.000000000000000000 ) ) ;
#52082=DIRECTION ( 'NONE',  ( 1.000000000000000000, -0.000000000000000000, -0.000000000000000000 ) ) ;
#52089=VECTOR ( 'NONE', #62738, 1000.000000000000000 ) ;
#52101=DIRECTION ( 'NONE',  ( 0.000000000000000000, 1.000000000000000000, 0.000000000000000000 ) ) ;
#52112=ORIENTED_EDGE ( 'NONE', *, *, #35616, .F. ) ;
#52113=ORIENTED_EDGE ( 'NONE', *, *, #96371, .F. ) ;
#52138=CARTESIAN_POINT ( 'NONE',  ( -8.000000000000001776, -20.65624999999999289, 3.313708498984759387 ) ) ;
#52146=CARTESIAN_POINT ( 'NONE',  ( -7.986711519608431509, 101.0263809637656607, -0.5300249774147618442 ) ) ;
#52147=EDGE_CURVE ( 'NONE', #53546, #94586, #88933, .T. ) ;
#52170=CARTESIAN_POINT ( 'NONE',  ( -10.00000000000000000, 15.00000000000000000, 4.397168787612342200 ) ) ;
#52232=LINE ( 'NONE', #36107, #45888 ) ;
#52264=CARTESIAN_POINT ( 'NONE',  ( -8.000000000000001776, -22.15624999999999289, 3.313708498984758943 ) ) ;
#52291=CARTESIAN_POINT ( 'NONE',  ( 7.188101187500000044, -10.15625000204838457, 0.000000000000000000 ) ) ;
#52331=LINE ( 'NONE', #94950, #99515 ) ;
#52353=CARTESIAN_POINT ( 'NONE',  ( 7.188101187500001821, -13.43750000204838457, -2.977408999572650483 ) ) ;
#52365=UNCERTAINTY_MEASURE_WITH_UNIT (LENGTH_MEASURE( 1.000000000000000082E-05 ), #87594, 'distance_accuracy_value', 'NONE');
#52368=CARTESIAN_POINT ( 'NONE',  ( -7.211357414135268762, 87.01146539934444490, 3.467230644691327690 ) ) ;
#52382=( BOUNDED_CURVE ( )  B_SPLINE_CURVE ( 2, ( #27439, #100739, #94262, #26901, #11184, #101808, #12262, #67852, #84036 ),
 .UNSPECIFIED., .F., .F. ) 
 B_SPLINE_CURVE_WITH_KNOTS ( ( 3, 2, 2, 2, 3 ),
 ( 0.3676470588235293824, 0.3749999999999999445, 0.3823529411764705621, 0.3897058823529411797, 0.3970588235294117418 ),
 .UNSPECIFIED. ) 
 CURVE ( )  GEOMETRIC_REPRESENTATION_ITEM ( )  RATIONAL_B_SPLINE_CURVE ( ( 1.000000000000000666, 0.9238795325112861834, 1.000000000000000000, 0.9238795325112867385, 1.000000000000000000, 0.9238795325112867385, 1.000000000000000000, 0.9238795325112867385, 1.000000000000000000 ) ) 
 REPRESENTATION_ITEM ( '' )  );
#52385=ORIENTED_EDGE ( 'NONE', *, *, #21437, .T. ) ;
#52386=CARTESIAN_POINT ( 'NONE',  ( 9.999999999999996447, 15.00000000000000000, -10.00000000000000000 ) ) ;
#52394=CARTESIAN_POINT ( 'NONE',  ( 5.082755093536324154, -13.71875000204838457, 5.082755093536326818 ) ) ;
#52396=CARTESIAN_POINT ( 'NONE',  ( 0.000000000000000000, 15.00000000000000000, 0.000000000000000000 ) ) ;
#52418=CARTESIAN_POINT ( 'NONE',  ( -1.320432766682874540E-15, -28.53125000204838813, 7.188101187500000044 ) ) ;
#52449=EDGE_CURVE ( 'NONE', #39461, #28165, #83230, .T. ) ;
#52470=CARTESIAN_POINT ( 'NONE',  ( -5.082755093536325042, -27.96875000204838457, -5.082755093536325930 ) ) ;
#52480=CARTESIAN_POINT ( 'NONE',  ( 7.188101187499999156, -30.12500000204838813, 2.977408999572654924 ) ) ;
#52520=CARTESIAN_POINT ( 'NONE',  ( 0.000000000000000000, -30.00000000000000000, 0.000000000000000000 ) ) ;
#52535=CARTESIAN_POINT ( 'NONE',  ( -5.082755093536325042, -18.59375000204838457, -5.082755093536325930 ) ) ;
#52546=CARTESIAN_POINT ( 'NONE',  ( -5.656854249492381470, -20.75000000409676915, 5.656854249492379694 ) ) ;
#52557=CARTESIAN_POINT ( 'NONE',  ( -1.469576158976823947E-15, -27.87499999999999645, 8.000000000000000000 ) ) ;
#52581=CYLINDRICAL_SURFACE ( 'NONE', #90775, 8.000000000000000000 ) ;
#52604=CARTESIAN_POINT ( 'NONE',  ( -5.082755093536325042, -33.59375000204838813, -5.082755093536325930 ) ) ;
#52655=ORIENTED_EDGE ( 'NONE', *, *, #71304, .T. ) ;
#52804=CARTESIAN_POINT ( 'NONE',  ( -5.656854249492379694, -23.93749999999999289, -5.656854249492380582 ) ) ;
#52831=( NAMED_UNIT ( * ) SI_UNIT ( $, .STERADIAN. ) SOLID_ANGLE_UNIT ( ) );
#52845=B_SPLINE_CURVE_WITH_KNOTS ( 'NONE', 3,
 ( #94746, #20895, #45650, #78526, #37592, #95265, #2510, #35455, #68329, #101225 ),
 .UNSPECIFIED., .F., .F.,
 ( 4, 2, 2, 2, 4 ),
 ( -2.000195913693545311E-05, 0.001085800244612924147, 0.002191602448362783492, 0.003297404652112643272, 0.004403206855862503051 ),
 .UNSPECIFIED. ) ;
#52848=CARTESIAN_POINT ( 'NONE',  ( -3.999986872311680042, -9.563226186441980303, 6.928210809543925208 ) ) ;
#52870=DIRECTION ( 'NONE',  ( -0.000000000000000000, 1.000000000000000000, -0.000000000000000000 ) ) ;
#52897=CARTESIAN_POINT ( 'NONE',  ( -2.977408999572650039, -16.06250000204838457, -7.188101187500001821 ) ) ;
#52901=ADVANCED_FACE ( 'NONE', ( #101161 ), #19764, .T. ) ;
#52933=CARTESIAN_POINT ( 'NONE',  ( 7.999999999999998224, -21.59374999999999645, 3.313708498984766049 ) ) ;
#52936=CARTESIAN_POINT ( 'NONE',  ( -5.082755093536325042, -12.96875000204838280, -5.082755093536325930 ) ) ;
#52962=CARTESIAN_POINT ( 'NONE',  ( -1.320432766682874540E-15, -25.53125000204838813, 7.188101187500000044 ) ) ;
#52965=CARTESIAN_POINT ( 'NONE',  ( 1.224646799147353256E-15, 115.0000000000000000, 10.00000000000000000 ) ) ;
#52974=DIRECTION ( 'NONE',  ( 1.000000000000000000, -0.000000000000000000, -0.000000000000000000 ) ) ;
#52981=CARTESIAN_POINT ( 'NONE',  ( 5.656854249492380582, -16.81249999999999289, -5.656854249492379694 ) ) ;
#52982=CARTESIAN_POINT ( 'NONE',  ( 8.000000000000000000, -21.68750000409676915, 0.000000000000000000 ) ) ;
#52986=CARTESIAN_POINT ( 'NONE',  ( -3.313708498984779371, -22.71875000409676915, -7.999999999999981348 ) ) ;
#53017=CARTESIAN_POINT ( 'NONE',  ( 5.082755093536325930, -26.84375000204838813, -5.082755093536325042 ) ) ;
#53028=CARTESIAN_POINT ( 'NONE',  ( -2.977408999572650039, -32.56250000204838813, -7.188101187500001821 ) ) ;
#53035=CARTESIAN_POINT ( 'NONE',  ( -7.934914944860276265, 108.8684564720010997, -1.051261972695692659 ) ) ;
#53071=CARTESIAN_POINT ( 'NONE',  ( 2.977408999572651815, -31.81250000204839168, 7.188101187500000933 ) ) ;
#53081=EDGE_LOOP ( 'NONE', ( #9603, #41973 ) ) ;
#53086=CARTESIAN_POINT ( 'NONE',  ( -2.977408999572650039, -17.18750000204838813, -7.188101187500000933 ) ) ;
#53089=ORIENTED_EDGE ( 'NONE', *, *, #53175, .F. ) ;
#53093=CARTESIAN_POINT ( 'NONE',  ( -10.00004721872059577, 80.99988195318846351, -0.2617599822266473142 ) ) ;
#53095=CARTESIAN_POINT ( 'NONE',  ( -8.000000000000000000, -19.53125000409677980, -3.313708498984762496 ) ) ;
#53099=CARTESIAN_POINT ( 'NONE',  ( -9.333892298909264085, 86.78275731625036826, -3.590295303293451923 ) ) ;
#53111=EDGE_LOOP ( 'NONE', ( #5419, #56354, #32313, #63005 ) ) ;
#53161=CARTESIAN_POINT ( 'NONE',  ( -2.977408999572654480, -27.12500000204838457, 7.188101187499999156 ) ) ;
#53174=FACE_OUTER_BOUND ( 'NONE', #76791, .T. ) ;
#53175=EDGE_CURVE ( 'NONE', #76534, #77405, #40138, .T. ) ;
#53191=CARTESIAN_POINT ( 'NONE',  ( 2.797224791467302740, 15.83450757143047305, 9.607634652978001455 ) ) ;
#53228=CARTESIAN_POINT ( 'NONE',  ( 8.000000000000000000, -33.59375000409677625, -3.313708498984761608 ) ) ;
#53235=FACE_OUTER_BOUND ( 'NONE', #69613, .T. ) ;
#53246=CARTESIAN_POINT ( 'NONE',  ( 9.797174393178825657E-16, -30.00000000000000000, -8.000000000000000000 ) ) ;
#53247=EDGE_CURVE ( 'NONE', #28968, #101925, #71917, .T. ) ;
#53280=CARTESIAN_POINT ( 'NONE',  ( 4.898587196589412829E-16, -19.62499999999999289, -8.000000000000000000 ) ) ;
#53337=CARTESIAN_POINT ( 'NONE',  ( -9.607612890400021755, 15.83452282593334992, -2.797297131808753168 ) ) ;
#53344=CARTESIAN_POINT ( 'NONE',  ( 4.898587196589412829E-16, -22.62499999999999289, -8.000000000000000000 ) ) ;
#53394=LINE ( 'NONE', #77130, #21891 ) ;
#53400=CARTESIAN_POINT ( 'NONE',  ( -9.253500431420430772, 28.70228450082293037, 3.792688295761953210 ) ) ;
#53435=CARTESIAN_POINT ( 'NONE',  ( -7.188101187500002709, -14.18750000204838280, 2.977408999572648707 ) ) ;
#53443=UNCERTAINTY_MEASURE_WITH_UNIT (LENGTH_MEASURE( 1.000000000000000082E-05 ), #89906, 'distance_accuracy_value', 'NONE');
#53458=CARTESIAN_POINT ( 'NONE',  ( 7.999999999999998224, -26.28125000409676915, 3.313708498984766049 ) ) ;
#53466=CARTESIAN_POINT ( 'NONE',  ( 7.212994264445061532, 32.01711344340037613, 3.463766307298584479 ) ) ;
#53470=DIRECTION ( 'NONE',  ( -0.000000000000000000, 1.000000000000000000, -0.000000000000000000 ) ) ;
#53471=CARTESIAN_POINT ( 'NONE',  ( 3.313708498984722972, -21.21874999999998934, -8.000000000000040856 ) ) ;
#53474=CARTESIAN_POINT ( 'NONE',  ( -7.188101187500001821, -11.37500000204838813, -2.977408999572651371 ) ) ;
#53499=CARTESIAN_POINT ( 'NONE',  ( -2.977408999572650039, -24.68750000204838457, -7.188101187500001821 ) ) ;
#53512=CARTESIAN_POINT ( 'NONE',  ( 4.898587196589412829E-16, -16.62499999999999289, -8.000000000000000000 ) ) ;
#53517=CARTESIAN_POINT ( 'NONE',  ( 9.644834624769973885, 101.9910949979422412, 2.648308524638421702 ) ) ;
#53525=CARTESIAN_POINT ( 'NONE',  ( 0.000000000000000000, 16.00000000000000000, 0.000000000000000000 ) ) ;
#53528=EDGE_LOOP ( 'NONE', ( #84809, #31678, #56525, #30263 ) ) ;
#53546=VERTEX_POINT ( 'NONE', #63651 ) ;
#53548=CARTESIAN_POINT ( 'NONE',  ( 7.188101187500000933, -26.93750000204838457, -2.977408999572650483 ) ) ;
#53557=CARTESIAN_POINT ( 'NONE',  ( -4.413588872740236368, -9.188952367645423891, 5.751921314332417268 ) ) ;
#53563=CARTESIAN_POINT ( 'NONE',  ( -7.344505440741524005, 107.4461892729869987, -3.175463080953003114 ) ) ;
#53595=CARTESIAN_POINT ( 'NONE',  ( -2.977408999572650039, -34.06250000204839523, -7.188101187500001821 ) ) ;
#53607=CARTESIAN_POINT ( 'NONE',  ( -1.320432766682874540E-15, -16.53125000204838813, 7.188101187500000044 ) ) ;
#53617=CARTESIAN_POINT ( 'NONE',  ( 5.656854249492380582, -15.50000000409677092, -5.656854249492379694 ) ) ;
#53619=CARTESIAN_POINT ( 'NONE',  ( 9.090909090909084611, 16.00000000000000000, 4.165977904505317575 ) ) ;
#53677=CARTESIAN_POINT ( 'NONE',  ( -7.188101187500001821, -23.00000000204839523, -2.977408999572651371 ) ) ;
#53681=PLANE ( 'NONE',  #60179 ) ;
#53686=CARTESIAN_POINT ( 'NONE',  ( -1.469576158976823947E-15, -17.37499999999999289, 8.000000000000000000 ) ) ;
#53687=CARTESIAN_POINT ( 'NONE',  ( 4.898587196589412829E-16, -22.81250000409677270, -8.000000000000000000 ) ) ;
#53720=CARTESIAN_POINT ( 'NONE',  ( -5.656854249492381470, -16.25000000409677270, 5.656854249492379694 ) ) ;
#53747=B_SPLINE_CURVE_WITH_KNOTS ( 'NONE', 3,
 ( #97918, #98963, #66618, #57985, #49895, #8904, #81193, #82803, #74693, #775, #25677, #48295, #39706, #91443, #72581, #47762, #80666, #64510, #97378, #89312, #7302, #40214, #73087, #32146, #26736, #43417, #69299, #18086, #77373, #35353, #75226, #59071, #68221, #19713 ),
 .UNSPECIFIED., .F., .F.,
 ( 4, 2, 2, 2, 2, 2, 2, 2, 2, 2, 2, 2, 2, 2, 2, 2, 4 ),
 ( 0.01263889472610567159, 0.01342810546992894739, 0.01421731621375222493, 0.01500652695757550073, 0.01579573770139877653, 0.01658494844522205580, 0.01737415918904533160, 0.01816336993286860740, 0.01895258067669188320, 0.01974179142051515901, 0.02053100216433843828, 0.02132021290816171408, 0.02210942365198498988, 0.02289863439580826915, 0.02368784513963154148, 0.02447705588345482075, 0.02526626662727809655 ),
 .UNSPECIFIED. ) ;
#53749=CARTESIAN_POINT ( 'NONE',  ( 9.999999999999998224, 15.11738935797198913, 0.3539438260532097869 ) ) ;
#53755=VECTOR ( 'NONE', #66473, 1000.000000000000000 ) ;
#53760=EDGE_CURVE ( 'NONE', #64846, #3711, #78541, .T. ) ;
#53794=VERTEX_POINT ( 'NONE', #17748 ) ;
#53863=CARTESIAN_POINT ( 'NONE',  ( -8.000000000000000000, -23.84374999999999645, -3.313708498984762496 ) ) ;
#53875=EDGE_CURVE ( 'NONE', #43496, #67063, #69401, .T. ) ;
#53884=ORIENTED_EDGE ( 'NONE', *, *, #22361, .T. ) ;
#53926=CARTESIAN_POINT ( 'NONE',  ( -9.482945380845299255, 102.5566694122106810, 3.177595346755238914 ) ) ;
#53928=CARTESIAN_POINT ( 'NONE',  ( 2.918503601030701056, 15.30040232763830765, -9.571198553003721798 ) ) ;
#53939=CARTESIAN_POINT ( 'NONE',  ( 5.082755093536324154, -13.71875000204838457, 5.082755093536326818 ) ) ;
#53941=CARTESIAN_POINT ( 'NONE',  ( -1.469576158976823947E-15, -20.37499999999999289, 8.000000000000000000 ) ) ;
#53961=CARTESIAN_POINT ( 'NONE',  ( 7.999999999999998224, -17.28125000409677625, 3.313708498984766049 ) ) ;
#53966=AXIS2_PLACEMENT_3D ( 'NONE', #52068, #35943, #77421 ) ;
#53975=CARTESIAN_POINT ( 'NONE',  ( 8.000000000000000000, -21.49999999999999645, 0.000000000000000000 ) ) ;
#53979=CARTESIAN_POINT ( 'NONE',  ( -5.082755093536325042, -14.46875000204838457, -5.082755093536325930 ) ) ;
#53985=CARTESIAN_POINT ( 'NONE',  ( 9.989690267985803729, 88.97444416594913719, -0.5238310916885796642 ) ) ;
#54003=FACE_BOUND ( 'NONE', #30472, .T. ) ;
#54005=CARTESIAN_POINT ( 'NONE',  ( 7.188101187499999156, -19.25000000204838813, 2.977408999572654924 ) ) ;
#54049=CARTESIAN_POINT ( 'NONE',  ( -2.977408999572650039, -17.56250000204838813, -7.188101187500000933 ) ) ;
#54059=CARTESIAN_POINT ( 'NONE',  ( 7.188101187499999156, -31.62500000204838813, 2.977408999572654924 ) ) ;
#54064=CARTESIAN_POINT ( 'NONE',  ( -6.928203230275509661, 105.2693092969554129, -4.000000000000002665 ) ) ;
#54079=ADVANCED_FACE ( 'NONE', ( #46791 ), #102371, .T. ) ;
#54104=CARTESIAN_POINT ( 'NONE',  ( 7.188101187500000044, -30.03125000204838813, 0.000000000000000000 ) ) ;
#54117=CARTESIAN_POINT ( 'NONE',  ( -5.082755093536325042, -17.09375000204838813, -5.082755093536325930 ) ) ;
#54121=CARTESIAN_POINT ( 'NONE',  ( -9.537291425704609082, 82.35595622667227644, 3.012810007365997134 ) ) ;
#54124=CARTESIAN_POINT ( 'NONE',  ( -8.000000000000000000, -13.43750000409676915, -9.797174393178825657E-16 ) ) ;
#54142=CARTESIAN_POINT ( 'NONE',  ( 0.000000000000000000, 115.0000000000000000, 0.000000000000000000 ) ) ;
#54172=CARTESIAN_POINT ( 'NONE',  ( -6.928203230275508773, 105.0000000000000000, 4.000000000000001776 ) ) ;
#54177=LINE ( 'NONE', #3536, #61932 ) ;
#54190=CARTESIAN_POINT ( 'NONE',  ( 7.188101187499999156, -22.25000000204839168, 2.977408999572654924 ) ) ;
#54191=VERTEX_POINT ( 'NONE', #23605 ) ;
#54248=AXIS2_PLACEMENT_3D ( 'NONE', #55413, #76648, #79175 ) ;
#54260=PRESENTATION_STYLE_ASSIGNMENT (( #96359 ) ) ;
#54273=DIRECTION ( 'NONE',  ( -0.000000000000000000, -1.000000000000000000, -0.000000000000000000 ) ) ;
#54359=CARTESIAN_POINT ( 'NONE',  ( -3.313708498984765161, -10.15625000409677092, 7.999999999999998224 ) ) ;
#54367=CARTESIAN_POINT ( 'NONE',  ( -3.313708498984760720, -21.03124999999999645, -8.000000000000000000 ) ) ;
#54394=FACE_OUTER_BOUND ( 'NONE', #6775, .T. ) ;
#54420=CARTESIAN_POINT ( 'NONE',  ( -9.334514330295430540, 28.21377262318213042, -3.588704711590614771 ) ) ;
#54437=CARTESIAN_POINT ( 'NONE',  ( -9.797372177749755551, 101.5349050515243619, 2.014953862275849161 ) ) ;
#54452=CARTESIAN_POINT ( 'NONE',  ( 9.165151389911681434, 85.00000000000001421, -4.000000000000000000 ) ) ;
#54453=CARTESIAN_POINT ( 'NONE',  ( -7.188101187500000044, -15.78125000204838635, -8.802885111219163269E-16 ) ) ;
#54461=CARTESIAN_POINT ( 'NONE',  ( 5.656854249492378806, -24.68749999999999289, 5.656854249492381470 ) ) ;
#54491=CARTESIAN_POINT ( 'NONE',  ( 7.551892080562057075, 33.00987702539382695, 2.647003822403975359 ) ) ;
#54492=CARTESIAN_POINT ( 'NONE',  ( -7.003653396366583905, 28.94293794440322642, -3.866846144092863202 ) ) ;
#54500=CARTESIAN_POINT ( 'NONE',  ( 4.401442555609581635E-16, -11.65625000204838635, -7.188101187500000044 ) ) ;
#54525=CARTESIAN_POINT ( 'NONE',  ( 2.977408999572650927, -21.87500000204838813, -7.188101187500001821 ) ) ;
#54539=DIRECTION ( 'NONE',  ( -0.8660191070795881796, -2.771849051803015643E-05, -0.5000109052858326963 ) ) ;
#54578=CARTESIAN_POINT ( 'NONE',  ( -7.188101187500000933, -18.87500000204838457, -2.977408999572651371 ) ) ;
#54581=CARTESIAN_POINT ( 'NONE',  ( -8.000000000000000000, -27.03125000409677270, -3.313708498984762496 ) ) ;
#54587=CARTESIAN_POINT ( 'NONE',  ( 7.188101187500001821, -31.43750000204839168, -2.977408999572650483 ) ) ;
#54592=CARTESIAN_POINT ( 'NONE',  ( -7.002619243997878939, 106.0500731801381704, -3.868708944012999140 ) ) ;
#54628=CARTESIAN_POINT ( 'NONE',  ( -5.082755093536325042, -29.46875000204838813, -5.082755093536325930 ) ) ;
#54646=CARTESIAN_POINT ( 'NONE',  ( -7.188101187500000933, -21.50000000204839523, -2.977408999572651371 ) ) ;
#54648=FACE_OUTER_BOUND ( 'NONE', #41453, .T. ) ;
#54649=ORIENTED_EDGE ( 'NONE', *, *, #16241, .F. ) ;
#54653=CARTESIAN_POINT ( 'NONE',  ( -9.165151389911683211, 84.73289218717086158, -3.999999999999998224 ) ) ;
#54656=CARTESIAN_POINT ( 'NONE',  ( -5.656854249492381470, -10.25000000409677092, 5.656854249492379694 ) ) ;
#54658=FACE_OUTER_BOUND ( 'NONE', #15850, .T. ) ;
#54673=CARTESIAN_POINT ( 'NONE',  ( 7.122964895856751077, -30.00000000000000355, -0.9654893961775683486 ) ) ;
#54676=DIRECTION ( 'NONE',  ( -1.734723475976807094E-16, -0.000000000000000000, -1.000000000000000000 ) ) ;
#54721=CARTESIAN_POINT ( 'NONE',  ( -2.977408999572654480, -25.62500000204838813, 7.188101187499999156 ) ) ;
#54728=CARTESIAN_POINT ( 'NONE',  ( 4.898587196589412829E-16, -13.81250000409676915, -8.000000000000000000 ) ) ;
#54749=ORIENTED_EDGE ( 'NONE', *, *, #44874, .T. ) ;
#54792=CARTESIAN_POINT ( 'NONE',  ( -1.469576158976823947E-15, -29.56250000409677270, 8.000000000000000000 ) ) ;
#54796=CARTESIAN_POINT ( 'NONE',  ( 0.000000000000000000, 15.00000000000000000, 0.000000000000000000 ) ) ;
#54812=EDGE_CURVE ( 'NONE', #28267, #41081, #94661, .T. ) ;
#54822=VERTEX_POINT ( 'NONE', #39068 ) ;
#54845=VERTEX_POINT ( 'NONE', #47130 ) ;
#54916=CARTESIAN_POINT ( 'NONE',  ( -8.000000000000000000, -16.34374999999999289, -3.313708498984762496 ) ) ;
#54960=CARTESIAN_POINT ( 'NONE',  ( 8.000000000000000000, -27.68750000409677270, 0.000000000000000000 ) ) ;
#54969=EDGE_LOOP ( 'NONE', ( #30971, #64466, #5776, #49128 ) ) ;
#54972=ORIENTED_EDGE ( 'NONE', *, *, #68350, .T. ) ;
#54974=CARTESIAN_POINT ( 'NONE',  ( -9.606080321247050691, 15.83563386295778308, -2.802461721338014300 ) ) ;
#54995=CARTESIAN_POINT ( 'NONE',  ( 7.188101187500001821, -10.43750000204838457, -2.977408999572650483 ) ) ;
#55021=CARTESIAN_POINT ( 'NONE',  ( 3.313708498984799800, -16.90625000409677270, -7.999999999999961808 ) ) ;
#55039=CARTESIAN_POINT ( 'NONE',  ( 8.000000000000000000, -30.49999999999999645, 0.000000000000000000 ) ) ;
#55059=VECTOR ( 'NONE', #49767, 1000.000000000000000 ) ;
#55066=CARTESIAN_POINT ( 'NONE',  ( -2.977408999572654480, -19.62500000204838457, 7.188101187499999156 ) ) ;
#55116=CARTESIAN_POINT ( 'NONE',  ( -2.977408999572650039, -22.06250000204838813, -7.188101187500000933 ) ) ;
#55125=CARTESIAN_POINT ( 'NONE',  ( -5.082755093536326818, -24.59375000204838813, 5.082755093536325042 ) ) ;
#55142=AXIS2_PLACEMENT_3D ( 'NONE', #76675, #50274, #9805 ) ;
#55167=CARTESIAN_POINT ( 'NONE',  ( 7.188101187499999156, -30.12500000204838813, 2.977408999572654924 ) ) ;
#55183=CARTESIAN_POINT ( 'NONE',  ( -1.320432766682874540E-15, -10.53125000204838457, 7.188101187500000044 ) ) ;
#55194=CARTESIAN_POINT ( 'NONE',  ( 5.656854249492378806, -11.37500000409677092, 5.656854249492381470 ) ) ;
#55197=CARTESIAN_POINT ( 'NONE',  ( 9.341953373613241851, 15.21714514899092485, 3.572352985695210759 ) ) ;
#55235=CARTESIAN_POINT ( 'NONE',  ( -1.469576158976823947E-15, -26.37499999999999645, 8.000000000000000000 ) ) ;
#55257=CARTESIAN_POINT ( 'NONE',  ( 5.082755093536325930, -18.96875000204838457, -5.082755093536325042 ) ) ;
#55259=CARTESIAN_POINT ( 'NONE',  ( -3.313708498984798467, -24.03124999999998934, -7.999999999999961808 ) ) ;
#55305=CARTESIAN_POINT ( 'NONE',  ( 4.898587196589412829E-16, -12.12499999999999289, -8.000000000000000000 ) ) ;
#55322=CARTESIAN_POINT ( 'NONE',  ( -3.313708498984760720, -28.71875000409677625, -8.000000000000000000 ) ) ;
#55403=ORIENTED_EDGE ( 'NONE', *, *, #96884, .T. ) ;
#55413=CARTESIAN_POINT ( 'NONE',  ( -10.00000000000000355, 85.00000000000000000, 0.000000000000000000 ) ) ;
#55419=EDGE_CURVE ( 'NONE', #47033, #45637, #59366, .T. ) ;
#55427=CARTESIAN_POINT ( 'NONE',  ( 5.656854249492378806, -24.87500000409677270, 5.656854249492381470 ) ) ;
#55441=CARTESIAN_POINT ( 'NONE',  ( -5.656854249492381470, -13.06249999999999467, 5.656854249492379694 ) ) ;
#55463=AXIS2_PLACEMENT_3D ( 'NONE', #91462, #101136, #35918 ) ;
#55482=CARTESIAN_POINT ( 'NONE',  ( 3.313708498984742512, -27.40625000409677270, -8.000000000000019540 ) ) ;
#55497=CARTESIAN_POINT ( 'NONE',  ( -9.435590127033085750, 15.92795519102023860, -3.316968746323878836 ) ) ;
#55502=CARTESIAN_POINT ( 'NONE',  ( 0.000000000000000000, 15.00000000000000000, -9.999999999999998224 ) ) ;
#55510=ORIENTED_EDGE ( 'NONE', *, *, #85792, .F. ) ;
#55517=DIRECTION ( 'NONE',  ( 1.000000000000000000, -0.000000000000000000, -0.000000000000000000 ) ) ;
#55556=CARTESIAN_POINT ( 'NONE',  ( -7.801777176595948049, 26.41172014187366202, -1.786991866639918491 ) ) ;
#55563=CARTESIAN_POINT ( 'NONE',  ( 4.898587196589412829E-16, -31.62499999999999289, -8.000000000000000000 ) ) ;
#55587=CARTESIAN_POINT ( 'NONE',  ( 5.082755093536325930, -20.46875000204838813, -5.082755093536325042 ) ) ;
#55632=CARTESIAN_POINT ( 'NONE',  ( -2.977408999572654480, -20.00000000204838457, 7.188101187499999156 ) ) ;
#55636=CARTESIAN_POINT ( 'NONE',  ( -3.313708498984779371, -27.21875000409677270, -7.999999999999981348 ) ) ;
#55643=CARTESIAN_POINT ( 'NONE',  ( 7.188101187499999156, -24.12500000204838457, 2.977408999572654924 ) ) ;
#55686=CARTESIAN_POINT ( 'NONE',  ( -2.977408999572654480, -26.00000000204839168, 7.188101187499999156 ) ) ;
#55690=SHAPE_REPRESENTATION ( '7. Anchor', ( #10728 ), #38490 ) ;
#55693=CARTESIAN_POINT ( 'NONE',  ( 4.898587196589412829E-16, -9.312500004096769146, -8.000000000000000000 ) ) ;
#55700=CARTESIAN_POINT ( 'NONE',  ( -2.977408999572654480, -13.62500000204838457, 7.188101187499999156 ) ) ;
#55706=CARTESIAN_POINT ( 'NONE',  ( 4.898587196589412829E-16, -12.31250000409676915, -8.000000000000000000 ) ) ;
#55707=DIRECTION ( 'NONE',  ( 0.000000000000000000, -0.000000000000000000, 1.000000000000000000 ) ) ;
#55712=CARTESIAN_POINT ( 'NONE',  ( -1.469576158976823947E-15, -11.56250000409677092, 8.000000000000000000 ) ) ;
#55717=CARTESIAN_POINT ( 'NONE',  ( -9.221249107921748234, 86.04821371498486826, 3.869340886054257300 ) ) ;
#55723=CARTESIAN_POINT ( 'NONE',  ( -3.827754797006214016, 15.98931925350938243, 9.240220675753590740 ) ) ;
#55745=ORIENTED_EDGE ( 'NONE', *, *, #42075, .T. ) ;
#55774=CARTESIAN_POINT ( 'NONE',  ( 2.977408999572651815, -17.93750000204838457, 7.188101187500000933 ) ) ;
#55776=CARTESIAN_POINT ( 'NONE',  ( 9.918010731619574472, 81.20848315156776209, -1.300854425901574185 ) ) ;
#55802=ORIENTED_EDGE ( 'NONE', *, *, #19549, .T. ) ;
#55836=CARTESIAN_POINT ( 'NONE',  ( 8.000000000000000000, -32.18750000409676915, 0.000000000000000000 ) ) ;
#55850=CARTESIAN_POINT ( 'NONE',  ( 0.000000000000000000, 15.00000000000000000, 10.00000000000000000 ) ) ;
#55859=FILL_AREA_STYLE_COLOUR ( '', #103681 ) ;
#55909=CARTESIAN_POINT ( 'NONE',  ( 0.000000000000000000, 16.00000000000000000, 0.000000000000000000 ) ) ;
#55922=CARTESIAN_POINT ( 'NONE',  ( 6.928203230275509661, 105.0000000000000000, 4.000000000000001776 ) ) ;
#55923=EDGE_LOOP ( 'NONE', ( #10598, #71020, #19641, #48200 ) ) ;
#55964=CARTESIAN_POINT ( 'NONE',  ( -8.000000000000001776, -14.65624999999999289, 3.313708498984758943 ) ) ;
#55986=CARTESIAN_POINT ( 'NONE',  ( 9.151133496029800085, 15.07443463110313076, -4.034557488804713543 ) ) ;
#56025=ORIENTED_EDGE ( 'NONE', *, *, #96434, .T. ) ;
#56028=CARTESIAN_POINT ( 'NONE',  ( -9.571198553003062770, 15.30040232763797547, -2.918503601031004813 ) ) ;
#56071=VERTEX_POINT ( 'NONE', #46496 ) ;
#56076=CARTESIAN_POINT ( 'NONE',  ( -7.744168461338430731, 26.53745938284842154, 2.019395720771554714 ) ) ;
#56083=CARTESIAN_POINT ( 'NONE',  ( -3.313708498984765161, -33.96875000000000000, 7.999999999999998224 ) ) ;
#56091=EDGE_LOOP ( 'NONE', ( #91241, #1057 ) ) ;
#56109=FACE_OUTER_BOUND ( 'NONE', #819, .T. ) ;
#56112=CARTESIAN_POINT ( 'NONE',  ( -7.188101187500002709, -16.81250000204838457, 2.977408999572648707 ) ) ;
#56119=CARTESIAN_POINT ( 'NONE',  ( -10.00000000000000355, 105.0000000000000000, 0.000000000000000000 ) ) ;
#56159=CARTESIAN_POINT ( 'NONE',  ( -7.188101187500000044, -20.28125000204838813, -8.802885111219163269E-16 ) ) ;
#56170=CARTESIAN_POINT ( 'NONE',  ( 2.977408999572651815, -27.31250000204838457, 7.188101187500000933 ) ) ;
#56177=CYLINDRICAL_SURFACE ( 'NONE', #15094, 8.000000000000000000 ) ;
#56212=CARTESIAN_POINT ( 'NONE',  ( 9.699016383038316036, 26.82361828551655947, 2.444973590251030782 ) ) ;
#56213=CARTESIAN_POINT ( 'NONE',  ( -2.977408999572650039, -28.06250000204838813, -7.188101187500001821 ) ) ;
#56217=APPLICATION_CONTEXT ( 'automotive_design' ) ;
#56226=CARTESIAN_POINT ( 'NONE',  ( 2.977408999572652260, -13.43750000204838457, 7.188101187500000044 ) ) ;
#56227=CARTESIAN_POINT ( 'NONE',  ( 7.801339272325195751, 26.41268528040299302, -1.788609912539669722 ) ) ;
#56234=EDGE_CURVE ( 'NONE', #101925, #93035, #65860, .T. ) ;
#56241=CARTESIAN_POINT ( 'NONE',  ( 7.999999999999998224, -12.78125000409676915, 3.313708498984766493 ) ) ;
#56248=CARTESIAN_POINT ( 'NONE',  ( -5.656854249492379694, -16.43749999999999289, -5.656854249492380582 ) ) ;
#56256=CARTESIAN_POINT ( 'NONE',  ( 1.224646799147354440E-15, 15.00000000000000000, 9.999999999999998224 ) ) ;
#56296=( GEOMETRIC_REPRESENTATION_CONTEXT ( 3 ) GLOBAL_UNCERTAINTY_ASSIGNED_CONTEXT ( ( #87933 ) ) GLOBAL_UNIT_ASSIGNED_CONTEXT ( ( #29028, #61892, #76981 ) ) REPRESENTATION_CONTEXT ( 'NONE', 'WORKASPACE' ) );
#56301=DIRECTION ( 'NONE',  ( -0.4165977904505313578, -0.000000000000000000, -0.9090909090909090606 ) ) ;
#56304=CARTESIAN_POINT ( 'NONE',  ( -5.082755093536326818, -16.71875000204838813, 5.082755093536325042 ) ) ;
#56326=CARTESIAN_POINT ( 'NONE',  ( -10.00000000000000355, 15.00000000000000000, -10.00000000000000000 ) ) ;
#56340=EDGE_CURVE ( 'NONE', #72737, #87634, #34065, .T. ) ;
#56354=ORIENTED_EDGE ( 'NONE', *, *, #41896, .T. ) ;
#56361=ORIENTED_EDGE ( 'NONE', *, *, #90603, .T. ) ;
#56372=CARTESIAN_POINT ( 'NONE',  ( -3.313708498984760720, -30.21875000409677980, -8.000000000000000000 ) ) ;
#56393=CARTESIAN_POINT ( 'NONE',  ( -9.999999999999998224, 15.00000000000000000, 1.734723475976807489E-15 ) ) ;
#56405=CARTESIAN_POINT ( 'NONE',  ( 3.313708498984722972, -12.21874999999999112, -8.000000000000040856 ) ) ;
#56435=CARTESIAN_POINT ( 'NONE',  ( 3.884543032213806146, 15.13241195026071928, 9.216463528758731982 ) ) ;
#56473=( BOUNDED_SURFACE ( )  B_SPLINE_SURFACE ( 3, 2, ( 
 ( #71691, #30211, #39881 ),
 ( #95996, #105141, #56570 ),
 ( #81372, #104599, #15055 ),
 ( #7483, #22122, #104068 ),
 ( #55497, #97040, #5896 ),
 ( #54974, #56028, #15589 ),
 ( #31797, #73281, #32339 ),
 ( #89494, #23181, #46378 ),
 ( #47944, #65209, #13457 ),
 ( #98103, #47421, #13988 ) ),
 .UNSPECIFIED., .F., .F., .F. ) 
 B_SPLINE_SURFACE_WITH_KNOTS ( ( 4, 2, 2, 2, 4 ),
 ( 3, 3 ),
 ( 0.002450517525418903411, 0.003060732775749471640, 0.003670948026080039436, 0.004891378526741175028, 0.007332239528063447080 ),
 ( 0.000000000000000000, 1.000000000000000000 ),
 .UNSPECIFIED. ) 
 GEOMETRIC_REPRESENTATION_ITEM ( )  RATIONAL_B_SPLINE_SURFACE ( (
 ( 1.000000000000000000, 0.7071067811865481278, 1.000000000000000000),
 ( 1.000000000000000000, 0.7344063550101934679, 1.000000000000000000),
 ( 1.000000000000000000, 0.7590375248711017653, 1.000000000000000000),
 ( 1.000000000000000000, 0.8038331608704095688, 1.000000000000000000),
 ( 1.000000000000000000, 0.8240352460866353645, 1.000000000000000000),
 ( 1.000000000000000000, 0.8791017378332343091, 1.000000000000000000),
 ( 1.000000000000000000, 0.9085032776980891400, 1.000000000000000000),
 ( 1.000000000000000000, 0.9784170511696808070, 1.000000000000000000),
 ( 1.000000000000000000, 0.9996598051696591325, 1.000000000000000000),
 ( 1.000000000000000000, 1.000000000000000000, 1.000000000000000000) ) ) 
 REPRESENTATION_ITEM ( '' )  SURFACE ( )  );
#56474=CARTESIAN_POINT ( 'NONE',  ( 6.928203230275507885, 104.7306907030446723, -4.000000000000001776 ) ) ;
#56504=CARTESIAN_POINT ( 'NONE',  ( 3.313708498984762496, -12.78124999999999289, 7.999999999999998224 ) ) ;
#56525=ORIENTED_EDGE ( 'NONE', *, *, #89578, .T. ) ;
#56529=CARTESIAN_POINT ( 'NONE',  ( 9.606080321247246090, 15.83563386295778308, -2.802461721337421885 ) ) ;
#56547=EDGE_CURVE ( 'NONE', #99482, #64846, #81984, .T. ) ;
#56570=CARTESIAN_POINT ( 'NONE',  ( -10.00000000000000000, 15.00000000000000000, -4.397168787612341312 ) ) ;
#56592=CARTESIAN_POINT ( 'NONE',  ( -7.188101187500001821, -11.37500000204838813, -2.977408999572651371 ) ) ;
#56634=CARTESIAN_POINT ( 'NONE',  ( -3.594029362035469966, -9.531975552779805128, 6.225090491435913975 ) ) ;
#56653=CARTESIAN_POINT ( 'NONE',  ( 7.344133061198929724, 107.4449439268058057, 3.176267128233876136 ) ) ;
#56658=CARTESIAN_POINT ( 'NONE',  ( -1.320432766682874540E-15, -13.53125000204838457, 7.188101187500000044 ) ) ;
#56683=CARTESIAN_POINT ( 'NONE',  ( 4.582575694955842494, 16.00000000000000000, -9.999999999999998224 ) ) ;
#56694=EDGE_CURVE ( 'NONE', #59320, #81173, #70354, .T. ) ;
#56709=CARTESIAN_POINT ( 'NONE',  ( -7.188101187500002709, -12.68750000204838635, 2.977408999572647819 ) ) ;
#56719=CARTESIAN_POINT ( 'NONE',  ( 2.977408999572651815, -28.81250000204838457, 7.188101187500000933 ) ) ;
#56748=VERTEX_POINT ( 'NONE', #53280 ) ;
#56758=CARTESIAN_POINT ( 'NONE',  ( -7.188101187500002709, -27.68750000204838813, 2.977408999572648707 ) ) ;
#56765=CARTESIAN_POINT ( 'NONE',  ( -10.00000000000000355, 85.00000000000000000, 4.000000000000000000 ) ) ;
#56775=CARTESIAN_POINT ( 'NONE',  ( -5.082755093536326818, -15.21875000204838457, 5.082755093536325042 ) ) ;
#56776=CARTESIAN_POINT ( 'NONE',  ( 7.414346147792000075, 27.35410842337735815, -3.010818766110528344 ) ) ;
#56777=( BOUNDED_CURVE ( )  B_SPLINE_CURVE ( 2, ( #101227, #78009, #4126, #35457, #36534, #3054, #102281, #37594, #44595 ),
 .UNSPECIFIED., .F., .F. ) 
 B_SPLINE_CURVE_WITH_KNOTS ( ( 3, 2, 2, 2, 3 ),
 ( 0.8676470588235293269, 0.8749999999999998890, 0.8823529411764705621, 0.8897058823529411242, 0.8970588235294117974 ),
 .UNSPECIFIED. ) 
 CURVE ( )  GEOMETRIC_REPRESENTATION_ITEM ( )  RATIONAL_B_SPLINE_CURVE ( ( 1.000000000000001110, 0.9238795325112856283, 1.000000000000000000, 0.9238795325112867385, 1.000000000000000000, 0.9238795325112867385, 1.000000000000000000, 0.9238795325112867385, 1.000000000000000000 ) ) 
 REPRESENTATION_ITEM ( '' )  );
#56787=CARTESIAN_POINT ( 'NONE',  ( 7.188101187500001821, -29.56250000204838813, -2.977408999572650483 ) ) ;
#56791=CARTESIAN_POINT ( 'NONE',  ( -9.843039827103245543, 88.59083502508335073, -1.781495459429540684 ) ) ;
#56795=CARTESIAN_POINT ( 'NONE',  ( -9.165151389911679658, 30.26319506294883510, 3.999999999999999112 ) ) ;
#56802=( BOUNDED_SURFACE ( )  B_SPLINE_SURFACE ( 3, 2, ( 
 ( #19865, #37634, #19341 ),
 ( #52170, #3098, #64011 ),
 ( #104433, #31642, #22504 ),
 ( #89330, #7321, #6259 ),
 ( #47257, #79629, #96888 ),
 ( #23553, #23023, #30582 ),
 ( #46219, #13827, #15423 ),
 ( #79107, #62410, #13291 ),
 ( #38156, #14884, #31127 ),
 ( #56393, #5229, #46739 ) ),
 .UNSPECIFIED., .F., .F., .T. ) 
 B_SPLINE_SURFACE_WITH_KNOTS ( ( 4, 2, 2, 2, 4 ),
 ( 3, 3 ),
 ( 0.002450517525418897339, 0.003060732775749461232, 0.003670948026080025559, 0.004891378526741153344, 0.007332239528063409784 ),
 ( 0.000000000000000000, 1.000000000000000000 ),
 .UNSPECIFIED. ) 
 GEOMETRIC_REPRESENTATION_ITEM ( )  RATIONAL_B_SPLINE_SURFACE ( (
 ( 1.000000000000000000, 0.7071067811865481278, 1.000000000000000000),
 ( 1.000000000000000000, 0.7344063550101943560, 1.000000000000000000),
 ( 1.000000000000000000, 0.7590375248711014322, 1.000000000000000000),
 ( 1.000000000000000000, 0.8038331608704090137, 1.000000000000000000),
 ( 1.000000000000000000, 0.8240352460866353645, 1.000000000000000000),
 ( 1.000000000000000000, 0.8791017378332339760, 1.000000000000000000),
 ( 1.000000000000000000, 0.9085032776980893621, 1.000000000000000000),
 ( 1.000000000000000000, 0.9784170511696805850, 1.000000000000000000),
 ( 1.000000000000000000, 0.9996598051696602427, 1.000000000000000000),
 ( 1.000000000000000000, 1.000000000000000000, 1.000000000000000000) ) ) 
 REPRESENTATION_ITEM ( '' )  SURFACE ( )  );
#56839=CARTESIAN_POINT ( 'NONE',  ( 7.151597709147950788, 86.78929265052215669, 3.587174531012138790 ) ) ;
#56850=CARTESIAN_POINT ( 'NONE',  ( 7.188101187499999156, -17.75000000204838457, 2.977408999572654924 ) ) ;
#56852=CARTESIAN_POINT ( 'NONE',  ( 9.989285784994814676, 81.02657572554299747, 0.5301777604595927507 ) ) ;
#56855=CARTESIAN_POINT ( 'NONE',  ( -8.000000000000001776, -13.34375000409676737, 3.313708498984759387 ) ) ;
#56865=DIRECTION ( 'NONE',  ( 1.000000000000000000, 0.000000000000000000, -0.000000000000000000 ) ) ;
#56910=CARTESIAN_POINT ( 'NONE',  ( -5.656854249492381470, -29.75000000409677270, 5.656854249492379694 ) ) ;
#56925=CARTESIAN_POINT ( 'NONE',  ( 3.313708498984761608, -15.40625000409677092, -8.000000000000000000 ) ) ;
#56958=CARTESIAN_POINT ( 'NONE',  ( -4.681884270554226291, -29.99999999999996803, 5.894723978655478369 ) ) ;
#56991=( NAMED_UNIT ( * ) SI_UNIT ( $, .STERADIAN. ) SOLID_ANGLE_UNIT ( ) );
#56994=DIRECTION ( 'NONE',  ( 0.000000000000000000, 0.000000000000000000, 1.000000000000000000 ) ) ;
#56997=ORIENTED_EDGE ( 'NONE', *, *, #37721, .F. ) ;
#57007=CARTESIAN_POINT ( 'NONE',  ( 7.150053860865848598, 103.2173454608602299, 3.590189269391292015 ) ) ;
#57033=DIRECTION ( 'NONE',  ( 0.000000000000000000, 0.000000000000000000, 1.000000000000000000 ) ) ;
#57037=CARTESIAN_POINT ( 'NONE',  ( -8.000000000000000000, -14.74999999999999289, -9.797174393178825657E-16 ) ) ;
#57072=CARTESIAN_POINT ( 'NONE',  ( -7.551560007654695816, 81.99089648193009339, -2.648022159607839043 ) ) ;
#57095=( BOUNDED_CURVE ( )  B_SPLINE_CURVE ( 2, ( #60057, #27704, #20689, #12517, #92913, #2838, #19080, #51917, #75665 ),
 .UNSPECIFIED., .F., .T. ) 
 B_SPLINE_CURVE_WITH_KNOTS ( ( 3, 2, 2, 2, 3 ),
 ( 0.3382352941176470229, 0.3455882352941175850, 0.3529411764705882026, 0.3602941176470588203, 0.3676470588235294379 ),
 .UNSPECIFIED. ) 
 CURVE ( )  GEOMETRIC_REPRESENTATION_ITEM ( )  RATIONAL_B_SPLINE_CURVE ( ( 1.000000000000000666, 0.9238795325112861834, 1.000000000000000000, 0.9238795325112867385, 1.000000000000000000, 0.9238795325112867385, 1.000000000000000000, 0.9238795325112867385, 1.000000000000000000 ) ) 
 REPRESENTATION_ITEM ( '' )  );
#57102=CARTESIAN_POINT ( 'NONE',  ( 9.090909090909088164, 16.00000000000000000, 4.165977904505314910 ) ) ;
#57104=CARTESIAN_POINT ( 'NONE',  ( -5.082755093536325042, -30.59375000204838813, -5.082755093536325930 ) ) ;
#57133=ORIENTED_EDGE ( 'NONE', *, *, #49663, .T. ) ;
#57165=CARTESIAN_POINT ( 'NONE',  ( -8.000000000000000000, -34.34375000000000000, -3.313708498984762496 ) ) ;
#57186=CARTESIAN_POINT ( 'NONE',  ( 5.082755093536324154, -16.34375000204838813, 5.082755093536326818 ) ) ;
#57195=DIRECTION ( 'NONE',  ( 0.000000000000000000, 0.000000000000000000, -1.000000000000000000 ) ) ;
#57204=CARTESIAN_POINT ( 'NONE',  ( -1.469576158976823947E-15, -16.06250000409677270, 8.000000000000000000 ) ) ;
#57229=EDGE_CURVE ( 'NONE', #24908, #35576, #20000, .T. ) ;
#57237=CARTESIAN_POINT ( 'NONE',  ( -2.977408999572654480, -11.00000000204838635, 7.188101187499999156 ) ) ;
#57239=CARTESIAN_POINT ( 'NONE',  ( -1.469576158976823947E-15, -29.37499999999999645, 8.000000000000000000 ) ) ;
#57245=CARTESIAN_POINT ( 'NONE',  ( 5.082755093536324154, -25.71875000204838813, 5.082755093536326818 ) ) ;
#57276=ORIENTED_EDGE ( 'NONE', *, *, #89865, .F. ) ;
#57285=CARTESIAN_POINT ( 'NONE',  ( 9.165151389911677882, 29.73264844392884143, -4.000000000000000000 ) ) ;
#57287=CARTESIAN_POINT ( 'NONE',  ( 2.977408999572650927, -23.75000000204839168, -7.188101187500001821 ) ) ;
#57297=CARTESIAN_POINT ( 'NONE',  ( 9.646032546913144046, 88.01280328474365433, 2.644051433538241902 ) ) ;
#57301=CARTESIAN_POINT ( 'NONE',  ( 7.188101187499999156, -11.75000000204838813, 2.977408999572654924 ) ) ;
#57308=ORIENTED_EDGE ( 'NONE', *, *, #68350, .F. ) ;
#57316=CARTESIAN_POINT ( 'NONE',  ( -1.320432766682874540E-15, -33.03125000204838813, 7.188101187500000044 ) ) ;
#57326=CARTESIAN_POINT ( 'NONE',  ( 9.090909090909089940, 16.00000000000000000, -4.165977904505312246 ) ) ;
#57343=VERTEX_POINT ( 'NONE', #57239 ) ;
#57365=CARTESIAN_POINT ( 'NONE',  ( 6.928203230275508773, 85.26883324508999351, -4.000000000000001776 ) ) ;
#57376=CARTESIAN_POINT ( 'NONE',  ( -5.082755093536326818, -19.71875000204838457, 5.082755093536325042 ) ) ;
#57380=CIRCLE ( 'NONE', #46990, 1.000000000000000444 ) ;
#57381=CARTESIAN_POINT ( 'NONE',  ( 9.482856158761270748, 82.55692884145280175, 3.177891129109650770 ) ) ;
#57413=DIRECTION ( 'NONE',  ( 0.000000000000000000, 0.000000000000000000, 1.000000000000000000 ) ) ;
#57437=CARTESIAN_POINT ( 'NONE',  ( -8.000000000000000000, -25.53125000409676915, -3.313708498984762496 ) ) ;
#57446=CARTESIAN_POINT ( 'NONE',  ( -2.918503601031048333, 15.30040232763797192, -9.571198553003716469 ) ) ;
#57495=CARTESIAN_POINT ( 'NONE',  ( -8.000000000000000000, -22.34374999999999645, -3.313708498984762496 ) ) ;
#57500=EDGE_CURVE ( 'NONE', #68507, #62602, #84340, .T. ) ;
#57541=CARTESIAN_POINT ( 'NONE',  ( 9.177080501238306098, 105.5334694285426878, -3.972956046786646489 ) ) ;
#57560=CARTESIAN_POINT ( 'NONE',  ( 3.313708498984762052, -10.71874999999999289, -8.000000000000000000 ) ) ;
#57575=CARTESIAN_POINT ( 'NONE',  ( -3.979266480701241449, -30.00000000000000000, -6.940132439339150139 ) ) ;
#57580=CARTESIAN_POINT ( 'NONE',  ( -1.469576158976823947E-15, -29.56250000409677270, 8.000000000000000000 ) ) ;
#57594=CARTESIAN_POINT ( 'NONE',  ( -7.999885325681426629, 81.00022934870064262, 0.2682325777720090954 ) ) ;
#57627=CARTESIAN_POINT ( 'NONE',  ( 5.082755093536325930, -29.46875000204838813, -5.082755093536325042 ) ) ;
#57630=CARTESIAN_POINT ( 'NONE',  ( 0.7768758660237293778, 15.00000000000000000, -9.999999999999998224 ) ) ;
#57682=CARTESIAN_POINT ( 'NONE',  ( 6.928203230275510549, 30.00000000000000355, -4.000000000000000000 ) ) ;
#57690=CARTESIAN_POINT ( 'NONE',  ( -1.469576158976823947E-15, -27.87499999999999645, 8.000000000000000000 ) ) ;
#57711=CARTESIAN_POINT ( 'NONE',  ( -1.320432766682874540E-15, -15.03125000204838457, 7.188101187500000044 ) ) ;
#57717=ORIENTED_EDGE ( 'NONE', *, *, #13889, .F. ) ;
#57731=VERTEX_POINT ( 'NONE', #69561 ) ;
#57768=CARTESIAN_POINT ( 'NONE',  ( -7.188101187500000933, -11.37500000204838635, -2.977408999572651371 ) ) ;
#57771=CARTESIAN_POINT ( 'NONE',  ( 5.112876467197158270, -29.99999999999999289, 5.074076696858962343 ) ) ;
#57777=CARTESIAN_POINT ( 'NONE',  ( -7.188101187500002709, -20.18750000204838457, 2.977408999572648707 ) ) ;
#57795=CARTESIAN_POINT ( 'NONE',  ( -7.744991119775238353, 88.46438785425129936, -2.016316005557097224 ) ) ;
#57821=CARTESIAN_POINT ( 'NONE',  ( -5.082755093536325042, -23.46875000204838457, -5.082755093536325930 ) ) ;
#57828=CARTESIAN_POINT ( 'NONE',  ( 9.176803346051512378, 85.52947155797443202, 3.973598758023530131 ) ) ;
#57833=CARTESIAN_POINT ( 'NONE',  ( 7.212408192734265810, 27.98482910679631530, -3.465038817813886229 ) ) ;
#57845=CARTESIAN_POINT ( 'NONE',  ( -5.082755093536326818, -30.21875000204838813, 5.082755093536325042 ) ) ;
#57853=CARTESIAN_POINT ( 'NONE',  ( -9.699016383038316036, 33.17638171448344764, 2.444973590251029449 ) ) ;
#57897=ORIENTED_EDGE ( 'NONE', *, *, #44988, .F. ) ;
#57899=CARTESIAN_POINT ( 'NONE',  ( 7.986468734911285949, 88.97313679723080782, 0.5341897780976110344 ) ) ;
#57903=DIRECTION ( 'NONE',  ( 0.4165977904505305252, 0.000000000000000000, 0.9090909090909092827 ) ) ;
#57909=CARTESIAN_POINT ( 'NONE',  ( -5.082755093536326818, -12.21875000204838635, 5.082755093536325042 ) ) ;
#57912=CARTESIAN_POINT ( 'NONE',  ( 9.333079356992099562, 83.22166919925130912, 3.592383266237784589 ) ) ;
#57935=ORIENTED_EDGE ( 'NONE', *, *, #50187, .F. ) ;
#57970=CARTESIAN_POINT ( 'NONE',  ( -7.188101187500000933, -29.00000000204838813, -2.977408999572651371 ) ) ;
#57979=CARTESIAN_POINT ( 'NONE',  ( -1.469576158976823947E-15, -26.56250000409677270, 8.000000000000000000 ) ) ;
#57981=CARTESIAN_POINT ( 'NONE',  ( 0.000000000000000000, -30.00000000000000000, 0.000000000000000000 ) ) ;
#57985=CARTESIAN_POINT ( 'NONE',  ( 9.221216839714866609, 31.04759748168974198, 3.869414262756994294 ) ) ;
#57988=CARTESIAN_POINT ( 'NONE',  ( -4.210530276627872937, 14.99999999999998934, -10.00000000000003908 ) ) ;
#58042=PRESENTATION_STYLE_ASSIGNMENT (( #66139 ) ) ;
#58074=CARTESIAN_POINT ( 'NONE',  ( 7.550180524134850302, 101.9944075278681197, 2.651855549982494065 ) ) ;
#58088=ORIENTED_EDGE ( 'NONE', *, *, #49927, .T. ) ;
#58111=CARTESIAN_POINT ( 'NONE',  ( -7.045755811259131640, 103.6965839698644203, 3.790843699961854885 ) ) ;
#58128=DIRECTION ( 'NONE',  ( -0.000000000000000000, 1.000000000000000000, -0.000000000000000000 ) ) ;
#58143=CARTESIAN_POINT ( 'NONE',  ( -7.986468734911287726, 81.02686320276922061, 0.5341897780976151422 ) ) ;
#58149=ORIENTED_EDGE ( 'NONE', *, *, #76286, .T. ) ;
#58175=CARTESIAN_POINT ( 'NONE',  ( -1.320432766682874540E-15, -33.03125000204838813, 7.188101187500000044 ) ) ;
#58179=( GEOMETRIC_REPRESENTATION_CONTEXT ( 3 ) GLOBAL_UNCERTAINTY_ASSIGNED_CONTEXT ( ( #13570 ) ) GLOBAL_UNIT_ASSIGNED_CONTEXT ( ( #31284, #87905, #38827 ) ) REPRESENTATION_CONTEXT ( 'NONE', 'WORKASPACE' ) );
#58235=CARTESIAN_POINT ( 'NONE',  ( 8.000000000000000000, -22.90624999999999645, -3.313708498984761164 ) ) ;
#58236=CARTESIAN_POINT ( 'NONE',  ( 5.656854249492380582, -27.31249999999999645, -5.656854249492379694 ) ) ;
#58245=VERTEX_POINT ( 'NONE', #101273 ) ;
#58265=CARTESIAN_POINT ( 'NONE',  ( 4.401442555609581635E-16, -11.28125000204838457, -7.188101187500000044 ) ) ;
#58288=APPLICATION_CONTEXT ( 'automotive_design' ) ;
#58296=EDGE_LOOP ( 'NONE', ( #69159, #13343, #28546, #45698 ) ) ;
#58319=CARTESIAN_POINT ( 'NONE',  ( -7.188101187500000933, -14.37500000204838280, -2.977408999572651371 ) ) ;
#58327=CARTESIAN_POINT ( 'NONE',  ( 7.188101187500000044, -21.03125000204838813, 0.000000000000000000 ) ) ;
#58347=ORIENTED_EDGE ( 'NONE', *, *, #16596, .T. ) ;
#58367=CARTESIAN_POINT ( 'NONE',  ( 9.537909130738274399, 27.35385169036606356, -3.010726932293859903 ) ) ;
#58369=CARTESIAN_POINT ( 'NONE',  ( -7.188101187500002709, -17.18750000204838813, 2.977408999572648707 ) ) ;
#58401=CARTESIAN_POINT ( 'NONE',  ( 7.188101187500000044, -32.65625000204838813, 0.000000000000000000 ) ) ;
#58452=CARTESIAN_POINT ( 'NONE',  ( 7.801777176595948937, 88.58827985812634154, -1.786991866639919380 ) ) ;
#58462=CARTESIAN_POINT ( 'NONE',  ( 7.188101187499999156, -14.75000000204838457, 2.977408999572654924 ) ) ;
#58490=ORIENTED_EDGE ( 'NONE', *, *, #16074, .T. ) ;
#58502=CARTESIAN_POINT ( 'NONE',  ( 7.551437640244097693, 81.99127537477092176, -2.648272645923386293 ) ) ;
#58524=CARTESIAN_POINT ( 'NONE',  ( 4.401442555609581635E-16, -23.28125000204838457, -7.188101187500000044 ) ) ;
#58529=( NAMED_UNIT ( * ) SI_UNIT ( $, .STERADIAN. ) SOLID_ANGLE_UNIT ( ) );
#58537=CARTESIAN_POINT ( 'NONE',  ( -3.313708498984765161, -25.15625000409677270, 7.999999999999998224 ) ) ;
#58577=CARTESIAN_POINT ( 'NONE',  ( -7.150053860865850375, 31.78265453913976657, 3.590189269391290239 ) ) ;
#58595=CARTESIAN_POINT ( 'NONE',  ( 4.397168787612346641, 15.00000000000000000, 9.999999999999998224 ) ) ;
#58654=DIRECTION ( 'NONE',  ( -0.000000000000000000, 1.000000000000000000, -0.000000000000000000 ) ) ;
#58695=CARTESIAN_POINT ( 'NONE',  ( -7.003653396366583017, 83.94293794440324064, -3.866846144092864535 ) ) ;
#58729=CARTESIAN_POINT ( 'NONE',  ( 7.188101187499999156, -32.75000000204839523, 2.977408999572654924 ) ) ;
#58740=CARTESIAN_POINT ( 'NONE',  ( 3.313708498984780260, -27.21874999999999289, -7.999999999999981348 ) ) ;
#58788=CARTESIAN_POINT ( 'NONE',  ( -3.313708498984765161, -24.96874999999999645, 7.999999999999998224 ) ) ;
#58799=LINE ( 'NONE', #12748, #80739 ) ;
#58815=CARTESIAN_POINT ( 'NONE',  ( -9.165151389911679658, 85.00000000000000000, 4.000000000000000000 ) ) ;
#58816=CARTESIAN_POINT ( 'NONE',  ( 7.188101187500001821, -11.56250000204838635, -2.977408999572650483 ) ) ;
#58877=CARTESIAN_POINT ( 'NONE',  ( -2.977408999572654480, -23.00000000204839523, 7.188101187499999156 ) ) ;
#58893=ORIENTED_EDGE ( 'NONE', *, *, #90747, .T. ) ;
#58903=CARTESIAN_POINT ( 'NONE',  ( -3.594033448928638297, -9.156975712238446974, 6.225088131883843801 ) ) ;
#58906=CARTESIAN_POINT ( 'NONE',  ( -8.000000000000001776, -25.34375000409676915, 3.313708498984759387 ) ) ;
#58916=CARTESIAN_POINT ( 'NONE',  ( 2.977408999572651815, -21.31250000204838813, 7.188101187500000933 ) ) ;
#58919=CARTESIAN_POINT ( 'NONE',  ( -8.000000000000000000, -11.93750000409677092, -9.797174393178825657E-16 ) ) ;
#58929=CARTESIAN_POINT ( 'NONE',  ( 4.401442555609581635E-16, -9.781250002048384573, -7.188101187500000044 ) ) ;
#58941=CARTESIAN_POINT ( 'NONE',  ( 2.977408999572650927, -33.87500000204838813, -7.188101187500001821 ) ) ;
#58998=CARTESIAN_POINT ( 'NONE',  ( 2.977408999572651815, -13.43750000204838457, 7.188101187500000933 ) ) ;
#58999=CARTESIAN_POINT ( 'NONE',  ( -5.656854249492379694, -18.12500000409676915, -5.656854249492380582 ) ) ;
#59036=CARTESIAN_POINT ( 'NONE',  ( 8.000086790516061086, 80.99982641893991797, 0.2639471549312809029 ) ) ;
#59056=CARTESIAN_POINT ( 'NONE',  ( 2.977408999572650927, -23.37500000204838457, -7.188101187500000933 ) ) ;
#59066=CARTESIAN_POINT ( 'NONE',  ( -8.000000000000000000, -20.93750000409676915, -9.797174393178825657E-16 ) ) ;
#59071=CARTESIAN_POINT ( 'NONE',  ( 9.177080501238306098, 30.53346942854269841, -3.972956046786646489 ) ) ;
#59074=CARTESIAN_POINT ( 'NONE',  ( -2.563280883359797091, 15.30085158940939394, -9.673800154114783112 ) ) ;
#59078=LINE ( 'NONE', #85482, #79004 ) ;
#59101=CARTESIAN_POINT ( 'NONE',  ( -1.469576158976823947E-15, -11.37499999999999289, 8.000000000000000000 ) ) ;
#59119=DIRECTION ( 'NONE',  ( 0.000000000000000000, 0.000000000000000000, 1.000000000000000000 ) ) ;
#59129=CARTESIAN_POINT ( 'NONE',  ( -0.7018335428337032500, 15.23280014800325866, 9.981531048852463783 ) ) ;
#59190=CARTESIAN_POINT ( 'NONE',  ( -1.469576158976823947E-15, -20.37499999999999289, 8.000000000000000000 ) ) ;
#59203=CARTESIAN_POINT ( 'NONE',  ( 1.400881274228121143, 15.45483377860037955, -9.907626560209529032 ) ) ;
#59232=CARTESIAN_POINT ( 'NONE',  ( -7.801642220026313801, 81.41203173850969677, 1.787233835843583307 ) ) ;
#59239=CARTESIAN_POINT ( 'NONE',  ( 0.000000000000000000, -30.00000000000000000, 0.000000000000000000 ) ) ;
#59317=CARTESIAN_POINT ( 'NONE',  ( 3.313708498984762496, -24.78124999999999289, 7.999999999999998224 ) ) ;
#59320=VERTEX_POINT ( 'NONE', #79647 ) ;
#59339=CARTESIAN_POINT ( 'NONE',  ( 7.897196874019792645, 108.7912720416780559, -1.302055520192085369 ) ) ;
#59341=EDGE_CURVE ( 'NONE', #93999, #40311, #7633, .T. ) ;
#59347=CYLINDRICAL_SURFACE ( 'NONE', #100803, 8.000000000000000000 ) ;
#59355=UNCERTAINTY_MEASURE_WITH_UNIT (LENGTH_MEASURE( 1.000000000000000082E-05 ), #38317, 'distance_accuracy_value', 'NONE');
#59366=LINE ( 'NONE', #42628, #83376 ) ;
#59411=CARTESIAN_POINT ( 'NONE',  ( -7.188101187500000044, -23.28125000204838457, -8.802885111219163269E-16 ) ) ;
#59452=CARTESIAN_POINT ( 'NONE',  ( 5.082755093536325930, -20.84375000204838813, -5.082755093536325042 ) ) ;
#59473=ORIENTED_EDGE ( 'NONE', *, *, #89865, .T. ) ;
#59480=CARTESIAN_POINT ( 'NONE',  ( -2.977408999572654480, -25.62500000204838813, 7.188101187499999156 ) ) ;
#59530=CARTESIAN_POINT ( 'NONE',  ( 7.188101187500000044, -22.53125000204838457, 0.000000000000000000 ) ) ;
#59539=CARTESIAN_POINT ( 'NONE',  ( -7.188101187500002709, -13.81250000204838280, 2.977408999572648707 ) ) ;
#59540=CARTESIAN_POINT ( 'NONE',  ( -3.313708498984765161, -17.65625000409676559, 7.999999999999998224 ) ) ;
#59545=CARTESIAN_POINT ( 'NONE',  ( -3.313708498984798467, -15.03124999999999289, -7.999999999999961808 ) ) ;
#59574=CARTESIAN_POINT ( 'NONE',  ( 5.656854249492378806, -11.18749999999999289, 5.656854249492381470 ) ) ;
#59593=CARTESIAN_POINT ( 'NONE',  ( -7.188101187500000044, -25.90625000204838813, -8.802885111219163269E-16 ) ) ;
#59603=CARTESIAN_POINT ( 'NONE',  ( 3.313708498984762496, -24.96875000409677270, 7.999999999999998224 ) ) ;
#59631=( NAMED_UNIT ( * ) PLANE_ANGLE_UNIT ( ) SI_UNIT ( $, .RADIAN. ) );
#59658=ORIENTED_EDGE ( 'NONE', *, *, #8488, .T. ) ;
#59742=CARTESIAN_POINT ( 'NONE',  ( 4.898587196589412829E-16, -18.12499999999999645, -8.000000000000000000 ) ) ;
#59746=DIRECTION ( 'NONE',  ( 0.000000000000000000, 0.000000000000000000, 1.000000000000000000 ) ) ;
#59748=CARTESIAN_POINT ( 'NONE',  ( -8.000000000000000000, -29.93750000409677270, -9.797174393178825657E-16 ) ) ;
#59764=CARTESIAN_POINT ( 'NONE',  ( -9.948561005166130400, 108.8699027374820076, -1.045755304005130393 ) ) ;
#59785=ORIENTED_EDGE ( 'NONE', *, *, #53247, .F. ) ;
#59832=ORIENTED_EDGE ( 'NONE', *, *, #4912, .F. ) ;
#59859=CARTESIAN_POINT ( 'NONE',  ( 5.656854249492380582, -24.31249999999999289, -5.656854249492379694 ) ) ;
#59886=FACE_OUTER_BOUND ( 'NONE', #55923, .T. ) ;
#59922=ORIENTED_EDGE ( 'NONE', *, *, #95483, .F. ) ;
#59953=CARTESIAN_POINT ( 'NONE',  ( -5.082755093536326818, -18.59375000204838457, 5.082755093536325042 ) ) ;
#59978=CARTESIAN_POINT ( 'NONE',  ( 9.999999999999998224, 15.00000000000000000, -1.734723475976806897E-15 ) ) ;
#59997=CARTESIAN_POINT ( 'NONE',  ( 9.482856158761276077, 27.55692884145275201, 3.177891129109640556 ) ) ;
#59999=CARTESIAN_POINT ( 'NONE',  ( 7.188101187500000044, -18.03125000204838457, 0.000000000000000000 ) ) ;
#60003=DIRECTION ( 'NONE',  ( 0.000000000000000000, 0.000000000000000000, 1.000000000000000000 ) ) ;
#60025=CARTESIAN_POINT ( 'NONE',  ( 2.977408999572651815, -26.93750000204838457, 7.188101187500000933 ) ) ;
#60043=CARTESIAN_POINT ( 'NONE',  ( -5.656854249492379694, -22.62500000409676915, -5.656854249492380582 ) ) ;
#60044=CARTESIAN_POINT ( 'NONE',  ( 9.483056940782029542, 102.5561220989342388, -3.177305548492599829 ) ) ;
#60057=CARTESIAN_POINT ( 'NONE',  ( -1.469576158976823947E-15, -26.37499999999999645, 8.000000000000000000 ) ) ;
#60075=CARTESIAN_POINT ( 'NONE',  ( -7.188101187500000933, -26.37500000204838457, -2.977408999572651371 ) ) ;
#60084=CARTESIAN_POINT ( 'NONE',  ( 5.082755093536325930, -11.46875000204838635, -5.082755093536325042 ) ) ;
#60101=AXIS2_PLACEMENT_3D ( 'NONE', #6607, #39534, #40048 ) ;
#60106=CYLINDRICAL_SURFACE ( 'NONE', #21667, 4.000000000000001776 ) ;
#60131=CLOSED_SHELL ( 'NONE', ( #92536, #37525, #51526, #1341, #61836, #18327, #104446, #22180, #80840, #3605, #100451, #10332, #81057, #76232, #66837, #83214, #43171, #97407, #83026, #11692, #42206, #11960, #4049, #37230, #17785, #22819, #45648, #52901, #74681, #39301, #98866, #99633, #77930, #15803, #29571, #69617, #54079, #45805, #14106, #72932, #31718, #22427, #101611, #96719, #98518, #78322, #33243, #65606, #92608, #95968, #75886, #13251, #86094, #39801, #22559, #69158, #8365, #9661, #10276, #6297, #64886, #104567, #7331, #60625, #6831, #83666, #106412, #8942, #99717, #99162, #11818, #31536 ) ) ;
#60144=CARTESIAN_POINT ( 'NONE',  ( 5.082755093536325930, -26.46875000204838813, -5.082755093536325042 ) ) ;
#60151=CARTESIAN_POINT ( 'NONE',  ( -9.381394091586573225, 82.98650394418388032, 3.465950112474263989 ) ) ;
#60154=CARTESIAN_POINT ( 'NONE',  ( 5.656854249492380582, -17.00000000409676915, -5.656854249492379694 ) ) ;
#60161=CARTESIAN_POINT ( 'NONE',  ( 7.074371941841917533, -30.00000000000001066, -1.589546009095287982 ) ) ;
#60179=AXIS2_PLACEMENT_3D ( 'NONE', #13741, #45083, #87660 ) ;
#60210=UNCERTAINTY_MEASURE_WITH_UNIT (LENGTH_MEASURE( 1.000000000000000082E-05 ), #39591, 'distance_accuracy_value', 'NONE');
#60234=CARTESIAN_POINT ( 'NONE',  ( 0.000000000000000000, 16.00000000000000000, 0.000000000000000000 ) ) ;
#60253=CARTESIAN_POINT ( 'NONE',  ( -1.469576158976823947E-15, -15.87499999999999289, 8.000000000000000000 ) ) ;
#60290=CARTESIAN_POINT ( 'NONE',  ( 7.999999999999998224, -18.59374999999999289, 3.313708498984766049 ) ) ;
#60332=CARTESIAN_POINT ( 'NONE',  ( -8.000000000000000000, -28.24999999999999645, -9.797174393178825657E-16 ) ) ;
#60345=CIRCLE ( 'NONE', #27650, 11.00000000000000000 ) ;
#60349=CARTESIAN_POINT ( 'NONE',  ( -8.000000000000000000, -13.34374999999999467, -3.313708498984762496 ) ) ;
#60353=ORIENTED_EDGE ( 'NONE', *, *, #71269, .T. ) ;
#60368=EDGE_CURVE ( 'NONE', #103221, #45098, #100881, .T. ) ;
#60395=CARTESIAN_POINT ( 'NONE',  ( 5.656854249492380582, -18.31249999999999289, -5.656854249492379694 ) ) ;
#60449=CARTESIAN_POINT ( 'NONE',  ( -3.313708498984798467, -12.03124999999999112, -7.999999999999961808 ) ) ;
#60456=EDGE_CURVE ( 'NONE', #57731, #82593, #52331, .T. ) ;
#60473=( BOUNDED_CURVE ( )  B_SPLINE_CURVE ( 2, ( #92708, #18868, #99190, #49589, #99739, #43630, #50630, #25352, #35043 ),
 .UNSPECIFIED., .F., .F. ) 
 B_SPLINE_CURVE_WITH_KNOTS ( ( 3, 2, 2, 2, 3 ),
 ( 0.1617647058823529216, 0.1691176470588235115, 0.1764705882352941013, 0.1838235294117647189, 0.1911764705882352811 ),
 .UNSPECIFIED. ) 
 CURVE ( )  GEOMETRIC_REPRESENTATION_ITEM ( )  RATIONAL_B_SPLINE_CURVE ( ( 1.000000000000000222, 0.9238795325112864054, 1.000000000000000000, 0.9238795325112867385, 1.000000000000000000, 0.9238795325112867385, 1.000000000000000000, 0.9238795325112867385, 1.000000000000000000 ) ) 
 REPRESENTATION_ITEM ( '' )  );
#60486=CARTESIAN_POINT ( 'NONE',  ( 2.977408999572650927, -11.75000000204838813, -7.188101187500001821 ) ) ;
#60523=CARTESIAN_POINT ( 'NONE',  ( 5.082755093536324154, -18.21875000204838457, 5.082755093536326818 ) ) ;
#60526=CARTESIAN_POINT ( 'NONE',  ( -5.656854249492381470, -11.75000000409677092, 5.656854249492379694 ) ) ;
#60531=CARTESIAN_POINT ( 'NONE',  ( 9.699189539447123920, 88.17692228246710329, -2.444343703917210231 ) ) ;
#60533=DIRECTION ( 'NONE',  ( -0.000000000000000000, 1.000000000000000000, -0.000000000000000000 ) ) ;
#60547=CARTESIAN_POINT ( 'NONE',  ( -2.977408999572654480, -22.62500000204838813, 7.188101187499999156 ) ) ;
#60557=LINE ( 'NONE', #17967, #48064 ) ;
#60564=ORIENTED_EDGE ( 'NONE', *, *, #44800, .F. ) ;
#60568=CARTESIAN_POINT ( 'NONE',  ( 9.176855344542989457, 104.4703957302259028, -3.973472207155928970 ) ) ;
#60598=ORIENTED_EDGE ( 'NONE', *, *, #45267, .F. ) ;
#60600=CARTESIAN_POINT ( 'NONE',  ( -5.082755093536326818, -26.09375000204838813, 5.082755093536325042 ) ) ;
#60609=CARTESIAN_POINT ( 'NONE',  ( -1.320432766682874540E-15, -30.40625000204838813, 7.188101187500000044 ) ) ;
#60615=CARTESIAN_POINT ( 'NONE',  ( -5.656854249492381470, -14.56249999999999289, 5.656854249492379694 ) ) ;
#60625=ADVANCED_FACE ( 'NONE', ( #85800 ), #56473, .F. ) ;
#60647=CARTESIAN_POINT ( 'NONE',  ( 8.000000000000000000, -10.99999999999999289, 0.000000000000000000 ) ) ;
#60666=CARTESIAN_POINT ( 'NONE',  ( 5.082755093536325930, -23.46875000204838457, -5.082755093536325042 ) ) ;
#60669=VECTOR ( 'NONE', #22004, 1000.000000000000000 ) ;
#60673=TOROIDAL_SURFACE ( 'NONE', #55463, 11.00000000000000000, 1.000000000000000000 ) ;
#60675=CARTESIAN_POINT ( 'NONE',  ( -3.313708498984765161, -20.65625000409677270, 7.999999999999998224 ) ) ;
#60708=AXIS2_PLACEMENT_3D ( 'NONE', #83190, #74563, #99350 ) ;
#60732=CARTESIAN_POINT ( 'NONE',  ( -7.188101187500001821, -29.00000000204838813, -2.977408999572651371 ) ) ;
#60736=CARTESIAN_POINT ( 'NONE',  ( -2.450541714948251126, 15.75132464342601146, 9.701712097384769251 ) ) ;
#60739=CARTESIAN_POINT ( 'NONE',  ( -8.000000000000000000, -17.74999999999999645, -9.797174393178825657E-16 ) ) ;
#60826=CARTESIAN_POINT ( 'NONE',  ( -9.165151389911679658, 105.2673515560711337, -4.000000000000001776 ) ) ;
#60867=VERTEX_POINT ( 'NONE', #57102 ) ;
#60918=CARTESIAN_POINT ( 'NONE',  ( -1.469576158976823947E-15, -23.37499999999999289, 8.000000000000000000 ) ) ;
#60960=CYLINDRICAL_SURFACE ( 'NONE', #16982, 8.000000000000000000 ) ;
#60967=CARTESIAN_POINT ( 'NONE',  ( -3.313708498984746065, -24.96874999999998934, 8.000000000000017764 ) ) ;
#60987=CARTESIAN_POINT ( 'NONE',  ( -9.842984802582135373, 101.4093040952434563, 1.781981959250506842 ) ) ;
#60989=CARTESIAN_POINT ( 'NONE',  ( 4.582575694955843382, 15.00000000000000000, -9.999999999999998224 ) ) ;
#61000=CARTESIAN_POINT ( 'NONE',  ( 3.313708498984762496, -18.96875000409677270, 7.999999999999998224 ) ) ;
#61008=CARTESIAN_POINT ( 'NONE',  ( 7.188101187499999156, -16.62500000204838457, 2.977408999572654924 ) ) ;
#61015=EDGE_CURVE ( 'NONE', #89525, #56748, #2590, .T. ) ;
#61021=CARTESIAN_POINT ( 'NONE',  ( -7.550180524134852078, 88.00559247213188030, 2.651855549982491400 ) ) ;
#61047=CARTESIAN_POINT ( 'NONE',  ( 2.977408999572651815, -13.81250000204838280, 7.188101187500000933 ) ) ;
#61070=CARTESIAN_POINT ( 'NONE',  ( -5.082755093536325042, -26.09375000204838813, -5.082755093536325930 ) ) ;
#61088=CARTESIAN_POINT ( 'NONE',  ( 9.843039827103241990, 101.4091649749166635, -1.781495459429543793 ) ) ;
#61112=ORIENTED_EDGE ( 'NONE', *, *, #12229, .F. ) ;
#61117=DIRECTION ( 'NONE',  ( 1.000000000000000000, -0.000000000000000000, -0.000000000000000000 ) ) ;
#61118=CARTESIAN_POINT ( 'NONE',  ( 2.977408999572652260, -27.31250000204838457, 7.188101187500000044 ) ) ;
#61127=CARTESIAN_POINT ( 'NONE',  ( 7.188101187500001821, -32.93750000204839523, -2.977408999572650483 ) ) ;
#61128=LINE ( 'NONE', #91887, #86065 ) ;
#61132=CARTESIAN_POINT ( 'NONE',  ( -6.943926999490793506, 105.5330099262614709, -3.973092371898548691 ) ) ;
#61135=VECTOR ( 'NONE', #37167, 1000.000000000000000 ) ;
#61171=CARTESIAN_POINT ( 'NONE',  ( 2.977408999572651815, -28.81250000204838457, 7.188101187500000933 ) ) ;
#61185=CARTESIAN_POINT ( 'NONE',  ( 2.977408999572652260, -20.93750000204839168, 7.188101187500000044 ) ) ;
#61189=ORIENTED_EDGE ( 'NONE', *, *, #19549, .F. ) ;
#61194=CARTESIAN_POINT ( 'NONE',  ( 3.313708498984762052, -16.90625000409676915, -8.000000000000000000 ) ) ;
#61202=CARTESIAN_POINT ( 'NONE',  ( -0.08034007072829510432, -30.00000000000001066, -7.793135878010705397 ) ) ;
#61257=CARTESIAN_POINT ( 'NONE',  ( 5.082755093536324154, -25.34375000204838813, 5.082755093536326818 ) ) ;
#61260=CARTESIAN_POINT ( 'NONE',  ( 1.510421413154731551, 15.23810023151366977, 9.910377230549928029 ) ) ;
#61263=CARTESIAN_POINT ( 'NONE',  ( -3.313708498984726969, -17.46874999999999645, 8.000000000000039080 ) ) ;
#61276=DIRECTION ( 'NONE',  ( 0.000000000000000000, 0.000000000000000000, 1.000000000000000000 ) ) ;
#61284=CARTESIAN_POINT ( 'NONE',  ( 2.450449656239129581, 15.75130202679986269, 9.701736001019305888 ) ) ;
#61296=CARTESIAN_POINT ( 'NONE',  ( 0.000000000000000000, 0.000000000000000000, 8.000000000000000000 ) ) ;
#61403=ORIENTED_EDGE ( 'NONE', *, *, #88665, .F. ) ;
#61438=VECTOR ( 'NONE', #73746, 1000.000000000000000 ) ;
#61442=VERTEX_POINT ( 'NONE', #81507 ) ;
#61451=CARTESIAN_POINT ( 'NONE',  ( 7.999999999999998224, -20.09374999999999289, 3.313708498984766493 ) ) ;
#61526=CARTESIAN_POINT ( 'NONE',  ( -10.00004721872059754, 100.9998819531884919, -0.2617599822266485909 ) ) ;
#61528=CARTESIAN_POINT ( 'NONE',  ( 3.409011323176964758, 15.24615751665866981, -9.403185743875123848 ) ) ;
#61543=CARTESIAN_POINT ( 'NONE',  ( 5.082755093536324154, -15.21875000204838457, 5.082755093536326818 ) ) ;
#61556=CARTESIAN_POINT ( 'NONE',  ( 4.898587196589412829E-16, -13.62499999999999112, -8.000000000000000000 ) ) ;
#61566=CARTESIAN_POINT ( 'NONE',  ( 5.656854249492380582, -26.00000000409677270, -5.656854249492379694 ) ) ;
#61567=CARTESIAN_POINT ( 'NONE',  ( 5.656854249492380582, -17.00000000409676915, -5.656854249492379694 ) ) ;
#61575=EDGE_CURVE ( 'NONE', #68507, #40311, #100582, .T. ) ;
#61584=CARTESIAN_POINT ( 'NONE',  ( 4.401442555609581635E-16, -16.15625000204838457, -7.188101187500000044 ) ) ;
#61592=AXIS2_PLACEMENT_3D ( 'NONE', #49206, #48671, #71905 ) ;
#61609=CARTESIAN_POINT ( 'NONE',  ( -10.00000000000000355, 105.0000000000000000, 4.000000000000001776 ) ) ;
#61613=CARTESIAN_POINT ( 'NONE',  ( 4.401442555609581635E-16, -26.28125000204838813, -7.188101187500000044 ) ) ;
#61627=EDGE_LOOP ( 'NONE', ( #55403, #57717, #3962, #5258 ) ) ;
#61629=CARTESIAN_POINT ( 'NONE',  ( -1.469576158976823947E-15, -17.37499999999999289, 8.000000000000000000 ) ) ;
#61635=CARTESIAN_POINT ( 'NONE',  ( 9.380871178326117388, 102.9888362020167563, 3.467392232194208557 ) ) ;
#61670=CARTESIAN_POINT ( 'NONE',  ( 5.082755093536325930, -28.34375000204838813, -5.082755093536325042 ) ) ;
#61681=CARTESIAN_POINT ( 'NONE',  ( 2.977408999572650927, -9.875000002048386349, -7.188101187500001821 ) ) ;
#61686=CARTESIAN_POINT ( 'NONE',  ( -7.986539162393897939, 108.9732717105745223, -0.5321833565149903800 ) ) ;
#61720=CARTESIAN_POINT ( 'NONE',  ( -2.977408999572654480, -33.50000000204838813, 7.188101187499999156 ) ) ;
#61732=CARTESIAN_POINT ( 'NONE',  ( -5.082755093536326818, -16.71875000204838813, 5.082755093536325042 ) ) ;
#61741=CARTESIAN_POINT ( 'NONE',  ( 3.313708498984762052, -19.90625000409677270, -8.000000000000000000 ) ) ;
#61743=CARTESIAN_POINT ( 'NONE',  ( 9.435590127032934760, 15.92795519102023860, 3.316968746324335804 ) ) ;
#61805=CARTESIAN_POINT ( 'NONE',  ( 7.188101187500000044, -23.65625000204838457, 0.000000000000000000 ) ) ;
#61808=CARTESIAN_POINT ( 'NONE',  ( -3.313708498984726969, -23.46874999999999289, 8.000000000000039080 ) ) ;
#61836=ADVANCED_FACE ( 'NONE', ( #53174 ), #102782, .F. ) ;
#61838=ORIENTED_EDGE ( 'NONE', *, *, #81115, .T. ) ;
#61875=DIRECTION ( 'NONE',  ( 0.000000000000000000, 1.000000000000000000, 0.000000000000000000 ) ) ;
#61892=( NAMED_UNIT ( * ) PLANE_ANGLE_UNIT ( ) SI_UNIT ( $, .RADIAN. ) );
#61900=CARTESIAN_POINT ( 'NONE',  ( -9.220915120640581719, 106.0445488643208165, -3.870126578504840431 ) ) ;
#61932=VECTOR ( 'NONE', #13192, 1000.000000000000000 ) ;
#61979=LINE ( 'NONE', #104521, #74022 ) ;
#61992=CARTESIAN_POINT ( 'NONE',  ( -8.000000000000000000, -20.84374999999999645, -3.313708498984762496 ) ) ;
#62043=CARTESIAN_POINT ( 'NONE',  ( -1.469576158976823947E-15, -11.37499999999999289, 8.000000000000000000 ) ) ;
#62045=CARTESIAN_POINT ( 'NONE',  ( -9.221346651730838673, 28.95165979931662292, -3.869102247876034184 ) ) ;
#62067=FILL_AREA_STYLE ('',( #12404 ) ) ;
#62080=CARTESIAN_POINT ( 'NONE',  ( 7.188101187500001821, -14.93750000204838457, -2.977408999572650483 ) ) ;
#62122=CARTESIAN_POINT ( 'NONE',  ( 2.977408999572650927, -14.75000000204838457, -7.188101187500001821 ) ) ;
#62148=CARTESIAN_POINT ( 'NONE',  ( 7.188101187499999156, -17.75000000204838457, 2.977408999572654924 ) ) ;
#62176=EDGE_CURVE ( 'NONE', #42837, #50100, #18726, .T. ) ;
#62177=( BOUNDED_CURVE ( )  B_SPLINE_CURVE ( 2, ( #36315, #69182, #20130, #85903, #52982, #44906, #14089, #104171, #38410 ),
 .UNSPECIFIED., .F., .F. ) 
 B_SPLINE_CURVE_WITH_KNOTS ( ( 3, 2, 2, 2, 3 ),
 ( 0.4558823529411765163, 0.4632352941176471339, 0.4705882352941177516, 0.4779411764705883692, 0.4852941176470589313 ),
 .UNSPECIFIED. ) 
 CURVE ( )  GEOMETRIC_REPRESENTATION_ITEM ( )  RATIONAL_B_SPLINE_CURVE ( ( 0.9999999999999994449, 0.9238795325112872936, 1.000000000000000000, 0.9238795325112867385, 1.000000000000000000, 0.9238795325112867385, 1.000000000000000000, 0.9238795325112856283, 1.000000000000001110 ) ) 
 REPRESENTATION_ITEM ( '' )  );
#62202=CARTESIAN_POINT ( 'NONE',  ( -7.188101187500000933, -21.87500000204838813, -2.977408999572651371 ) ) ;
#62205=CARTESIAN_POINT ( 'NONE',  ( -8.000000000000000000, -26.93750000409677625, -9.797174393178825657E-16 ) ) ;
#62211=CARTESIAN_POINT ( 'NONE',  ( -2.977408999572650039, -34.06250000204839523, -7.188101187500001821 ) ) ;
#62216=CARTESIAN_POINT ( 'NONE',  ( -8.000086790516061086, 109.0001735810600678, 0.2639471549312831233 ) ) ;
#62250=CARTESIAN_POINT ( 'NONE',  ( 7.188101187499999156, -31.62500000204838813, 2.977408999572654924 ) ) ;
#62256=ORIENTED_EDGE ( 'NONE', *, *, #68601, .F. ) ;
#62262=CARTESIAN_POINT ( 'NONE',  ( 4.401442555609581635E-16, -17.28125000204838813, -7.188101187500000044 ) ) ;
#62267=VECTOR ( 'NONE', #52082, 1000.000000000000000 ) ;
#62271=CARTESIAN_POINT ( 'NONE',  ( -5.656854249492381470, -17.75000000409676915, 5.656854249492379694 ) ) ;
#62274=CARTESIAN_POINT ( 'NONE',  ( -9.176855344542985904, 85.52960426977412567, -3.973472207155925862 ) ) ;
#62324=CARTESIAN_POINT ( 'NONE',  ( -7.188101187500001821, -26.00000000204838457, -2.977408999572651371 ) ) ;
#62370=LINE ( 'NONE', #21392, #98335 ) ;
#62410=CARTESIAN_POINT ( 'NONE',  ( -9.910377230549258343, 15.23810023151367155, 1.510421413154401371 ) ) ;
#62430=ORIENTED_EDGE ( 'NONE', *, *, #54812, .T. ) ;
#62448=CARTESIAN_POINT ( 'NONE',  ( 9.999999999999996447, 15.00000000000000000, -10.00000000000000000 ) ) ;
#62459=VECTOR ( 'NONE', #1237, 1000.000000000000000 ) ;
#62508=CARTESIAN_POINT ( 'NONE',  ( 3.313708498984762052, -22.71875000000000355, -8.000000000000000000 ) ) ;
#62543=ORIENTED_EDGE ( 'NONE', *, *, #100053, .T. ) ;
#62555=CARTESIAN_POINT ( 'NONE',  ( -9.176803346051508825, 29.47052844202562483, 3.973598758023531019 ) ) ;
#62561=ORIENTED_EDGE ( 'NONE', *, *, #72882, .T. ) ;
#62576=CARTESIAN_POINT ( 'NONE',  ( -9.253500431420432548, 103.7022845008229126, 3.792688295761953210 ) ) ;
#62580=EDGE_CURVE ( 'NONE', #84193, #87634, #95904, .T. ) ;
#62593=CARTESIAN_POINT ( 'NONE',  ( -2.977408999572654480, -12.50000000204838990, 7.188101187499999156 ) ) ;
#62602=VERTEX_POINT ( 'NONE', #37705 ) ;
#62625=CARTESIAN_POINT ( 'NONE',  ( 7.151597709147945459, 31.78929265052214603, 3.587174531012141454 ) ) ;
#62627=CARTESIAN_POINT ( 'NONE',  ( -7.986468734911285949, 26.02686320276919929, 0.5341897780976145871 ) ) ;
#62634=CARTESIAN_POINT ( 'NONE',  ( -2.977408999572650039, -14.56250000204838457, -7.188101187500001821 ) ) ;
#62665=CARTESIAN_POINT ( 'NONE',  ( -5.082755093536326818, -16.71875000204838813, 5.082755093536325042 ) ) ;
#62710=CARTESIAN_POINT ( 'NONE',  ( 7.188101187500000044, -19.53125000204838457, 0.000000000000000000 ) ) ;
#62720=CARTESIAN_POINT ( 'NONE',  ( 4.401442555609581635E-16, -9.781250002048384573, -7.188101187500000044 ) ) ;
#62738=DIRECTION ( 'NONE',  ( 1.000000000000000000, 0.000000000000000000, 0.000000000000000000 ) ) ;
#62755=ORIENTED_EDGE ( 'NONE', *, *, #59341, .F. ) ;
#62762=CARTESIAN_POINT ( 'NONE',  ( -7.188101187500002709, -30.68750000204839168, 2.977408999572648707 ) ) ;
#62778=CARTESIAN_POINT ( 'NONE',  ( -2.977408999572650039, -18.68750000204838457, -7.188101187500000933 ) ) ;
#62783=DIRECTION ( 'NONE',  ( 0.000000000000000000, 0.000000000000000000, 1.000000000000000000 ) ) ;
#62784=CARTESIAN_POINT ( 'NONE',  ( -9.948181520647858989, 81.13107197239621371, 1.049088206181491012 ) ) ;
#62786=CARTESIAN_POINT ( 'NONE',  ( 3.313708498984762052, -12.40625000409676915, -8.000000000000000000 ) ) ;
#62838=PLANE ( 'NONE',  #82617 ) ;
#62853=CARTESIAN_POINT ( 'NONE',  ( -7.188101187500001821, -24.50000000204839168, -2.977408999572651371 ) ) ;
#62918=CARTESIAN_POINT ( 'NONE',  ( -5.656854249492381470, -31.25000000409677270, 5.656854249492379694 ) ) ;
#62926=FILL_AREA_STYLE ('',( #72583 ) ) ;
#62970=VERTEX_POINT ( 'NONE', #83687 ) ;
#62979=TOROIDAL_SURFACE ( 'NONE', #76731, 11.00000000000000000, 1.000000000000000000 ) ;
#63005=ORIENTED_EDGE ( 'NONE', *, *, #8807, .F. ) ;
#63010=VERTEX_POINT ( 'NONE', #41648 ) ;
#63033=CARTESIAN_POINT ( 'NONE',  ( 3.313708498984762052, -12.21874999999999467, -8.000000000000000000 ) ) ;
#63071=EDGE_CURVE ( 'NONE', #32259, #18153, #69825, .T. ) ;
#63080=CARTESIAN_POINT ( 'NONE',  ( -9.380169522195149767, 15.95824666716552365, 3.484756791224360661 ) ) ;
#63083=DIRECTION ( 'NONE',  ( 0.000000000000000000, 0.000000000000000000, 1.000000000000000000 ) ) ;
#63110=DIRECTION ( 'NONE',  ( -0.000000000000000000, 1.000000000000000000, -0.000000000000000000 ) ) ;
#63116=CARTESIAN_POINT ( 'NONE',  ( -7.188101187500001821, -9.875000002048386349, -2.977408999572651371 ) ) ;
#63128=ORIENTED_EDGE ( 'NONE', *, *, #94713, .T. ) ;
#63163=CARTESIAN_POINT ( 'NONE',  ( -1.469576158976823947E-15, -30.87499999999999645, 8.000000000000000000 ) ) ;
#63190=CARTESIAN_POINT ( 'NONE',  ( -1.320432766682874540E-15, -22.53125000204838457, 7.188101187500000044 ) ) ;
#63202=EDGE_LOOP ( 'NONE', ( #79425, #59785 ) ) ;
#63242=CARTESIAN_POINT ( 'NONE',  ( -2.977408999572654480, -18.50000000204838457, 7.188101187499999156 ) ) ;
#63248=CARTESIAN_POINT ( 'NONE',  ( 0.000000000000000000, -30.00000000000000000, 0.000000000000000000 ) ) ;
#63252=CARTESIAN_POINT ( 'NONE',  ( -7.188101187500001821, -24.87500000204838457, -2.977408999572651371 ) ) ;
#63294=CARTESIAN_POINT ( 'NONE',  ( -2.977408999572654480, -30.50000000204838813, 7.188101187499999156 ) ) ;
#63311=CARTESIAN_POINT ( 'NONE',  ( -7.188101187500000044, -19.90625000204838457, -8.802885111219163269E-16 ) ) ;
#63321=CARTESIAN_POINT ( 'NONE',  ( -9.381593208289373820, 82.98561361880494758, -3.465401811657801368 ) ) ;
#63324=CARTESIAN_POINT ( 'NONE',  ( 5.656854249492380582, -11.00000000409677092, -5.656854249492379694 ) ) ;
#63326=( NAMED_UNIT ( * ) SI_UNIT ( $, .STERADIAN. ) SOLID_ANGLE_UNIT ( ) );
#63337=CARTESIAN_POINT ( 'NONE',  ( -4.210530276627961754, 14.99999999999998934, 10.00000000000003908 ) ) ;
#63354=CARTESIAN_POINT ( 'NONE',  ( -9.165151389911679658, 85.00000000000000000, 4.000000000000000000 ) ) ;
#63366=CARTESIAN_POINT ( 'NONE',  ( 4.898587196589412829E-16, -18.31250000409676915, -8.000000000000000000 ) ) ;
#63393=CARTESIAN_POINT ( 'NONE',  ( 5.082755093536325930, -24.96875000204838813, -5.082755093536325042 ) ) ;
#63438=ORIENTED_EDGE ( 'NONE', *, *, #73465, .F. ) ;
#63448=LINE ( 'NONE', #45659, #67864 ) ;
#63456=CARTESIAN_POINT ( 'NONE',  ( 4.898587196589412829E-16, -27.31250000409677270, -8.000000000000000000 ) ) ;
#63478=FACE_BOUND ( 'NONE', #31220, .T. ) ;
#63509=CARTESIAN_POINT ( 'NONE',  ( 8.000000000000000000, -12.68750000409676915, 0.000000000000000000 ) ) ;
#63553=ORIENTED_EDGE ( 'NONE', *, *, #92248, .F. ) ;
#63568=CARTESIAN_POINT ( 'NONE',  ( -9.981531048852469112, 15.23280014800326398, -0.7018335428337003634 ) ) ;
#63578=CARTESIAN_POINT ( 'NONE',  ( -8.000000000000000000, -16.24999999999999289, -9.797174393178825657E-16 ) ) ;
#63651=CARTESIAN_POINT ( 'NONE',  ( -1.469576158976823947E-15, -12.87499999999999467, 8.000000000000000000 ) ) ;
#63695=CARTESIAN_POINT ( 'NONE',  ( 7.896254658894421574, 33.78929182754200156, 1.307282859663294383 ) ) ;
#63705=CARTESIAN_POINT ( 'NONE',  ( -2.977408999572650039, -10.06250000204838280, -7.188101187500001821 ) ) ;
#63718=DIRECTION ( 'NONE',  ( -0.000000000000000000, 1.000000000000000000, -0.000000000000000000 ) ) ;
#63730=CARTESIAN_POINT ( 'NONE',  ( -5.082755093536325042, -18.59375000204838457, -5.082755093536325930 ) ) ;
#63774=CARTESIAN_POINT ( 'NONE',  ( 7.188101187500000044, -21.03125000204838813, 0.000000000000000000 ) ) ;
#63784=CARTESIAN_POINT ( 'NONE',  ( 2.977408999572650927, -26.75000000204838457, -7.188101187500001821 ) ) ;
#63810=CARTESIAN_POINT ( 'NONE',  ( -10.00000000000000355, 15.00000000000000000, -10.00000000000000000 ) ) ;
#63825=CARTESIAN_POINT ( 'NONE',  ( -1.320432766682874540E-15, -27.40625000204838813, 7.188101187500000044 ) ) ;
#63838=CARTESIAN_POINT ( 'NONE',  ( -5.082755093536326818, -12.21875000204838635, 5.082755093536325042 ) ) ;
#63852=CARTESIAN_POINT ( 'NONE',  ( 8.000000000000000000, -12.68750000409676915, 0.000000000000000000 ) ) ;
#63859=SURFACE_STYLE_USAGE ( .BOTH. , #22881 ) ;
#63861=CARTESIAN_POINT ( 'NONE',  ( -9.918010731619569142, 33.79151684843224501, -1.300854425901587286 ) ) ;
#63866=CARTESIAN_POINT ( 'NONE',  ( -3.409011323177015385, 15.24615751665830743, 9.403185743874946212 ) ) ;
#63901=DIRECTION ( 'NONE',  ( -1.734723475976807094E-16, -0.000000000000000000, -1.000000000000000000 ) ) ;
#63916=CARTESIAN_POINT ( 'NONE',  ( -10.00000000000000355, 30.00000000000000000, 0.000000000000000000 ) ) ;
#63918=CARTESIAN_POINT ( 'NONE',  ( -5.082755093536326818, -18.21875000204838457, 5.082755093536325042 ) ) ;
#63920=CARTESIAN_POINT ( 'NONE',  ( 9.165151389911681434, 85.00000000000001421, -4.000000000000000000 ) ) ;
#63974=CARTESIAN_POINT ( 'NONE',  ( 2.977408999572652260, -28.43750000204839523, 7.188101187500000044 ) ) ;
#63984=EDGE_CURVE ( 'NONE', #13534, #9794, #94075, .T. ) ;
#63987=CARTESIAN_POINT ( 'NONE',  ( -8.000000000000000000, -27.03125000409677270, -3.313708498984762496 ) ) ;
#64011=CARTESIAN_POINT ( 'NONE',  ( -9.168149550320920937, 15.99999999372935022, 3.997425403568219515 ) ) ;
#64035=CARTESIAN_POINT ( 'NONE',  ( -8.000000000000000000, -20.93750000409676915, -9.797174393178825657E-16 ) ) ;
#64047=STYLED_ITEM ( 'NONE', ( #37264 ), #106412 ) ;
#64076=( BOUNDED_CURVE ( )  B_SPLINE_CURVE ( 2, ( #31627, #81197, #48300, #47245, #73091, #40222, #87736, #80147, #106541 ),
 .UNSPECIFIED., .F., .F. ) 
 B_SPLINE_CURVE_WITH_KNOTS ( ( 3, 2, 2, 2, 3 ),
 ( 0.9558823529411765163, 0.9632352941176470784, 0.9705882352941176405, 0.9779411764705882026, 0.9804062239465977102 ),
 .UNSPECIFIED. ) 
 CURVE ( )  GEOMETRIC_REPRESENTATION_ITEM ( )  RATIONAL_B_SPLINE_CURVE ( ( 1.000000000000000000, 0.9238795325112867385, 1.000000000000000000, 0.9238795325112867385, 1.000000000000000000, 0.9238795325112867385, 1.000000000000000000, 0.9744808829892229740, 0.9660721530923004341 ) ) 
 REPRESENTATION_ITEM ( '' )  );
#64104=EDGE_LOOP ( 'NONE', ( #52385, #85153, #28530, #100765 ) ) ;
#64110=CARTESIAN_POINT ( 'NONE',  ( 8.000000000000000000, -13.90624999999999112, -3.313708498984761608 ) ) ;
#64126=EDGE_CURVE ( 'NONE', #49838, #27681, #30364, .T. ) ;
#64172=CARTESIAN_POINT ( 'NONE',  ( 7.188101187500000044, -34.15625000204838813, 0.000000000000000000 ) ) ;
#64190=CARTESIAN_POINT ( 'NONE',  ( -1.320432766682874540E-15, -10.90625000204838457, 7.188101187500000044 ) ) ;
#64196=CARTESIAN_POINT ( 'NONE',  ( -9.090909090909093493, 16.00000000000000000, -4.165977904505304252 ) ) ;
#64232=CARTESIAN_POINT ( 'NONE',  ( 8.000000000000000000, -33.40625000000000000, -3.313708498984761608 ) ) ;
#64253=CARTESIAN_POINT ( 'NONE',  ( 6.928203230275509661, 105.2647926725356911, 4.000000000000000888 ) ) ;
#64257=CARTESIAN_POINT ( 'NONE',  ( 7.188101187500000044, -19.15625000204838457, 0.000000000000000000 ) ) ;
#64265=CYLINDRICAL_SURFACE ( 'NONE', #72188, 4.000000000000001776 ) ;
#64267=MECHANICAL_DESIGN_GEOMETRIC_PRESENTATION_REPRESENTATION('',(#22943),#83192);
#64279=DIRECTION ( 'NONE',  ( -0.000000000000000000, 1.000000000000000000, -0.000000000000000000 ) ) ;
#64284=ORIENTED_EDGE ( 'NONE', *, *, #96884, .F. ) ;
#64301=CARTESIAN_POINT ( 'NONE',  ( -7.188101187500002709, -21.68750000204838813, 2.977408999572647819 ) ) ;
#64310=CARTESIAN_POINT ( 'NONE',  ( 2.977408999572650927, -29.75000000204838813, -7.188101187500000933 ) ) ;
#64313=CARTESIAN_POINT ( 'NONE',  ( -7.188101187500002709, -27.68750000204838813, 2.977408999572648707 ) ) ;
#64319=CARTESIAN_POINT ( 'NONE',  ( -6.943482370013978944, 105.5284837026072182, 3.973876482044367275 ) ) ;
#64357=CARTESIAN_POINT ( 'NONE',  ( 9.644834624769975662, 26.99109499794224831, 2.648308524638413264 ) ) ;
#64359=CARTESIAN_POINT ( 'NONE',  ( -5.082755093536325042, -24.96875000204838813, -5.082755093536325930 ) ) ;
#64370=CARTESIAN_POINT ( 'NONE',  ( 7.188101187500000044, -14.65625000204838457, 0.000000000000000000 ) ) ;
#64380=CARTESIAN_POINT ( 'NONE',  ( -1.469576158976823947E-15, -14.56250000409677092, 8.000000000000000000 ) ) ;
#64385=CARTESIAN_POINT ( 'NONE',  ( -9.380871178326117388, 87.01116379798325795, 3.467392232194206780 ) ) ;
#64391=CARTESIAN_POINT ( 'NONE',  ( -0.7408669144221268210, 15.11700796859948426, 9.999999999997887912 ) ) ;
#64416=EDGE_CURVE ( 'NONE', #32331, #93999, #64076, .T. ) ;
#64442=CARTESIAN_POINT ( 'NONE',  ( 5.082755093536324154, -19.34375000204838457, 5.082755093536326818 ) ) ;
#64449=ORIENTED_EDGE ( 'NONE', *, *, #72874, .F. ) ;
#64466=ORIENTED_EDGE ( 'NONE', *, *, #37754, .T. ) ;
#64496=CARTESIAN_POINT ( 'NONE',  ( 5.082755093536324154, -28.34375000204838813, 5.082755093536326818 ) ) ;
#64507=CARTESIAN_POINT ( 'NONE',  ( 4.898587196589412829E-16, -28.81250000409677270, -8.000000000000000000 ) ) ;
#64510=CARTESIAN_POINT ( 'NONE',  ( 10.00004721872059754, 34.00011804681151517, -0.2617599822266539755 ) ) ;
#64542=CARTESIAN_POINT ( 'NONE',  ( -6.928203230275508773, 30.26526156932586176, 4.000000000000000000 ) ) ;
#64550=CARTESIAN_POINT ( 'NONE',  ( -5.637738193748796256, -30.00000000000000711, 5.087150282644762989 ) ) ;
#64560=CARTESIAN_POINT ( 'NONE',  ( 4.034557488804142444, 15.07443463110229054, 9.151133496029162373 ) ) ;
#64580=DIRECTION ( 'NONE',  ( 0.000000000000000000, 1.000000000000000000, 0.000000000000000000 ) ) ;
#64615=CIRCLE ( 'NONE', #76760, 10.00000000000000000 ) ;
#64620=B_SPLINE_CURVE_WITH_KNOTS ( 'NONE', 3,
 ( #83330, #778, #90909, #89841, #33215, #8377, #49898, #61202, #84410, #102713, #68225, #3492, #12618, #27279, #51495, #92485, #18635, #20791, #77912, #37487, #35897, #93569, #77376, #85477, #86559, #60161, #68774 ),
 .UNSPECIFIED., .F., .F.,
 ( 4, 2, 2, 2, 2, 2, 2, 2, 2, 2, 1, 2, 2, 4 ),
 ( 4.772854504744018845E-17, 0.001861613648588184705, 0.002792420472882253205, 0.003723227297176320838, 0.004654034121470389772, 0.005584840945764458706, 0.006515647770058525905, 0.007446454594352594838, 0.009308068242940732706, 0.01023887506723480251, 0.01116968189152887057, 0.01210048871582293864, 0.01303129554011700671, 0.01489290918870514804 ),
 .UNSPECIFIED. ) ;
#64626=CARTESIAN_POINT ( 'NONE',  ( -3.313708498984765161, -12.96874999999999289, 7.999999999999998224 ) ) ;
#64628=EDGE_CURVE ( 'NONE', #99488, #79080, #49901, .T. ) ;
#64645=CARTESIAN_POINT ( 'NONE',  ( 9.435590127032984498, 15.92795519102023860, -3.316968746324189699 ) ) ;
#64676=ORIENTED_EDGE ( 'NONE', *, *, #64628, .F. ) ;
#64678=( BOUNDED_SURFACE ( )  B_SPLINE_SURFACE ( 1, 2, ( 
 ( #13271, #53228, #20915, #86677, #46197, #34013, #91695, #17808, #9682, #104961, #31619, #48290, #88249, #80660, #71511, #97913, #55836, #89835, #23000, #13804, #88772, #14329, #5723, #32142, #46716, #96350, #62918, #15936, #47235, #80133, #6782, #6237, #5208, #65020, #14866, #70993, #47757, #56372, #81188, #104413, #24065, #30030, #56910, #7298, #54792, #38139, #39701, #40210, #39173, #89308, #103883, #22481, #64507, #55322, #30558, #72577, #97373, #73084, #105479, #72055, #79608, #38647, #105993, #23534, #79085, #15403, #95813, #31103, #63456, #21940, #87723, #63987, #96867, #66614, #33208, #99498, #57979, #16468, #50941, #98443, #1863, #26731, #25672, #50412, #90358, #83856, #1319, #57437, #42870, #83323, #17015, #58537, #48814, #59603, #92476, #7831, #81708, #49891, #82799, #40741, #49351, #74688, #17553, #73626, #8899, #41800, #106531, #75768, #75221, #91952, #25118, #32686, #82258, #9415, #771, #65554, #42333, #8371, #33739, #98959, #24590, #9967, #91439, #18082, #34282, #34821, #67155, #100569, #41273, #66080, #100040, #67687, #74163, #26208, #244, #90900, #59066, #45021, #52546, #60675, #68213, #77369, #27269, #84931, #19709, #20247, #77903, #61741, #101648, #84402, #19181, #53095, #11550, #76294, #86017, #52019, #3485, #68767, #35349, #86552, #69294, #94636, #102168, #4538, #12088, #70343, #11019, #2934, #44478, #37480, #62271, #36425, #101109, #51486, #93562, #4011, #85467, #28317, #60154, #61194, #93018, #43937, #94083, #36941, #69808, #76825, #102704, #27805, #35889, #78418, #28869, #20782, #2404, #29385, #53617, #12609, #45546, #103240, #10497, #18627, #43413, #87067, #104828, #72453, #64380, #87592, #81066, #46069, #7178, #97257, #70871, #21288, #71927, #23400, #104282, #105361, #54124, #38519, #80534, #71382, #13677, #30972, #6652, #56241, #63852, #22350, #29900, #62786, #89179, #96744, #15280, #22877, #39579, #30430, #95675, #95156, #55712, #13140, #55194, #6116, #79486, #39041, #63324, #21817, #48165, #38008, #40092, #72967, #88642, #14734, #54656, #105875, #47633, #103763, #32018, #31500, #96219, #78952, #5074, #46586, #5596, #88123, #14203, #47105, #80007, #1739, #65431, #90771, #33611 ),
 ( #83200, #98835, #34156, #58941, #99913, #50297, #644, #16889, #17422, #67032, #74039, #66483, #57316, #83721, #41682, #75637, #58401, #9296, #33091, #50815, #98325, #82672, #17954, #42208, #106398, #99361, #74570, #24481, #9829, #75090, #26083, #8244, #25543, #65956, #91313, #91833, #90234, #1185, #15811, #49769, #8777, #16339, #57845, #64894, #49225, #42746, #7704, #97781, #23947, #56787, #89712, #82126, #48692, #81578, #40615, #41156, #73499, #32559, #121, #24992, #52418, #93436, #20116, #10366, #84269, #11962, #10887, #67567, #35214, #28202, #43279, #45421, #19588, #102038, #100447, #85889, #92885, #60025, #34693, #76165, #2265, #85336, #3889, #18494, #61613, #51887, #61070, #93965, #44894, #11420, #27675, #59480, #52962, #44346, #77243, #101519, #68084, #36302, #102581, #77778, #36821, #53499, #86423, #28728, #100978, #69687, #19048, #26606, #69168, #3358, #94508, #35761, #27135, #20660, #12487, #78292, #84804, #92345, #51358, #68641, #43803, #76697, #2808, #60547, #63190, #37349, #87996, #6516, #13550, #88524, #70212, #54525, #96614, #87469, #29787, #46982, #22749, #80403, #79880, #38398, #45940, #78819, #39451, #14074, #72328, #5988, #55587, #46468, #4952, #4411, #38915, #29266, #71263, #22217, #95548, #55066, #79356, #37882, #105232, #54005, #64257, #89047, #71782, #104691, #70740, #31376, #63730, #13013, #97128, #30845, #5473, #14600, #103115, #15149, #48034, #62148, #95038, #104157, #30302, #21175, #103635, #96083, #47512, #86945, #23268, #56112, #62665, #21692, #514, #17297, #57186, #39968, #81456, #8647, #73907, #31888, #82543, #7570, #65826, #24344, #97645, #42079, #24860, #50171, #57711, #66902, #41551, #25957, #73367, #65299, #40455, #99786, #17826, #32957, #23813, #7051, #16208, #33479, #8111, #49091, #56658, #98705, #89583, #40488, #81993, #74435, #90637, #15676, #16745, #90102, #106265, #34029, #48565, #98189, #64770, #91708, #41024, #49636, #66353, #99237, #72839, #58816, #25405, #105750, #58265, #91190, #83074, #32428, #80941, #9165, #74962, #1054, #26474, #68501, #10758, #51218, #52291, #11830, #101911, #28068, #69559, #102449, #44760, #84143, #11287, #76037, #9699, #85202, #19456 ) ),
 .UNSPECIFIED., .F., .F., .F. ) 
 B_SPLINE_SURFACE_WITH_KNOTS ( ( 2, 2 ),
 ( 3, 2, 2, 2, 2, 2, 2, 2, 2, 2, 2, 2, 2, 2, 2, 2, 2, 2, 2, 2, 2, 2, 2, 2, 2, 2, 2, 2, 2, 2, 2, 2, 2, 2, 2, 2, 2, 2, 2, 2, 2, 2, 2, 2, 2, 2, 2, 2, 2, 2, 2, 2, 2, 2, 2, 2, 2, 2, 2, 2, 2, 2, 2, 2, 2, 2, 2, 2, 2, 2, 2, 2, 2, 2, 2, 2, 2, 2, 2, 2, 2, 2, 2, 2, 2, 2, 2, 2, 2, 2, 2, 2, 2, 2, 2, 2, 2, 2, 2, 2, 2, 2, 2, 2, 2, 2, 2, 2, 2, 2, 2, 2, 2, 2, 2, 2, 2, 2, 2, 2, 2, 2, 2, 2, 2, 2, 2, 2, 2, 2, 2, 2, 2, 2, 3 ),
 ( 0.000000000000000000, 1.000000000000000000 ),
 ( 0.000000000000000000, 0.007352941176470588133, 0.01470588235294117627, 0.02205882352941176613, 0.02941176470588235253, 0.03676470588235294240, 0.04411764705882353227, 0.05147058823529411520, 0.05882352941176470507, 0.06617647058823529493, 0.07352941176470588480, 0.08088235294117647467, 0.08823529411764706454, 0.09558823529411764053, 0.1029411764705882304, 0.1102941176470588203, 0.1176470588235294101, 0.1250000000000000000, 0.1323529411764705899, 0.1397058823529411797, 0.1470588235294117696, 0.1544117647058823595, 0.1617647058823529493, 0.1691176470588235392, 0.1764705882352941291, 0.1838235294117647189, 0.1911764705882352811, 0.1985294117647058709, 0.2058823529411764608, 0.2132352941176470507, 0.2205882352941176405, 0.2279411764705882304, 0.2352941176470588203, 0.2426470588235294101, 0.2500000000000000000, 0.2573529411764705621, 0.2647058823529411797, 0.2720588235294117418, 0.2794117647058823595, 0.2867647058823529216, 0.2941176470588235392, 0.3014705882352941013, 0.3088235294117647189, 0.3161764705882352811, 0.3235294117647058987, 0.3308823529411764608, 0.3382352941176470784, 0.3455882352941176405, 0.3529411764705882582, 0.3602941176470588203, 0.3676470588235294379, 0.3750000000000000000, 0.3823529411764705621, 0.3897058823529411797, 0.3970588235294117418, 0.4044117647058823595, 0.4117647058823529216, 0.4191176470588235392, 0.4264705882352941013, 0.4338235294117647189, 0.4411764705882352811, 0.4485294117647058987, 0.4558823529411764608, 0.4632352941176470784, 0.4705882352941176405, 0.4779411764705882582, 0.4852941176470588203, 0.4926470588235294379, 0.5000000000000000000, 0.5073529411764705621, 0.5147058823529411242, 0.5220588235294117974, 0.5294117647058823595, 0.5367647058823529216, 0.5441176470588234837, 0.5514705882352941568, 0.5588235294117647189, 0.5661764705882352811, 0.5735294117647058432, 0.5808823529411765163, 0.5882352941176470784, 0.5955882352941176405, 0.6029411764705882026, 0.6102941176470588758, 0.6176470588235294379, 0.6250000000000000000, 0.6323529411764705621, 0.6397058823529411242, 0.6470588235294117974, 0.6544117647058823595, 0.6617647058823529216, 0.6691176470588234837, 0.6764705882352941568, 0.6838235294117647189, 0.6911764705882352811, 0.6985294117647058432, 0.7058823529411765163, 0.7132352941176470784, 0.7205882352941176405, 0.7279411764705882026, 0.7352941176470588758, 0.7426470588235294379, 0.7500000000000000000, 0.7573529411764705621, 0.7647058823529411242, 0.7720588235294117974, 0.7794117647058823595, 0.7867647058823529216, 0.7941176470588234837, 0.8014705882352941568, 0.8088235294117647189, 0.8161764705882352811, 0.8235294117647058432, 0.8308823529411765163, 0.8382352941176470784, 0.8455882352941176405, 0.8529411764705882026, 0.8602941176470588758, 0.8676470588235294379, 0.8750000000000000000, 0.8823529411764705621, 0.8897058823529411242, 0.8970588235294117974, 0.9044117647058823595, 0.9117647058823529216, 0.9191176470588234837, 0.9264705882352941568, 0.9338235294117647189, 0.9411764705882352811, 0.9485294117647058432, 0.9558823529411765163, 0.9632352941176470784, 0.9705882352941176405, 0.9779411764705882026, 0.9804062415945057340 ),
 .UNSPECIFIED. ) 
 GEOMETRIC_REPRESENTATION_ITEM ( )  RATIONAL_B_SPLINE_SURFACE ( (
 ( 1.000000000000000000, 0.9238795325112867385, 1.000000000000000000, 0.9238795325112867385, 1.000000000000000000, 0.9238795325112867385, 1.000000000000000000, 0.9238795325112867385, 1.000000000000000000, 0.9238795325112867385, 1.000000000000000000, 0.9238795325112867385, 1.000000000000000000, 0.9238795325112867385, 1.000000000000000000, 0.9238795325112867385, 1.000000000000000000, 0.9238795325112867385, 1.000000000000000000, 0.9238795325112867385, 1.000000000000000000, 0.9238795325112867385, 1.000000000000000000, 0.9238795325112867385, 1.000000000000000000, 0.9238795325112867385, 1.000000000000000000, 0.9238795325112867385, 1.000000000000000000, 0.9238795325112867385, 1.000000000000000000, 0.9238795325112867385, 1.000000000000000000, 0.9238795325112867385, 1.000000000000000000, 0.9238795325112867385, 1.000000000000000000, 0.9238795325112867385, 1.000000000000000000, 0.9238795325112867385, 1.000000000000000000, 0.9238795325112867385, 1.000000000000000000, 0.9238795325112867385, 1.000000000000000000, 0.9238795325112867385, 1.000000000000000000, 0.9238795325112867385, 1.000000000000000000, 0.9238795325112867385, 1.000000000000000000, 0.9238795325112867385, 1.000000000000000000, 0.9238795325112867385, 1.000000000000000000, 0.9238795325112867385, 1.000000000000000000, 0.9238795325112867385, 1.000000000000000000, 0.9238795325112867385, 1.000000000000000000, 0.9238795325112867385, 1.000000000000000000, 0.9238795325112867385, 1.000000000000000000, 0.9238795325112867385, 1.000000000000000000, 0.9238795325112867385, 1.000000000000000000, 0.9238795325112867385, 1.000000000000000000, 0.9238795325112867385, 1.000000000000000000, 0.9238795325112867385, 1.000000000000000000, 0.9238795325112867385, 1.000000000000000000, 0.9238795325112867385, 1.000000000000000000, 0.9238795325112867385, 1.000000000000000000, 0.9238795325112867385, 1.000000000000000000, 0.9238795325112867385, 1.000000000000000000, 0.9238795325112867385, 1.000000000000000000, 0.9238795325112867385, 1.000000000000000000, 0.9238795325112867385, 1.000000000000000000, 0.9238795325112867385, 1.000000000000000000, 0.9238795325112867385, 1.000000000000000000, 0.9238795325112867385, 1.000000000000000000, 0.9238795325112867385, 1.000000000000000000, 0.9238795325112867385, 1.000000000000000000, 0.9238795325112867385, 1.000000000000000000, 0.9238795325112867385, 1.000000000000000000, 0.9238795325112867385, 1.000000000000000000, 0.9238795325112867385, 1.000000000000000000, 0.9238795325112867385, 1.000000000000000000, 0.9238795325112867385, 1.000000000000000000, 0.9238795325112867385, 1.000000000000000000, 0.9238795325112867385, 1.000000000000000000, 0.9238795325112867385, 1.000000000000000000, 0.9238795325112867385, 1.000000000000000000, 0.9238795325112867385, 1.000000000000000000, 0.9238795325112867385, 1.000000000000000000, 0.9238795325112867385, 1.000000000000000000, 0.9238795325112867385, 1.000000000000000000, 0.9238795325112867385, 1.000000000000000000, 0.9238795325112867385, 1.000000000000000000, 0.9238795325112867385, 1.000000000000000000, 0.9238795325112867385, 1.000000000000000000, 0.9238795325112867385, 1.000000000000000000, 0.9238795325112867385, 1.000000000000000000, 0.9238795325112867385, 1.000000000000000000, 0.9238795325112867385, 1.000000000000000000, 0.9238795325112867385, 1.000000000000000000, 0.9238795325112867385, 1.000000000000000000, 0.9238795325112867385, 1.000000000000000000, 0.9238795325112867385, 1.000000000000000000, 0.9238795325112867385, 1.000000000000000000, 0.9238795325112867385, 1.000000000000000000, 0.9238795325112867385, 1.000000000000000000, 0.9238795325112867385, 1.000000000000000000, 0.9238795325112867385, 1.000000000000000000, 0.9238795325112867385, 1.000000000000000000, 0.9238795325112867385, 1.000000000000000000, 0.9238795325112867385, 1.000000000000000000, 0.9238795325112867385, 1.000000000000000000, 0.9238795325112867385, 1.000000000000000000, 0.9238795325112867385, 1.000000000000000000, 0.9238795325112867385, 1.000000000000000000, 0.9238795325112867385, 1.000000000000000000, 0.9238795325112867385, 1.000000000000000000, 0.9238795325112867385, 1.000000000000000000, 0.9238795325112867385, 1.000000000000000000, 0.9238795325112867385, 1.000000000000000000, 0.9238795325112867385, 1.000000000000000000, 0.9238795325112867385, 1.000000000000000000, 0.9238795325112867385, 1.000000000000000000, 0.9238795325112867385, 1.000000000000000000, 0.9238795325112867385, 1.000000000000000000, 0.9238795325112867385, 1.000000000000000000, 0.9238795325112867385, 1.000000000000000000, 0.9238795325112867385, 1.000000000000000000, 0.9238795325112867385, 1.000000000000000000, 0.9238795325112867385, 1.000000000000000000, 0.9238795325112867385, 1.000000000000000000, 0.9238795325112867385, 1.000000000000000000, 0.9238795325112867385, 1.000000000000000000, 0.9238795325112867385, 1.000000000000000000, 0.9238795325112867385, 1.000000000000000000, 0.9238795325112867385, 1.000000000000000000, 0.9238795325112867385, 1.000000000000000000, 0.9238795325112867385, 1.000000000000000000, 0.9238795325112867385, 1.000000000000000000, 0.9238795325112867385, 1.000000000000000000, 0.9238795325112867385, 1.000000000000000000, 0.9238795325112867385, 1.000000000000000000, 0.9238795325112867385, 1.000000000000000000, 0.9238795325112867385, 1.000000000000000000, 0.9238795325112867385, 1.000000000000000000, 0.9238795325112867385, 1.000000000000000000, 0.9238795325112867385, 1.000000000000000000, 0.9238795325112867385, 1.000000000000000000, 0.9238795325112867385, 1.000000000000000000, 0.9238795325112867385, 1.000000000000000000, 0.9238795325112867385, 1.000000000000000000, 0.9238795325112867385, 1.000000000000000000, 0.9238795325112867385, 1.000000000000000000, 0.9238795325112867385, 1.000000000000000000, 0.9238795325112867385, 1.000000000000000000, 0.9238795325112867385, 1.000000000000000000, 0.9238795325112867385, 1.000000000000000000, 0.9238795325112867385, 1.000000000000000000, 0.9238795325112867385, 1.000000000000000000, 0.9238795325112867385, 1.000000000000000000, 0.9744807002913096206, 0.9660720326926630630),
 ( 1.000000000000000000, 0.9238795325112867385, 1.000000000000000000, 0.9238795325112867385, 1.000000000000000000, 0.9238795325112867385, 1.000000000000000000, 0.9238795325112867385, 1.000000000000000000, 0.9238795325112867385, 1.000000000000000000, 0.9238795325112867385, 1.000000000000000000, 0.9238795325112867385, 1.000000000000000000, 0.9238795325112867385, 1.000000000000000000, 0.9238795325112867385, 1.000000000000000000, 0.9238795325112867385, 1.000000000000000000, 0.9238795325112867385, 1.000000000000000000, 0.9238795325112867385, 1.000000000000000000, 0.9238795325112867385, 1.000000000000000000, 0.9238795325112867385, 1.000000000000000000, 0.9238795325112867385, 1.000000000000000000, 0.9238795325112867385, 1.000000000000000000, 0.9238795325112867385, 1.000000000000000000, 0.9238795325112867385, 1.000000000000000000, 0.9238795325112867385, 1.000000000000000000, 0.9238795325112867385, 1.000000000000000000, 0.9238795325112867385, 1.000000000000000000, 0.9238795325112867385, 1.000000000000000000, 0.9238795325112867385, 1.000000000000000000, 0.9238795325112867385, 1.000000000000000000, 0.9238795325112867385, 1.000000000000000000, 0.9238795325112867385, 1.000000000000000000, 0.9238795325112867385, 1.000000000000000000, 0.9238795325112867385, 1.000000000000000000, 0.9238795325112867385, 1.000000000000000000, 0.9238795325112867385, 1.000000000000000000, 0.9238795325112867385, 1.000000000000000000, 0.9238795325112867385, 1.000000000000000000, 0.9238795325112867385, 1.000000000000000000, 0.9238795325112867385, 1.000000000000000000, 0.9238795325112867385, 1.000000000000000000, 0.9238795325112867385, 1.000000000000000000, 0.9238795325112867385, 1.000000000000000000, 0.9238795325112867385, 1.000000000000000000, 0.9238795325112867385, 1.000000000000000000, 0.9238795325112867385, 1.000000000000000000, 0.9238795325112867385, 1.000000000000000000, 0.9238795325112867385, 1.000000000000000000, 0.9238795325112867385, 1.000000000000000000, 0.9238795325112867385, 1.000000000000000000, 0.9238795325112867385, 1.000000000000000000, 0.9238795325112867385, 1.000000000000000000, 0.9238795325112867385, 1.000000000000000000, 0.9238795325112867385, 1.000000000000000000, 0.9238795325112867385, 1.000000000000000000, 0.9238795325112867385, 1.000000000000000000, 0.9238795325112867385, 1.000000000000000000, 0.9238795325112867385, 1.000000000000000000, 0.9238795325112867385, 1.000000000000000000, 0.9238795325112867385, 1.000000000000000000, 0.9238795325112867385, 1.000000000000000000, 0.9238795325112867385, 1.000000000000000000, 0.9238795325112867385, 1.000000000000000000, 0.9238795325112867385, 1.000000000000000000, 0.9238795325112867385, 1.000000000000000000, 0.9238795325112867385, 1.000000000000000000, 0.9238795325112867385, 1.000000000000000000, 0.9238795325112867385, 1.000000000000000000, 0.9238795325112867385, 1.000000000000000000, 0.9238795325112867385, 1.000000000000000000, 0.9238795325112867385, 1.000000000000000000, 0.9238795325112867385, 1.000000000000000000, 0.9238795325112867385, 1.000000000000000000, 0.9238795325112867385, 1.000000000000000000, 0.9238795325112867385, 1.000000000000000000, 0.9238795325112867385, 1.000000000000000000, 0.9238795325112867385, 1.000000000000000000, 0.9238795325112867385, 1.000000000000000000, 0.9238795325112867385, 1.000000000000000000, 0.9238795325112867385, 1.000000000000000000, 0.9238795325112867385, 1.000000000000000000, 0.9238795325112867385, 1.000000000000000000, 0.9238795325112867385, 1.000000000000000000, 0.9238795325112867385, 1.000000000000000000, 0.9238795325112867385, 1.000000000000000000, 0.9238795325112867385, 1.000000000000000000, 0.9238795325112867385, 1.000000000000000000, 0.9238795325112867385, 1.000000000000000000, 0.9238795325112867385, 1.000000000000000000, 0.9238795325112867385, 1.000000000000000000, 0.9238795325112867385, 1.000000000000000000, 0.9238795325112867385, 1.000000000000000000, 0.9238795325112867385, 1.000000000000000000, 0.9238795325112867385, 1.000000000000000000, 0.9238795325112867385, 1.000000000000000000, 0.9238795325112867385, 1.000000000000000000, 0.9238795325112867385, 1.000000000000000000, 0.9238795325112867385, 1.000000000000000000, 0.9238795325112867385, 1.000000000000000000, 0.9238795325112867385, 1.000000000000000000, 0.9238795325112867385, 1.000000000000000000, 0.9238795325112867385, 1.000000000000000000, 0.9238795325112867385, 1.000000000000000000, 0.9238795325112867385, 1.000000000000000000, 0.9238795325112867385, 1.000000000000000000, 0.9238795325112867385, 1.000000000000000000, 0.9238795325112867385, 1.000000000000000000, 0.9238795325112867385, 1.000000000000000000, 0.9238795325112867385, 1.000000000000000000, 0.9238795325112867385, 1.000000000000000000, 0.9238795325112867385, 1.000000000000000000, 0.9238795325112867385, 1.000000000000000000, 0.9238795325112867385, 1.000000000000000000, 0.9238795325112867385, 1.000000000000000000, 0.9238795325112867385, 1.000000000000000000, 0.9238795325112867385, 1.000000000000000000, 0.9238795325112867385, 1.000000000000000000, 0.9238795325112867385, 1.000000000000000000, 0.9238795325112867385, 1.000000000000000000, 0.9238795325112867385, 1.000000000000000000, 0.9238795325112867385, 1.000000000000000000, 0.9238795325112867385, 1.000000000000000000, 0.9238795325112867385, 1.000000000000000000, 0.9238795325112867385, 1.000000000000000000, 0.9238795325112867385, 1.000000000000000000, 0.9238795325112867385, 1.000000000000000000, 0.9238795325112867385, 1.000000000000000000, 0.9238795325112867385, 1.000000000000000000, 0.9238795325112867385, 1.000000000000000000, 0.9238795325112867385, 1.000000000000000000, 0.9238795325112867385, 1.000000000000000000, 0.9238795325112867385, 1.000000000000000000, 0.9238795325112867385, 1.000000000000000000, 0.9238795325112867385, 1.000000000000000000, 0.9238795325112867385, 1.000000000000000000, 0.9238795325112867385, 1.000000000000000000, 0.9238795325112867385, 1.000000000000000000, 0.9238795325112867385, 1.000000000000000000, 0.9238795325112867385, 1.000000000000000000, 0.9744807002913096206, 0.9660720326926630630) ) ) 
 REPRESENTATION_ITEM ( '' )  SURFACE ( )  );
#64703=CARTESIAN_POINT ( 'NONE',  ( 5.082755093536325930, -10.34375000204838457, -5.082755093536325042 ) ) ;
#64745=CARTESIAN_POINT ( 'NONE',  ( -5.656854249492381470, -34.06249999999999289, 5.656854249492379694 ) ) ;
#64766=CARTESIAN_POINT ( 'NONE',  ( 7.002990960197232440, 106.0526681838345837, 3.868040364119523566 ) ) ;
#64770=CARTESIAN_POINT ( 'NONE',  ( -5.082755093536326818, -12.21875000204838635, 5.082755093536325042 ) ) ;
#64821=CARTESIAN_POINT ( 'NONE',  ( -2.977408999572654480, -14.00000000204838457, 7.188101187499999156 ) ) ;
#64828=CARTESIAN_POINT ( 'NONE',  ( 2.977408999572652260, -28.81250000204838813, 7.188101187500000044 ) ) ;
#64831=CARTESIAN_POINT ( 'NONE',  ( 7.188101187500000044, -27.03125000204838813, 0.000000000000000000 ) ) ;
#64846=VERTEX_POINT ( 'NONE', #52557 ) ;
#64866=CARTESIAN_POINT ( 'NONE',  ( 9.842473135306407883, 26.41068182886412785, 1.785129593756274113 ) ) ;
#64867=CARTESIAN_POINT ( 'NONE',  ( 7.188101187500001821, -26.93750000204838457, -2.977408999572650483 ) ) ;
#64875=CARTESIAN_POINT ( 'NONE',  ( -10.00000000000000178, 15.00000000000000000, -4.582575694955834500 ) ) ;
#64881=CARTESIAN_POINT ( 'NONE',  ( -7.188101187500000044, -13.90625000204838457, -8.802885111219163269E-16 ) ) ;
#64886=ADVANCED_FACE ( 'NONE', ( #77379 ), #82637, .F. ) ;
#64891=CARTESIAN_POINT ( 'NONE',  ( -3.313708498984726969, -18.96874999999998934, 8.000000000000039080 ) ) ;
#64894=CARTESIAN_POINT ( 'NONE',  ( -2.977408999572654480, -30.12500000204838813, 7.188101187499999156 ) ) ;
#64903=CARTESIAN_POINT ( 'NONE',  ( -9.918010731619574472, 88.79151684843223791, -1.300854425901573519 ) ) ;
#64910=CARTESIAN_POINT ( 'NONE',  ( -4.165977904505308693, 15.00000000000000000, 9.090909090909091717 ) ) ;
#64916=ORIENTED_EDGE ( 'NONE', *, *, #87900, .T. ) ;
#64917=LINE ( 'NONE', #7724, #80627 ) ;
#64946=CARTESIAN_POINT ( 'NONE',  ( 7.045755811259135193, 86.30341603013555130, 3.790843699961853552 ) ) ;
#64955=CARTESIAN_POINT ( 'NONE',  ( -7.188101187500002709, -19.81250000204838813, 2.977408999572648707 ) ) ;
#64957=CARTESIAN_POINT ( 'NONE',  ( 9.797537890442933772, 81.53442202333808098, 2.014215961808879296 ) ) ;
#64961=CARTESIAN_POINT ( 'NONE',  ( -8.000000000000000000, -13.43750000409676915, -9.797174393178825657E-16 ) ) ;
#65020=CARTESIAN_POINT ( 'NONE',  ( 8.000000000000000000, -30.59375000409677270, -3.313708498984761608 ) ) ;
#65036=CARTESIAN_POINT ( 'NONE',  ( 8.000000000000000000, -15.59375000409677270, -3.313708498984761164 ) ) ;
#65060=CARTESIAN_POINT ( 'NONE',  ( -7.744991119775237465, 33.46438785425129936, -2.016316005557099000 ) ) ;
#65076=ORIENTED_EDGE ( 'NONE', *, *, #90578, .T. ) ;
#65123=CARTESIAN_POINT ( 'NONE',  ( 9.165151389911677882, 105.2671078128291384, -4.000000000000000888 ) ) ;
#65143=CARTESIAN_POINT ( 'NONE',  ( -1.469576158976823947E-15, -15.87499999999999289, 8.000000000000000000 ) ) ;
#65209=CARTESIAN_POINT ( 'NONE',  ( -9.999999999997182698, 15.11700796860534268, -0.7408669144211869062 ) ) ;
#65211=CARTESIAN_POINT ( 'NONE',  ( -1.320432766682874540E-15, -28.53125000204838813, 7.188101187500000044 ) ) ;
#65273=CARTESIAN_POINT ( 'NONE',  ( 4.898587196589412829E-16, -34.62499999999999289, -8.000000000000000000 ) ) ;
#65292=CARTESIAN_POINT ( 'NONE',  ( 7.151597709147948123, 106.7892926505221283, 3.587174531012140566 ) ) ;
#65299=CARTESIAN_POINT ( 'NONE',  ( 7.188101187500001821, -14.56250000204838457, -2.977408999572650483 ) ) ;
#65315=VECTOR ( 'NONE', #33737, 1000.000000000000000 ) ;
#65325=FACE_OUTER_BOUND ( 'NONE', #53111, .T. ) ;
#65353=CARTESIAN_POINT ( 'NONE',  ( -5.082755093536325042, -15.96875000204838635, -5.082755093536325930 ) ) ;
#65362=CARTESIAN_POINT ( 'NONE',  ( -5.082755093536326818, -26.09375000204838813, 5.082755093536325042 ) ) ;
#65403=CARTESIAN_POINT ( 'NONE',  ( 4.401442555609581635E-16, -23.65625000204838457, -7.188101187500000044 ) ) ;
#65406=EDGE_LOOP ( 'NONE', ( #1949, #34704, #21591 ) ) ;
#65418=CARTESIAN_POINT ( 'NONE',  ( 5.082755093536325930, -12.96875000204838280, -5.082755093536325042 ) ) ;
#65419=CARTESIAN_POINT ( 'NONE',  ( 7.045965687440314262, 28.69607536213965560, 3.790395326974319357 ) ) ;
#65423=ORIENTED_EDGE ( 'NONE', *, *, #45808, .F. ) ;
#65427=CARTESIAN_POINT ( 'NONE',  ( -8.000000000000000000, -19.34374999999999289, -3.313708498984762496 ) ) ;
#65431=CARTESIAN_POINT ( 'NONE',  ( -5.656854249492381470, -8.750000004096769146, 5.656854249492379694 ) ) ;
#65433=CARTESIAN_POINT ( 'NONE',  ( 9.999999999999998224, 15.00000000000000000, -2.832769448823991188E-15 ) ) ;
#65493=CARTESIAN_POINT ( 'NONE',  ( 7.188101187500000044, -16.15625000204838457, 0.000000000000000000 ) ) ;
#65500=ORIENTED_EDGE ( 'NONE', *, *, #89607, .T. ) ;
#65512=CARTESIAN_POINT ( 'NONE',  ( 4.898587196589412829E-16, -19.81250000409677270, -8.000000000000000000 ) ) ;
#65515=ORIENTED_EDGE ( 'NONE', *, *, #8807, .T. ) ;
#65531=CARTESIAN_POINT ( 'NONE',  ( 0.000000000000000000, -30.00000000000000000, 0.000000000000000000 ) ) ;
#65554=CARTESIAN_POINT ( 'NONE',  ( 3.313708498984762052, -22.90625000409676915, -8.000000000000000000 ) ) ;
#65561=CARTESIAN_POINT ( 'NONE',  ( -3.082707893549470501, 15.00000000000000178, -9.999999999999998224 ) ) ;
#65593=CARTESIAN_POINT ( 'NONE',  ( -7.046289519167718396, 31.30591819944377008, -3.789821819998816288 ) ) ;
#65597=EDGE_CURVE ( 'NONE', #57731, #16013, #52382, .T. ) ;
#65601=CARTESIAN_POINT ( 'NONE',  ( -1.529297411792386763, -30.00000000000000711, 7.172883640994426990 ) ) ;
#65606=ADVANCED_FACE ( 'NONE', ( #27973, #43052, #75942, #93728 ), #20954, .T. ) ;
#65615=CARTESIAN_POINT ( 'NONE',  ( 4.165977904505310470, 16.00000000000000000, 9.090909090909089940 ) ) ;
#65660=CARTESIAN_POINT ( 'NONE',  ( 9.918512371096300129, 108.7928299227055220, -1.297150762882702146 ) ) ;
#65663=DIRECTION ( 'NONE',  ( -0.000000000000000000, -1.000000000000000000, -0.000000000000000000 ) ) ;
#65687=EDGE_LOOP ( 'NONE', ( #86729, #94144, #23286, #39778 ) ) ;
#65748=CARTESIAN_POINT ( 'NONE',  ( -7.188101187500001821, -33.50000000204838813, -2.977408999572651371 ) ) ;
#65805=CARTESIAN_POINT ( 'NONE',  ( -1.469576158976823947E-15, -29.37499999999999645, 8.000000000000000000 ) ) ;
#65808=ORIENTED_EDGE ( 'NONE', *, *, #25322, .F. ) ;
#65815=FACE_OUTER_BOUND ( 'NONE', #65406, .T. ) ;
#65826=CARTESIAN_POINT ( 'NONE',  ( -5.082755093536325042, -15.59375000204838635, -5.082755093536325930 ) ) ;
#65829=VERTEX_POINT ( 'NONE', #55706 ) ;
#65860=LINE ( 'NONE', #8683, #40491 ) ;
#65880=CARTESIAN_POINT ( 'NONE',  ( 2.977408999572652260, -10.81250000204838457, 7.188101187500000044 ) ) ;
#65883=CARTESIAN_POINT ( 'NONE',  ( 6.252586356923180766, -30.00000000000000000, 3.576699445452887094 ) ) ;
#65887=CARTESIAN_POINT ( 'NONE',  ( 2.977408999572650927, -22.25000000204839168, -7.188101187500001821 ) ) ;
#65904=CARTESIAN_POINT ( 'NONE',  ( -7.212408192734267587, 87.01517089320370246, -3.465038817813880012 ) ) ;
#65933=CARTESIAN_POINT ( 'NONE',  ( 5.082755093536324154, -24.21875000204838813, 5.082755093536326818 ) ) ;
#65944=CARTESIAN_POINT ( 'NONE',  ( -5.082755093536326818, -10.71875000204838457, 5.082755093536325042 ) ) ;
#65945=CARTESIAN_POINT ( 'NONE',  ( 7.999912353029506207, 26.00017529396907179, -0.2691822806794995637 ) ) ;
#65947=( BOUNDED_CURVE ( )  B_SPLINE_CURVE ( 2, ( #99874, #33569, #49184, #15768, #40578, #58906, #90194, #17387, #48650 ),
 .UNSPECIFIED., .F., .F. ) 
 B_SPLINE_CURVE_WITH_KNOTS ( ( 3, 2, 2, 2, 3 ),
 ( 0.3088235294117646634, 0.3161764705882352255, 0.3235294117647058432, 0.3308823529411764053, 0.3382352941176470229 ),
 .UNSPECIFIED. ) 
 CURVE ( )  GEOMETRIC_REPRESENTATION_ITEM ( )  RATIONAL_B_SPLINE_CURVE ( ( 1.000000000000000666, 0.9238795325112861834, 1.000000000000000000, 0.9238795325112867385, 1.000000000000000000, 0.9238795325112867385, 1.000000000000000000, 0.9238795325112872936, 0.9999999999999994449 ) ) 
 REPRESENTATION_ITEM ( '' )  );
#65956=CARTESIAN_POINT ( 'NONE',  ( 7.188101187500001821, -31.06250000204838813, -2.977408999572650483 ) ) ;
#66015=CARTESIAN_POINT ( 'NONE',  ( -7.188101187500001821, -21.50000000204839168, -2.977408999572651371 ) ) ;
#66017=CARTESIAN_POINT ( 'NONE',  ( 9.698972129396508990, 81.82370287258061126, -2.445345647270320999 ) ) ;
#66042=CARTESIAN_POINT ( 'NONE',  ( 4.582575694955839829, 16.00000000000000000, 10.00000000000000000 ) ) ;
#66044=EDGE_CURVE ( 'NONE', #44948, #47033, #81823, .T. ) ;
#66072=CARTESIAN_POINT ( 'NONE',  ( 5.082755093536325930, -29.46875000204838813, -5.082755093536325042 ) ) ;
#66079=CARTESIAN_POINT ( 'NONE',  ( -10.00000000000000355, 15.00000000000000000, -10.00000000000000000 ) ) ;
#66080=CARTESIAN_POINT ( 'NONE',  ( 8.000000000000000000, -21.59375000409677625, -3.313708498984761608 ) ) ;
#66087=CARTESIAN_POINT ( 'NONE',  ( -4.034557488803232062, 15.07443463110226212, -9.151133496028503345 ) ) ;
#66090=DIRECTION ( 'NONE',  ( -0.000000000000000000, -1.000000000000000000, -0.000000000000000000 ) ) ;
#66120=CARTESIAN_POINT ( 'NONE',  ( -7.002641335706727865, 31.05087262680831728, 3.868676264653293728 ) ) ;
#66137=ORIENTED_EDGE ( 'NONE', *, *, #56694, .F. ) ;
#66139=SURFACE_STYLE_USAGE ( .BOTH. , #82859 ) ;
#66177=ORIENTED_EDGE ( 'NONE', *, *, #43638, .T. ) ;
#66186=CARTESIAN_POINT ( 'NONE',  ( 9.165151389911679658, 105.0000000000000142, -4.000000000000001776 ) ) ;
#66203=CARTESIAN_POINT ( 'NONE',  ( -8.000000000000001776, -11.65624999999999289, 3.313708498984758943 ) ) ;
#66235=SURFACE_SIDE_STYLE ('',( #926 ) ) ;
#66236=CARTESIAN_POINT ( 'NONE',  ( -6.928203230275509661, 84.73520732746429474, 3.999999999999999112 ) ) ;
#66271=CARTESIAN_POINT ( 'NONE',  ( 7.188101187500000044, -31.15625000204838813, 0.000000000000000000 ) ) ;
#66288=VECTOR ( 'NONE', #17232, 1000.000000000000000 ) ;
#66332=CARTESIAN_POINT ( 'NONE',  ( 3.313708498984762496, -27.78124999999999289, 7.999999999999998224 ) ) ;
#66353=CARTESIAN_POINT ( 'NONE',  ( 5.082755093536324154, -11.84375000204838635, 5.082755093536326818 ) ) ;
#66407=CARTESIAN_POINT ( 'NONE',  ( -2.977408999572650039, -16.06250000204838457, -7.188101187500000933 ) ) ;
#66415=CARTESIAN_POINT ( 'NONE',  ( -2.977408999572650039, -19.06250000204838813, -7.188101187500001821 ) ) ;
#66461=CARTESIAN_POINT ( 'NONE',  ( 2.977408999572651815, -19.81250000204838813, 7.188101187500000933 ) ) ;
#66472=CARTESIAN_POINT ( 'NONE',  ( 2.977408999572650927, -9.875000002048388126, -7.188101187500000933 ) ) ;
#66473=DIRECTION ( 'NONE',  ( -1.000000000000000000, -0.000000000000000000, -0.000000000000000000 ) ) ;
#66483=CARTESIAN_POINT ( 'NONE',  ( -2.977408999572654480, -33.12500000204838813, 7.188101187499999156 ) ) ;
#66538=CARTESIAN_POINT ( 'NONE',  ( 7.801642220026312025, 88.58796826149033166, 1.787233835843583973 ) ) ;
#66547=CARTESIAN_POINT ( 'NONE',  ( 7.188101187500000044, -10.15625000204838457, 0.000000000000000000 ) ) ;
#66586=FACE_OUTER_BOUND ( 'NONE', #54969, .T. ) ;
#66607=CARTESIAN_POINT ( 'NONE',  ( -1.320432766682874540E-15, -22.53125000204838457, 7.188101187500000044 ) ) ;
#66614=CARTESIAN_POINT ( 'NONE',  ( -8.000000000000001776, -26.84375000409676915, 3.313708498984758943 ) ) ;
#66618=CARTESIAN_POINT ( 'NONE',  ( 9.176803346051508825, 30.52947155797438583, 3.973598758023531019 ) ) ;
#66621=CARTESIAN_POINT ( 'NONE',  ( -2.455962139888511420, 15.75268258782372754, -9.700350089084256666 ) ) ;
#66640=MECHANICAL_DESIGN_GEOMETRIC_PRESENTATION_REPRESENTATION('',(#77035),#56296);
#66657=CARTESIAN_POINT ( 'NONE',  ( -7.412906595240166929, 32.64188272852253903, 3.014362223629236670 ) ) ;
#66680=( NAMED_UNIT ( * ) SI_UNIT ( $, .STERADIAN. ) SOLID_ANGLE_UNIT ( ) );
#66700=CARTESIAN_POINT ( 'NONE',  ( 4.898587196589412829E-16, -28.81250000409677270, -8.000000000000000000 ) ) ;
#66715=CARTESIAN_POINT ( 'NONE',  ( 7.002641335706725201, 103.9491273731916294, 3.868676264653294172 ) ) ;
#66717=ORIENTED_EDGE ( 'NONE', *, *, #41767, .T. ) ;
#66718=ORIENTED_EDGE ( 'NONE', *, *, #43042, .F. ) ;
#66749=CARTESIAN_POINT ( 'NONE',  ( -7.344133061198929724, 102.5550560731942369, 3.176267128233874804 ) ) ;
#66781=CARTESIAN_POINT ( 'NONE',  ( -7.150931910075642328, 83.21374201477736676, -3.588457848165356623 ) ) ;
#66784=EDGE_CURVE ( 'NONE', #28968, #29729, #74018, .T. ) ;
#66787=VERTEX_POINT ( 'NONE', #55693 ) ;
#66805=CARTESIAN_POINT ( 'NONE',  ( -5.656854249492381470, -28.06249999999999645, 5.656854249492379694 ) ) ;
#66812=CARTESIAN_POINT ( 'NONE',  ( -5.082755093536325042, -29.09375000204838813, -5.082755093536325930 ) ) ;
#66837=ADVANCED_FACE ( 'NONE', ( #96721 ), #79987, .T. ) ;
#66842=ORIENTED_EDGE ( 'NONE', *, *, #50187, .T. ) ;
#66874=CARTESIAN_POINT ( 'NONE',  ( -5.656854249492379694, -25.43749999999999645, -5.656854249492380582 ) ) ;
#66896=CARTESIAN_POINT ( 'NONE',  ( 6.928203230275507885, 105.0000000000000000, -4.000000000000001776 ) ) ;
#66901=CARTESIAN_POINT ( 'NONE',  ( -9.989435848181784650, 88.97380292528423240, -0.5278651953175997891 ) ) ;
#66902=CARTESIAN_POINT ( 'NONE',  ( 2.977408999572651815, -14.93750000204838457, 7.188101187500000933 ) ) ;
#66932=ORIENTED_EDGE ( 'NONE', *, *, #4912, .T. ) ;
#66935=ORIENTED_EDGE ( 'NONE', *, *, #88247, .F. ) ;
#66958=CARTESIAN_POINT ( 'NONE',  ( -7.188101187500000933, -12.87500000204838813, -2.977408999572651371 ) ) ;
#66967=CARTESIAN_POINT ( 'NONE',  ( 7.188101187500000044, -18.03125000204838457, 0.000000000000000000 ) ) ;
#66991=CARTESIAN_POINT ( 'NONE',  ( -3.594029361870008099, -9.531975552773349847, 6.225090491531444670 ) ) ;
#67007=CARTESIAN_POINT ( 'NONE',  ( -1.320432766682874540E-15, -19.90625000204838457, 7.188101187500000044 ) ) ;
#67020=CARTESIAN_POINT ( 'NONE',  ( -7.188101187500000044, -9.406250002048384573, -8.802885111219163269E-16 ) ) ;
#67031=DIRECTION ( 'NONE',  ( 0.000000000000000000, 0.000000000000000000, 1.000000000000000000 ) ) ;
#67032=CARTESIAN_POINT ( 'NONE',  ( -7.188101187500002709, -33.31250000204838813, 2.977408999572648707 ) ) ;
#67063=VERTEX_POINT ( 'NONE', #11940 ) ;
#67088=FACE_BOUND ( 'NONE', #46038, .T. ) ;
#67089=CARTESIAN_POINT ( 'NONE',  ( 7.188101187500001821, -14.56250000204838457, -2.977408999572650483 ) ) ;
#67124=CARTESIAN_POINT ( 'NONE',  ( 7.550180524134852966, 81.99440752786813391, 2.651855549982491400 ) ) ;
#67146=CARTESIAN_POINT ( 'NONE',  ( 7.188101187500000044, -22.15625000204838457, 0.000000000000000000 ) ) ;
#67155=CARTESIAN_POINT ( 'NONE',  ( 5.656854249492378806, -21.87500000409676915, 5.656854249492381470 ) ) ;
#67214=CARTESIAN_POINT ( 'NONE',  ( -5.656854249492381470, -20.75000000409676915, 5.656854249492379694 ) ) ;
#67216=EDGE_CURVE ( 'NONE', #41081, #88535, #97363, .T. ) ;
#67223=( BOUNDED_CURVE ( )  B_SPLINE_CURVE ( 2, ( #26934, #101321, #9625, #60349, #27471, #75970, #93225, #19914, #19387 ),
 .UNSPECIFIED., .F., .F. ) 
 B_SPLINE_CURVE_WITH_KNOTS ( ( 3, 2, 2, 2, 3 ),
 ( 0.8382352941176473005, 0.8455882352941177516, 0.8529411764705883137, 0.8602941176470588758, 0.8676470588235294379 ),
 .UNSPECIFIED. ) 
 CURVE ( )  GEOMETRIC_REPRESENTATION_ITEM ( )  RATIONAL_B_SPLINE_CURVE ( ( 0.9999999999999976685, 0.9238795325112890700, 1.000000000000000000, 0.9238795325112867385, 1.000000000000000000, 0.9238795325112867385, 1.000000000000000000, 0.9238795325112867385, 1.000000000000000000 ) ) 
 REPRESENTATION_ITEM ( '' )  );
#67242=FACE_OUTER_BOUND ( 'NONE', #4824, .T. ) ;
#67245=CARTESIAN_POINT ( 'NONE',  ( -1.469576158976823947E-15, -23.37499999999999289, 8.000000000000000000 ) ) ;
#67287=CARTESIAN_POINT ( 'NONE',  ( -5.656854249492379694, -11.93749999999999289, -5.656854249492380582 ) ) ;
#67322=CARTESIAN_POINT ( 'NONE',  ( -7.344133061198930612, 82.55505607319422268, 3.176267128233873471 ) ) ;
#67347=ORIENTED_EDGE ( 'NONE', *, *, #5600, .F. ) ;
#67412=CARTESIAN_POINT ( 'NONE',  ( -3.313708498984760720, -25.53124999999999645, -8.000000000000000000 ) ) ;
#67423=DIRECTION ( 'NONE',  ( 0.000000000000000000, -0.000000000000000000, 1.000000000000000000 ) ) ;
#67432=CARTESIAN_POINT ( 'NONE',  ( 7.003653396366579464, 106.0570620555967594, -3.866846144092870752 ) ) ;
#67438=CARTESIAN_POINT ( 'NONE',  ( -10.00005432054556742, 89.00013580137914460, 0.2621623937322776765 ) ) ;
#67497=CARTESIAN_POINT ( 'NONE',  ( -2.977408999572650039, -23.56250000204839168, -7.188101187500001821 ) ) ;
#67512=CARTESIAN_POINT ( 'NONE',  ( -7.551437640244098581, 88.00872462522912087, -2.648272645923386293 ) ) ;
#67539=CARTESIAN_POINT ( 'NONE',  ( 7.188101187500000044, -19.53125000204838457, 0.000000000000000000 ) ) ;
#67552=CARTESIAN_POINT ( 'NONE',  ( -2.977408999572650039, -9.687500002048384573, -7.188101187500000933 ) ) ;
#67567=CARTESIAN_POINT ( 'NONE',  ( 2.977408999572650927, -27.87500000204838457, -7.188101187500001821 ) ) ;
#67577=DIRECTION ( 'NONE',  ( -0.000000000000000000, 1.000000000000000000, -0.000000000000000000 ) ) ;
#67590=AXIS2_PLACEMENT_3D ( 'NONE', #80629, #15373, #41243 ) ;
#67617=CARTESIAN_POINT ( 'NONE',  ( 5.082755093536324154, -22.71875000204838457, 5.082755093536326818 ) ) ;
#67625=CARTESIAN_POINT ( 'NONE',  ( 5.082755093536325930, -14.46875000204838457, -5.082755093536325042 ) ) ;
#67659=CARTESIAN_POINT ( 'NONE',  ( 6.928203230275506996, 84.73069070304462969, -4.000000000000000888 ) ) ;
#67677=CARTESIAN_POINT ( 'NONE',  ( -7.188101187500002709, -27.31250000204838457, 2.977408999572647819 ) ) ;
#67687=CARTESIAN_POINT ( 'NONE',  ( 3.313708498984762052, -21.40625000409677270, -8.000000000000000000 ) ) ;
#67696=CARTESIAN_POINT ( 'NONE',  ( -4.397168787612410590, 15.00000000000000000, -9.999999999999998224 ) ) ;
#67703=EDGE_CURVE ( 'NONE', #15011, #54845, #17724, .T. ) ;
#67729=EDGE_CURVE ( 'NONE', #56748, #49838, #7011, .T. ) ;
#67814=CARTESIAN_POINT ( 'NONE',  ( -7.213352437320216914, 102.9816352699231743, -3.463014597543483397 ) ) ;
#67817=CARTESIAN_POINT ( 'NONE',  ( 0.7018335428337041382, 15.23280014800325510, -9.981531048852462007 ) ) ;
#67852=CARTESIAN_POINT ( 'NONE',  ( -3.313708498984765161, -23.65625000409677625, 7.999999999999998224 ) ) ;
#67864=VECTOR ( 'NONE', #14321, 1000.000000000000000 ) ;
#67928=CARTESIAN_POINT ( 'NONE',  ( 5.656854249492380582, -22.81249999999999289, -5.656854249492379694 ) ) ;
#67929=CARTESIAN_POINT ( 'NONE',  ( 8.000000000000000000, -24.40624999999999645, -3.313708498984761608 ) ) ;
#67979=CARTESIAN_POINT ( 'NONE',  ( -8.000000000000000000, -25.24999999999999289, -9.797174393178825657E-16 ) ) ;
#68016=CARTESIAN_POINT ( 'NONE',  ( -1.320432766682874540E-15, -22.90625000204838457, 7.188101187500000044 ) ) ;
#68054=CARTESIAN_POINT ( 'NONE',  ( -7.188101187500002709, -20.18750000204838457, 2.977408999572648707 ) ) ;
#68061=EDGE_CURVE ( 'NONE', #37759, #71772, #93364, .T. ) ;
#68068=CARTESIAN_POINT ( 'NONE',  ( 9.918512371096300129, 88.79282992270555042, -1.297150762882697261 ) ) ;
#68073=CARTESIAN_POINT ( 'NONE',  ( 4.898587196589412829E-16, -24.12499999999999289, -8.000000000000000000 ) ) ;
#68084=CARTESIAN_POINT ( 'NONE',  ( 7.188101187500000044, -25.15625000204838813, 0.000000000000000000 ) ) ;
#68136=CARTESIAN_POINT ( 'NONE',  ( -5.082755093536325042, -26.46875000204838813, -5.082755093536325930 ) ) ;
#68145=CARTESIAN_POINT ( 'NONE',  ( 5.082755093536324154, -11.84375000204838635, 5.082755093536326818 ) ) ;
#68180=CARTESIAN_POINT ( 'NONE',  ( 6.928203230275510549, 85.00000000000000000, 4.000000000000000000 ) ) ;
#68189=DIRECTION ( 'NONE',  ( -1.734723475976807094E-16, 0.000000000000000000, -1.000000000000000000 ) ) ;
#68201=CARTESIAN_POINT ( 'NONE',  ( -1.320432766682874540E-15, -27.03125000204838813, 7.188101187500000044 ) ) ;
#68205=SURFACE_STYLE_FILL_AREA ( #10489 ) ;
#68210=CARTESIAN_POINT ( 'NONE',  ( -9.176803346051510601, 84.47052844202561062, 3.973598758023530131 ) ) ;
#68213=CARTESIAN_POINT ( 'NONE',  ( -1.469576158976823947E-15, -20.56250000409676915, 8.000000000000000000 ) ) ;
#68221=CARTESIAN_POINT ( 'NONE',  ( 9.165151389911677882, 30.26710781282912777, -4.000000000000000888 ) ) ;
#68225=CARTESIAN_POINT ( 'NONE',  ( 1.155400528493880197, -30.00000000000000711, -7.642489478904992417 ) ) ;
#68229=DIRECTION ( 'NONE',  ( -0.000000000000000000, 1.000000000000000000, -0.000000000000000000 ) ) ;
#68277=ORIENTED_EDGE ( 'NONE', *, *, #16596, .F. ) ;
#68285=CARTESIAN_POINT ( 'NONE',  ( -10.00000000000000355, 85.00000000000000000, 0.000000000000000000 ) ) ;
#68318=VECTOR ( 'NONE', #53470, 1000.000000000000000 ) ;
#68322=CARTESIAN_POINT ( 'NONE',  ( 5.656854249492380582, -15.31249999999999289, -5.656854249492379694 ) ) ;
#68329=CARTESIAN_POINT ( 'NONE',  ( -3.826931552919423662, 16.00000000000000000, -9.246279647933182133 ) ) ;
#68342=CARTESIAN_POINT ( 'NONE',  ( 4.898587196589412829E-16, -21.12499999999999289, -8.000000000000000000 ) ) ;
#68350=EDGE_CURVE ( 'NONE', #32259, #14808, #39479, .T. ) ;
#68351=EDGE_LOOP ( 'NONE', ( #79858, #27904 ) ) ;
#68372=PLANE ( 'NONE',  #43616 ) ;
#68374=SURFACE_SIDE_STYLE ('',( #20406 ) ) ;
#68384=CARTESIAN_POINT ( 'NONE',  ( -9.165151389911681434, 105.2631950629488387, 4.000000000000004441 ) ) ;
#68410=CARTESIAN_POINT ( 'NONE',  ( 0.000000000000000000, -30.00000000000000000, 8.000000000000000000 ) ) ;
#68415=DIRECTION ( 'NONE',  ( -0.000000000000000000, 1.000000000000000000, -0.000000000000000000 ) ) ;
#68424=DIRECTION ( 'NONE',  ( 0.000000000000000000, 0.000000000000000000, 1.000000000000000000 ) ) ;
#68436=DIRECTION ( 'NONE',  ( 0.4165977904505316354, 1.053856448911994735E-15, -0.9090909090909087276 ) ) ;
#68474=CARTESIAN_POINT ( 'NONE',  ( -5.656854249492379694, -22.43749999999999289, -5.656854249492380582 ) ) ;
#68495=CARTESIAN_POINT ( 'NONE',  ( 7.619135598915497631, 108.1730536778467808, 2.449260492474795825 ) ) ;
#68501=CARTESIAN_POINT ( 'NONE',  ( 2.977408999572651815, -10.43750000204838457, 7.188101187500000933 ) ) ;
#68507=VERTEX_POINT ( 'NONE', #54673 ) ;
#68555=AXIS2_PLACEMENT_3D ( 'NONE', #84337, #49832, #18020 ) ;
#68568=CARTESIAN_POINT ( 'NONE',  ( 7.188101187500000044, -12.03125000204838635, 0.000000000000000000 ) ) ;
#68588=CYLINDRICAL_SURFACE ( 'NONE', #54248, 4.000000000000000000 ) ;
#68598=DIRECTION ( 'NONE',  ( 0.000000000000000000, 0.000000000000000000, -1.000000000000000000 ) ) ;
#68601=EDGE_CURVE ( 'NONE', #9794, #13534, #46322, .T. ) ;
#68605=CARTESIAN_POINT ( 'NONE',  ( 8.000000000000000000, -21.40624999999999645, -3.313708498984761164 ) ) ;
#68609=CARTESIAN_POINT ( 'NONE',  ( -2.977408999572650039, -20.56250000204838457, -7.188101187500001821 ) ) ;
#68641=CARTESIAN_POINT ( 'NONE',  ( -7.188101187500001821, -23.00000000204839523, -2.977408999572651371 ) ) ;
#68659=CARTESIAN_POINT ( 'NONE',  ( 10.00005432054556742, 100.9998641986208838, 0.2621623937322780651 ) ) ;
#68690=CARTESIAN_POINT ( 'NONE',  ( -7.188101187500000044, -27.78125000204838813, -8.802885111219163269E-16 ) ) ;
#68700=CARTESIAN_POINT ( 'NONE',  ( -1.320432766682874540E-15, -12.03125000204838635, 7.188101187500000044 ) ) ;
#68704=CARTESIAN_POINT ( 'NONE',  ( -8.000000000000000000, -14.74999999999999289, -9.797174393178825657E-16 ) ) ;
#68734=CARTESIAN_POINT ( 'NONE',  ( 7.801339272325196639, 81.41268528040301078, -1.788609912539675495 ) ) ;
#68758=CARTESIAN_POINT ( 'NONE',  ( 5.082755093536324154, -23.84375000204838457, 5.082755093536326818 ) ) ;
#68767=CARTESIAN_POINT ( 'NONE',  ( 3.313708498984762496, -18.96875000409676915, 7.999999999999998224 ) ) ;
#68774=CARTESIAN_POINT ( 'NONE',  ( 7.122964895856751077, -30.00000000000000355, -0.9654893961775683486 ) ) ;
#68824=CARTESIAN_POINT ( 'NONE',  ( 7.188101187499999156, -29.75000000204838813, 2.977408999572654924 ) ) ;
#68827=CARTESIAN_POINT ( 'NONE',  ( -3.826949319562310325, 15.99999999999999645, 9.246271506234595705 ) ) ;
#68845=( LENGTH_UNIT ( ) NAMED_UNIT ( * ) SI_UNIT ( .MILLI., .METRE. ) );
#68893=EDGE_CURVE ( 'NONE', #94793, #7449, #60557, .T. ) ;
#69011=CARTESIAN_POINT ( 'NONE',  ( 5.656854249492378806, -23.18749999999999289, 5.656854249492381470 ) ) ;
#69040=CIRCLE ( 'NONE', #103291, 8.000000000000000000 ) ;
#69051=CARTESIAN_POINT ( 'NONE',  ( -3.999995229665001428, -8.688226215992830959, 6.928205984420947594 ) ) ;
#69091=CARTESIAN_POINT ( 'NONE',  ( 2.787519624836773513, -30.00000000000000711, 6.642210194323184602 ) ) ;
#69097=CARTESIAN_POINT ( 'NONE',  ( -5.082755093536326818, -17.09375000204838813, 5.082755093536325042 ) ) ;
#69139=CARTESIAN_POINT ( 'NONE',  ( 7.188101187499999156, -10.62500000204838813, 2.977408999572654924 ) ) ;
#69151=CARTESIAN_POINT ( 'NONE',  ( 9.989113211954167681, 88.97299273548998144, 0.5334031035449028346 ) ) ;
#69155=CARTESIAN_POINT ( 'NONE',  ( 8.000000000000000000, -28.90624999999999645, -3.313708498984761164 ) ) ;
#69158=ADVANCED_FACE ( 'NONE', ( #24867 ), #64265, .F. ) ;
#69159=ORIENTED_EDGE ( 'NONE', *, *, #75805, .T. ) ;
#69168=CARTESIAN_POINT ( 'NONE',  ( -1.320432766682874540E-15, -24.03125000204838457, 7.188101187500000044 ) ) ;
#69182=CARTESIAN_POINT ( 'NONE',  ( 3.313708498984781592, -21.96875000409677270, 7.999999999999979572 ) ) ;
#69187=CARTESIAN_POINT ( 'NONE',  ( 9.333079356992097786, 103.2216691992513091, 3.592383266237785477 ) ) ;
#69220=CARTESIAN_POINT ( 'NONE',  ( -2.977408999572654480, -23.00000000204839523, 7.188101187499999156 ) ) ;
#69229=CARTESIAN_POINT ( 'NONE',  ( -3.594029361870008099, -9.156975552773349847, 6.225090491531445558 ) ) ;
#69235=CARTESIAN_POINT ( 'NONE',  ( -7.551437640244095029, 108.0087246252290498, -2.648272645923386737 ) ) ;
#69270=CARTESIAN_POINT ( 'NONE',  ( -2.977408999572654480, -29.00000000204838813, 7.188101187499999156 ) ) ;
#69284=CARTESIAN_POINT ( 'NONE',  ( 2.977408999572652260, -19.43750000204838457, 7.188101187500000044 ) ) ;
#69290=DIRECTION ( 'NONE',  ( 0.000000000000000000, 0.000000000000000000, 1.000000000000000000 ) ) ;
#69294=CARTESIAN_POINT ( 'NONE',  ( 8.000000000000000000, -18.68750000409676915, 0.000000000000000000 ) ) ;
#69299=CARTESIAN_POINT ( 'NONE',  ( 9.482993638194542996, 32.44348720253677243, -3.177441187500463560 ) ) ;
#69353=CARTESIAN_POINT ( 'NONE',  ( -7.188101187500002709, -27.31250000204838457, 2.977408999572648707 ) ) ;
#69359=CARTESIAN_POINT ( 'NONE',  ( 4.898587196589412829E-16, -18.12499999999999645, -8.000000000000000000 ) ) ;
#69401=CIRCLE ( 'NONE', #74526, 10.00000000000000000 ) ;
#69419=CARTESIAN_POINT ( 'NONE',  ( -7.413471587080149305, 102.3564784083167183, -3.013058070223554541 ) ) ;
#69423=EDGE_CURVE ( 'NONE', #65829, #94586, #61979, .T. ) ;
#69438=LINE ( 'NONE', #53246, #6851 ) ;
#69448=CARTESIAN_POINT ( 'NONE',  ( -9.797537890442933772, 108.4655779766619048, 2.014215961808881517 ) ) ;
#69470=CARTESIAN_POINT ( 'NONE',  ( 3.313708498984762496, -14.46875000409676915, 7.999999999999998224 ) ) ;
#69534=CARTESIAN_POINT ( 'NONE',  ( 8.000000000000000000, -22.99999999999999289, 0.000000000000000000 ) ) ;
#69559=CARTESIAN_POINT ( 'NONE',  ( 4.401442555609581635E-16, -9.781250002048384573, -7.188101187500000044 ) ) ;
#69561=CARTESIAN_POINT ( 'NONE',  ( 4.898587196589412829E-16, -24.31250000409677270, -8.000000000000000000 ) ) ;
#69586=CARTESIAN_POINT ( 'NONE',  ( -10.00000000000000000, 15.00000000000000000, 10.00000000000000000 ) ) ;
#69587=CARTESIAN_POINT ( 'NONE',  ( -3.313708498984726969, -11.46874999999999289, 8.000000000000039080 ) ) ;
#69590=CARTESIAN_POINT ( 'NONE',  ( -5.656854249492379694, -26.93749999999999645, -5.656854249492380582 ) ) ;
#69605=CARTESIAN_POINT ( 'NONE',  ( -9.177080501238306098, 104.4665305714573122, -3.972956046786645601 ) ) ;
#69613=EDGE_LOOP ( 'NONE', ( #105900, #28562, #102177, #5573 ) ) ;
#69617=ADVANCED_FACE ( 'NONE', ( #26375 ), #93190, .T. ) ;
#69624=CARTESIAN_POINT ( 'NONE',  ( 4.401442555609581635E-16, -14.65625000204838457, -7.188101187500000044 ) ) ;
#69661=CARTESIAN_POINT ( 'NONE',  ( 2.977408999572651815, -12.31250000204838635, 7.188101187500000933 ) ) ;
#69667=CARTESIAN_POINT ( 'NONE',  ( 9.999952458099484076, 88.99988114523867466, 0.2653554233229086234 ) ) ;
#69687=CARTESIAN_POINT ( 'NONE',  ( -7.188101187500002709, -24.31250000204838813, 2.977408999572648707 ) ) ;
#69719=CARTESIAN_POINT ( 'NONE',  ( -1.469576158976823947E-15, -26.56250000409677270, 8.000000000000000000 ) ) ;
#69738=CARTESIAN_POINT ( 'NONE',  ( 7.188101187500000044, -24.03125000204838457, 0.000000000000000000 ) ) ;
#69747=CARTESIAN_POINT ( 'NONE',  ( 7.188101187500001821, -34.43750000204838813, -2.977408999572650483 ) ) ;
#69751=CARTESIAN_POINT ( 'NONE',  ( -7.414346147791995634, 107.6458915766226312, -3.010818766110534117 ) ) ;
#69787=CARTESIAN_POINT ( 'NONE',  ( 7.188101187500000044, -28.53125000204838813, 0.000000000000000000 ) ) ;
#69795=ORIENTED_EDGE ( 'NONE', *, *, #89523, .F. ) ;
#69799=CARTESIAN_POINT ( 'NONE',  ( -7.188101187500002709, -19.81250000204838457, 2.977408999572647819 ) ) ;
#69805=CARTESIAN_POINT ( 'NONE',  ( -9.221346651730840449, 83.95165979931661582, -3.869102247876030631 ) ) ;
#69808=CARTESIAN_POINT ( 'NONE',  ( -8.000000000000000000, -16.43750000409677270, -9.797174393178825657E-16 ) ) ;
#69810=CARTESIAN_POINT ( 'NONE',  ( 9.216463528758549018, 15.13241195026089692, 3.884543032214307079 ) ) ;
#69825=CIRCLE ( 'NONE', #4375, 8.000000000000000000 ) ;
#69858=EDGE_CURVE ( 'NONE', #44397, #70179, #17324, .T. ) ;
#69873=CARTESIAN_POINT ( 'NONE',  ( 7.188101187500001821, -23.56250000204838813, -2.977408999572650483 ) ) ;
#69876=CARTESIAN_POINT ( 'NONE',  ( -5.656854249492379694, -23.93749999999999289, -5.656854249492380582 ) ) ;
#69879=CARTESIAN_POINT ( 'NONE',  ( -5.656854249492381470, -17.56249999999999645, 5.656854249492379694 ) ) ;
#69935=EDGE_LOOP ( 'NONE', ( #40706, #19360 ) ) ;
#69961=PRESENTATION_STYLE_ASSIGNMENT (( #37098 ) ) ;
#70046=LINE ( 'NONE', #21527, #34446 ) ;
#70054=CARTESIAN_POINT ( 'NONE',  ( 5.656854249492378806, -21.68749999999999645, 5.656854249492381470 ) ) ;
#70103=CARTESIAN_POINT ( 'NONE',  ( 4.898587196589412829E-16, -27.31250000409677270, -8.000000000000000000 ) ) ;
#70127=DIRECTION ( 'NONE',  ( 0.000000000000000000, 0.000000000000000000, 1.000000000000000000 ) ) ;
#70129=CARTESIAN_POINT ( 'NONE',  ( 3.487646406148289913, 15.95332971149351842, -9.373884331925008695 ) ) ;
#70143=VERTEX_POINT ( 'NONE', #55235 ) ;
#70146=CARTESIAN_POINT ( 'NONE',  ( 2.977408999572650927, -13.25000000204838280, -7.188101187500001821 ) ) ;
#70151=TOROIDAL_SURFACE ( 'NONE', #23669, 11.00000000000000000, 1.000000000000000000 ) ;
#70179=VERTEX_POINT ( 'NONE', #31016 ) ;
#70185=CARTESIAN_POINT ( 'NONE',  ( -7.188101187500002709, -15.68750000204838457, 2.977408999572648707 ) ) ;
#70193=CARTESIAN_POINT ( 'NONE',  ( 9.334514330295430540, 86.78622737681789090, -3.588704711590611218 ) ) ;
#70204=MECHANICAL_DESIGN_GEOMETRIC_PRESENTATION_REPRESENTATION('',(#16861),#58179);
#70212=CARTESIAN_POINT ( 'NONE',  ( 5.082755093536325930, -21.96875000204838457, -5.082755093536325042 ) ) ;
#70234=CARTESIAN_POINT ( 'NONE',  ( 9.842473135306409660, 101.4106818288640994, 1.785129593756277666 ) ) ;
#70265=CARTESIAN_POINT ( 'NONE',  ( -1.320432766682874540E-15, -18.40625000204838457, 7.188101187500000044 ) ) ;
#70277=CARTESIAN_POINT ( 'NONE',  ( 4.401442555609581635E-16, -32.65625000204838813, -7.188101187500000044 ) ) ;
#70286=VERTEX_POINT ( 'NONE', #63366 ) ;
#70320=CARTESIAN_POINT ( 'NONE',  ( -5.082755093536326818, -32.09375000204838813, 5.082755093536325042 ) ) ;
#70332=CARTESIAN_POINT ( 'NONE',  ( 7.188101187499999156, -16.25000000204838457, 2.977408999572654924 ) ) ;
#70343=CARTESIAN_POINT ( 'NONE',  ( -3.313708498984760720, -18.21875000409676915, -8.000000000000000000 ) ) ;
#70345=FILL_AREA_STYLE_COLOUR ( '', #30231 ) ;
#70348=CARTESIAN_POINT ( 'NONE',  ( -9.165151389911681434, 84.99999999999998579, -4.000000000000000000 ) ) ;
#70354=( BOUNDED_CURVE ( )  B_SPLINE_CURVE ( 2, ( #29057, #69470, #70527, #30083, #13327, #46251, #87778, #13860, #4730 ),
 .UNSPECIFIED., .F., .F. ) 
 B_SPLINE_CURVE_WITH_KNOTS ( ( 3, 2, 2, 2, 3 ),
 ( 0.7500000000000000000, 0.7573529411764705621, 0.7647058823529411242, 0.7720588235294117974, 0.7794117647058823595 ),
 .UNSPECIFIED. ) 
 CURVE ( )  GEOMETRIC_REPRESENTATION_ITEM ( )  RATIONAL_B_SPLINE_CURVE ( ( 1.000000000000000000, 0.9238795325112867385, 1.000000000000000000, 0.9238795325112867385, 1.000000000000000000, 0.9238795325112867385, 1.000000000000000000, 0.9238795325112867385, 1.000000000000000000 ) ) 
 REPRESENTATION_ITEM ( '' )  );
#70383=VECTOR ( 'NONE', #50700, 1000.000000000000000 ) ;
#70407=CARTESIAN_POINT ( 'NONE',  ( 5.082755093536325930, -27.96875000204838457, -5.082755093536325042 ) ) ;
#70452=ORIENTED_EDGE ( 'NONE', *, *, #95678, .F. ) ;
#70527=CARTESIAN_POINT ( 'NONE',  ( 5.656854249492378806, -14.37500000409677092, 5.656854249492381470 ) ) ;
#70565=EDGE_LOOP ( 'NONE', ( #4188, #66718, #22646, #94891 ) ) ;
#70580=LINE ( 'NONE', #102942, #2914 ) ;
#70588=ORIENTED_EDGE ( 'NONE', *, *, #101340, .T. ) ;
#70593=CARTESIAN_POINT ( 'NONE',  ( -3.313708498984760720, -22.53124999999999289, -8.000000000000000000 ) ) ;
#70661=CARTESIAN_POINT ( 'NONE',  ( 3.572352985695238292, 15.21714514899076143, -9.341953373612907896 ) ) ;
#70669=ORIENTED_EDGE ( 'NONE', *, *, #31759, .T. ) ;
#70675=CARTESIAN_POINT ( 'NONE',  ( 5.082755093536325930, -13.34375000204838457, -5.082755093536325042 ) ) ;
#70711=CARTESIAN_POINT ( 'NONE',  ( -6.928203230275510549, 30.00000000000000000, 4.000000000000000000 ) ) ;
#70718=CARTESIAN_POINT ( 'NONE',  ( 7.188101187500001821, -11.93750000204838457, -2.977408999572650483 ) ) ;
#70740=CARTESIAN_POINT ( 'NONE',  ( 4.401442555609581635E-16, -18.78125000204838457, -7.188101187500000044 ) ) ;
#70743=CARTESIAN_POINT ( 'NONE',  ( -9.165151389911679658, 30.00000000000000000, 4.000000000000000000 ) ) ;
#70793=CARTESIAN_POINT ( 'NONE',  ( -2.977408999572654480, -17.00000000204838813, 7.188101187499999156 ) ) ;
#70796=CARTESIAN_POINT ( 'NONE',  ( -5.656854249492381470, -26.75000000409677625, 5.656854249492379694 ) ) ;
#70802=CARTESIAN_POINT ( 'NONE',  ( 7.188101187500000044, -34.53125000204838813, 0.000000000000000000 ) ) ;
#70809=CARTESIAN_POINT ( 'NONE',  ( -7.046289519167720172, 106.3059181994437949, -3.789821819998815400 ) ) ;
#70823=CARTESIAN_POINT ( 'NONE',  ( -10.00000000000000000, 15.00000000000000000, 10.00000000000000000 ) ) ;
#70846=CARTESIAN_POINT ( 'NONE',  ( -5.082755093536325042, -30.96875000204838813, -5.082755093536325930 ) ) ;
#70853=( BOUNDED_CURVE ( )  B_SPLINE_CURVE ( 2, ( #68342, #18210, #76409, #70857, #51606, #52138, #84526, #37995, #59190 ),
 .UNSPECIFIED., .F., .F. ) 
 B_SPLINE_CURVE_WITH_KNOTS ( ( 3, 2, 2, 2, 3 ),
 ( 0.5441176470588235947, 0.5514705882352942679, 0.5588235294117648300, 0.5661764705882353921, 0.5735294117647059542 ),
 .UNSPECIFIED. ) 
 CURVE ( )  GEOMETRIC_REPRESENTATION_ITEM ( )  RATIONAL_B_SPLINE_CURVE ( ( 0.9999999999999988898, 0.9238795325112878487, 1.000000000000000000, 0.9238795325112867385, 1.000000000000000000, 0.9238795325112867385, 1.000000000000000000, 0.9238795325112856283, 1.000000000000001110 ) ) 
 REPRESENTATION_ITEM ( '' )  );
#70857=CARTESIAN_POINT ( 'NONE',  ( -8.000000000000000000, -20.84374999999998934, -3.313708498984762496 ) ) ;
#70861=CARTESIAN_POINT ( 'NONE',  ( 7.188101187499999156, -20.75000000204839523, 2.977408999572654924 ) ) ;
#70871=CARTESIAN_POINT ( 'NONE',  ( 5.656854249492380582, -14.00000000409677092, -5.656854249492379694 ) ) ;
#70876=CARTESIAN_POINT ( 'NONE',  ( -9.948513602187993854, 33.86977943343858044, 1.045942665286128115 ) ) ;
#70910=ORIENTED_EDGE ( 'NONE', *, *, #64126, .T. ) ;
#70927=CARTESIAN_POINT ( 'NONE',  ( 5.082755093536325930, -26.46875000204838813, -5.082755093536325042 ) ) ;
#70993=CARTESIAN_POINT ( 'NONE',  ( 3.313708498984762052, -30.40625000409677270, -8.000000000000000000 ) ) ;
#71020=ORIENTED_EDGE ( 'NONE', *, *, #31116, .T. ) ;
#71049=CARTESIAN_POINT ( 'NONE',  ( 4.898587196589412829E-16, -12.31250000409676915, -8.000000000000000000 ) ) ;
#71051=EDGE_CURVE ( 'NONE', #72025, #80543, #69040, .T. ) ;
#71070=VERTEX_POINT ( 'NONE', #29966 ) ;
#71091=CARTESIAN_POINT ( 'NONE',  ( 9.253500431420432548, 106.2977154991770874, 3.792688295761953210 ) ) ;
#71114=CARTESIAN_POINT ( 'NONE',  ( 8.000000000000000000, -12.49999999999999289, 0.000000000000000000 ) ) ;
#71127=EDGE_CURVE ( 'NONE', #33604, #89525, #102803, .T. ) ;
#71159=CARTESIAN_POINT ( 'NONE',  ( -9.989113211954165905, 26.02700726451005764, 0.5334031035449032787 ) ) ;
#71160=CARTESIAN_POINT ( 'NONE',  ( 4.898587196589412829E-16, -27.12499999999999645, -8.000000000000000000 ) ) ;
#71201=CARTESIAN_POINT ( 'NONE',  ( 7.999999999999998224, -24.59374999999999289, 3.313708498984766049 ) ) ;
#71211=ORIENTED_EDGE ( 'NONE', *, *, #33574, .F. ) ;
#71229=CARTESIAN_POINT ( 'NONE',  ( -7.801642220026310248, 26.41203173850967900, 1.787233835843583751 ) ) ;
#71236=CARTESIAN_POINT ( 'NONE',  ( -2.977408999572650039, -13.06250000204838280, -7.188101187500001821 ) ) ;
#71263=CARTESIAN_POINT ( 'NONE',  ( -7.188101187500000044, -19.90625000204838457, -8.802885111219163269E-16 ) ) ;
#71269=EDGE_CURVE ( 'NONE', #94312, #79080, #61128, .T. ) ;
#71304=EDGE_CURVE ( 'NONE', #70286, #103221, #50472, .T. ) ;
#71310=EDGE_LOOP ( 'NONE', ( #17985, #38673, #37813, #92486 ) ) ;
#71312=CARTESIAN_POINT ( 'NONE',  ( -2.977408999572654480, -21.50000000204839523, 7.188101187499999156 ) ) ;
#71322=CARTESIAN_POINT ( 'NONE',  ( 4.401442555609581635E-16, -25.15625000204838813, -7.188101187500000044 ) ) ;
#71328=CARTESIAN_POINT ( 'NONE',  ( -7.896165657598942289, 108.7891113137197152, -1.307894402814546941 ) ) ;
#71359=CARTESIAN_POINT ( 'NONE',  ( -1.320432766682874540E-15, -31.90625000204838813, 7.188101187500000044 ) ) ;
#71374=CARTESIAN_POINT ( 'NONE',  ( -2.977408999572650039, -20.18750000204838813, -7.188101187500000933 ) ) ;
#71382=CARTESIAN_POINT ( 'NONE',  ( -3.313708498984765161, -13.15625000409676915, 7.999999999999998224 ) ) ;
#71392=CARTESIAN_POINT ( 'NONE',  ( -0.7768758660234635904, 15.00000000000000000, 9.999999999999998224 ) ) ;
#71445=CARTESIAN_POINT ( 'NONE',  ( 7.188101187500001821, -26.56250000204838457, -2.977408999572650483 ) ) ;
#71511=CARTESIAN_POINT ( 'NONE',  ( 5.656854249492378806, -32.37500000409676915, 5.656854249492381470 ) ) ;
#71573=LINE ( 'NONE', #99428, #97672 ) ;
#71575=AXIS2_PLACEMENT_3D ( 'NONE', #97997, #88853, #56994 ) ;
#71599=( BOUNDED_CURVE ( )  B_SPLINE_CURVE ( 2, ( #5944, #46427, #79312, #53961, #4908, #86380, #61567, #55021, #30257 ),
 .UNSPECIFIED., .F., .F. ) 
 B_SPLINE_CURVE_WITH_KNOTS ( ( 3, 2, 2, 2, 3 ),
 ( 0.6323529411764705621, 0.6397058823529411242, 0.6470588235294116863, 0.6544117647058822484, 0.6617647058823528106 ),
 .UNSPECIFIED. ) 
 CURVE ( )  GEOMETRIC_REPRESENTATION_ITEM ( )  RATIONAL_B_SPLINE_CURVE ( ( 1.000000000000000000, 0.9238795325112867385, 1.000000000000000000, 0.9238795325112867385, 1.000000000000000000, 0.9238795325112867385, 1.000000000000000000, 0.9238795325112878487, 0.9999999999999988898 ) ) 
 REPRESENTATION_ITEM ( '' )  );
#71618=CARTESIAN_POINT ( 'NONE',  ( 8.000000000000000000, -24.68750000409677270, 0.000000000000000000 ) ) ;
#71631=CARTESIAN_POINT ( 'NONE',  ( 3.313708498984762496, -14.28124999999999289, 7.999999999999998224 ) ) ;
#71656=CARTESIAN_POINT ( 'NONE',  ( 9.999999999998589573, 15.11700796859322260, -0.7408669144231687653 ) ) ;
#71691=CARTESIAN_POINT ( 'NONE',  ( -9.090909090909093493, 16.00000000000000000, -4.165977904505303364 ) ) ;
#71748=CARTESIAN_POINT ( 'NONE',  ( 7.551560007654698481, 33.00910351806991372, -2.648022159607831938 ) ) ;
#71757=CARTESIAN_POINT ( 'NONE',  ( 5.656854249492378806, -33.68749999999999289, 5.656854249492381470 ) ) ;
#71772=VERTEX_POINT ( 'NONE', #17892 ) ;
#71782=CARTESIAN_POINT ( 'NONE',  ( 5.082755093536325930, -18.96875000204838457, -5.082755093536325042 ) ) ;
#71837=CARTESIAN_POINT ( 'NONE',  ( -7.188101187500000933, -17.37500000204838813, -2.977408999572651371 ) ) ;
#71844=CARTESIAN_POINT ( 'NONE',  ( -5.082755093536326818, -29.09375000204838813, 5.082755093536325042 ) ) ;
#71847=CARTESIAN_POINT ( 'NONE',  ( -1.320432766682874540E-15, -24.40625000204838813, 7.188101187500000044 ) ) ;
#71853=CARTESIAN_POINT ( 'NONE',  ( -6.928203230275509661, 105.2652615693258724, 4.000000000000001776 ) ) ;
#71896=CARTESIAN_POINT ( 'NONE',  ( -7.188101187500001821, -23.37500000204839168, -2.977408999572651371 ) ) ;
#71905=DIRECTION ( 'NONE',  ( 0.000000000000000000, 0.000000000000000000, 1.000000000000000000 ) ) ;
#71912=CARTESIAN_POINT ( 'NONE',  ( -7.188101187500002709, -13.81250000204838457, 2.977408999572647819 ) ) ;
#71913=CARTESIAN_POINT ( 'NONE',  ( 6.928203230275512325, 29.73473843067414890, 4.000000000000002665 ) ) ;
#71917=B_SPLINE_CURVE_WITH_KNOTS ( 'NONE', 3,
 ( #98882, #98372, #82178, #16939, #64946, #56839, #89764, #73015, #15861, #25043, #8294, #34207, #66538, #8826, #99412, #57899, #48739, #90823, #25594, #49817, #41200, #58452, #82722, #42251, #81632, #7756, #40664, #73548, #41730, #74614, #106452, #83248, #57365, #48216 ),
 .UNSPECIFIED., .F., .F.,
 ( 4, 2, 2, 2, 2, 2, 2, 2, 2, 2, 2, 2, 2, 2, 2, 2, 4 ),
 ( 0.01272238763756221303, 0.01351613129786393037, 0.01430987495816564946, 0.01510361861846736681, 0.01589736227876908589, 0.01669110593907080498, 0.01748484959937252059, 0.01827859325967423967, 0.01907233691997595876, 0.01986608058027767437, 0.02065982424057939346, 0.02145356790088111254, 0.02224731156118282815, 0.02304105522148454724, 0.02383479888178626632, 0.02462854254208798194, 0.02542228620238970102 ),
 .UNSPECIFIED. ) ;
#71921=CARTESIAN_POINT ( 'NONE',  ( 0.000000000000000000, 15.00000000000000000, 0.000000000000000000 ) ) ;
#71927=CARTESIAN_POINT ( 'NONE',  ( 4.898587196589412829E-16, -13.81250000409676915, -8.000000000000000000 ) ) ;
#71937=CARTESIAN_POINT ( 'NONE',  ( -1.404490565849160877, 15.46725112412266334, 9.926810856659404436 ) ) ;
#71945=CARTESIAN_POINT ( 'NONE',  ( -1.469576158976823947E-15, -10.06250000409677092, 8.000000000000000000 ) ) ;
#71988=CARTESIAN_POINT ( 'NONE',  ( 5.082755093536324154, -20.84375000204838813, 5.082755093536326818 ) ) ;
#72010=CARTESIAN_POINT ( 'NONE',  ( -1.469576158976823947E-15, -19.06250000409677270, 8.000000000000000000 ) ) ;
#72025=VERTEX_POINT ( 'NONE', #5678 ) ;
#72046=CARTESIAN_POINT ( 'NONE',  ( -1.320432766682874540E-15, -28.53125000204838813, 7.188101187500000044 ) ) ;
#72055=CARTESIAN_POINT ( 'NONE',  ( -3.313708498984765161, -28.15625000409677270, 7.999999999999998224 ) ) ;
#72097=CARTESIAN_POINT ( 'NONE',  ( -8.000000000000000000, -21.03125000409677625, -3.313708498984762496 ) ) ;
#72128=CARTESIAN_POINT ( 'NONE',  ( -10.00000000000000355, 30.00000000000000000, 4.000000000000000000 ) ) ;
#72133=EDGE_LOOP ( 'NONE', ( #43545, #50468, #88856, #100892 ) ) ;
#72179=CARTESIAN_POINT ( 'NONE',  ( 4.898587196589412829E-16, -16.62499999999999289, -8.000000000000000000 ) ) ;
#72188=AXIS2_PLACEMENT_3D ( 'NONE', #56119, #15156, #57195 ) ;
#72189=CARTESIAN_POINT ( 'NONE',  ( 0.000000000000000000, 15.00000000000000000, 0.000000000000000000 ) ) ;
#72241=FACE_OUTER_BOUND ( 'NONE', #4101, .T. ) ;
#72300=CARTESIAN_POINT ( 'NONE',  ( -5.656854249492381470, -32.56249999999999289, 5.656854249492379694 ) ) ;
#72328=CARTESIAN_POINT ( 'NONE',  ( 7.188101187500000044, -20.65625000204838813, 0.000000000000000000 ) ) ;
#72333=ORIENTED_EDGE ( 'NONE', *, *, #61015, .T. ) ;
#72350=EDGE_CURVE ( 'NONE', #16013, #1287, #6379, .T. ) ;
#72360=DIRECTION ( 'NONE',  ( 1.000000000000000000, -0.000000000000000000, -0.000000000000000000 ) ) ;
#72374=CARTESIAN_POINT ( 'NONE',  ( 7.188101187499999156, -19.62500000204838457, 2.977408999572654924 ) ) ;
#72383=CARTESIAN_POINT ( 'NONE',  ( -2.977408999572654480, -29.00000000204838813, 7.188101187499999156 ) ) ;
#72427=CARTESIAN_POINT ( 'NONE',  ( 9.797537890442935549, 26.53442202333808098, 2.014215961808872635 ) ) ;
#72428=CARTESIAN_POINT ( 'NONE',  ( -5.082755093536326818, -27.59375000204838813, 5.082755093536325042 ) ) ;
#72442=CARTESIAN_POINT ( 'NONE',  ( -1.320432766682874540E-15, -15.03125000204838457, 7.188101187500000044 ) ) ;
#72453=CARTESIAN_POINT ( 'NONE',  ( -3.313708498984765161, -14.65625000409677092, 7.999999999999998224 ) ) ;
#72456=CARTESIAN_POINT ( 'NONE',  ( -3.313708498984726969, -15.96874999999998934, 8.000000000000039080 ) ) ;
#72475=EDGE_CURVE ( 'NONE', #89014, #84193, #80485, .T. ) ;
#72509=CARTESIAN_POINT ( 'NONE',  ( 9.999999999999998224, 16.00000000000000000, -4.582575694955843382 ) ) ;
#72513=CARTESIAN_POINT ( 'NONE',  ( 5.082755093536325930, -17.46875000204838457, -5.082755093536325042 ) ) ;
#72532=CARTESIAN_POINT ( 'NONE',  ( -8.000000000000000000, -19.53125000409677625, -3.313708498984762496 ) ) ;
#72577=CARTESIAN_POINT ( 'NONE',  ( -8.000000000000000000, -28.53125000409677270, -3.313708498984762496 ) ) ;
#72581=CARTESIAN_POINT ( 'NONE',  ( 9.948181520647858989, 33.86892802760377919, 1.049088206181486349 ) ) ;
#72583=FILL_AREA_STYLE_COLOUR ( '', #33214 ) ;
#72615=CARTESIAN_POINT ( 'NONE',  ( -7.986539162393899716, 33.97327171057451523, -0.5321833565149886036 ) ) ;
#72624=CARTESIAN_POINT ( 'NONE',  ( -0.2767341851108402473, -29.99999999999997868, 7.278698476187087429 ) ) ;
#72633=CARTESIAN_POINT ( 'NONE',  ( 3.827754797005777032, 15.98931925350938243, 9.240220675753764823 ) ) ;
#72667=CARTESIAN_POINT ( 'NONE',  ( 7.212408192734265810, 102.9848291067962975, -3.465038817813881789 ) ) ;
#72700=CARTESIAN_POINT ( 'NONE',  ( 5.656854249492378806, -15.68749999999999289, 5.656854249492381470 ) ) ;
#72737=VERTEX_POINT ( 'NONE', #81878 ) ;
#72739=CARTESIAN_POINT ( 'NONE',  ( -9.090909090909093493, 16.00000000000000000, 4.165977904505304252 ) ) ;
#72774=CARTESIAN_POINT ( 'NONE',  ( -2.977408999572654480, -11.00000000204838635, 7.188101187499999156 ) ) ;
#72814=LINE ( 'NONE', #105721, #9266 ) ;
#72815=CARTESIAN_POINT ( 'NONE',  ( -5.656854249492379694, -34.43749999999999289, -5.656854249492380582 ) ) ;
#72839=CARTESIAN_POINT ( 'NONE',  ( 7.188101187500000044, -11.65625000204838635, 0.000000000000000000 ) ) ;
#72874=EDGE_CURVE ( 'NONE', #76534, #106390, #60345, .T. ) ;
#72882=EDGE_CURVE ( 'NONE', #65829, #29277, #14561, .T. ) ;
#72889=CARTESIAN_POINT ( 'NONE',  ( 2.977408999572650927, -13.25000000204838280, -7.188101187500000933 ) ) ;
#72900=CARTESIAN_POINT ( 'NONE',  ( -7.188101187500000044, -26.28125000204838813, -8.802885111219163269E-16 ) ) ;
#72905=CARTESIAN_POINT ( 'NONE',  ( -7.211357414135265209, 107.0114653993443596, 3.467230644691329466 ) ) ;
#72932=ADVANCED_FACE ( 'NONE', ( #84780 ), #50790, .T. ) ;
#72940=CARTESIAN_POINT ( 'NONE',  ( 9.999945253488240482, 26.00013686629467458, -0.2662901834230989584 ) ) ;
#72942=CARTESIAN_POINT ( 'NONE',  ( 7.188101187500001821, -23.93750000204838457, -2.977408999572650483 ) ) ;
#72957=CARTESIAN_POINT ( 'NONE',  ( 7.188101187499999156, -10.25000000204838813, 2.977408999572654924 ) ) ;
#72967=CARTESIAN_POINT ( 'NONE',  ( -8.000000000000000000, -10.53125000409677092, -3.313708498984762496 ) ) ;
#73015=CARTESIAN_POINT ( 'NONE',  ( 7.344133061198929724, 87.44494392680577732, 3.176267128233873027 ) ) ;
#73024=CARTESIAN_POINT ( 'NONE',  ( 7.188101187500001821, -22.06250000204838813, -2.977408999572650483 ) ) ;
#73026=CARTESIAN_POINT ( 'NONE',  ( 9.220915120640585272, 83.95545113567915507, -3.870126578504838655 ) ) ;
#73029=CARTESIAN_POINT ( 'NONE',  ( -8.000000000000000000, -13.53125000409676915, -3.313708498984762496 ) ) ;
#73031=ORIENTED_EDGE ( 'NONE', *, *, #42489, .T. ) ;
#73042=CARTESIAN_POINT ( 'NONE',  ( -5.656854249492379694, -19.62500000409677270, -5.656854249492380582 ) ) ;
#73084=CARTESIAN_POINT ( 'NONE',  ( -8.000000000000001776, -28.34375000409677270, 3.313708498984758943 ) ) ;
#73087=CARTESIAN_POINT ( 'NONE',  ( 9.797936955406312265, 33.46671689770484193, -2.012343231877598448 ) ) ;
#73091=CARTESIAN_POINT ( 'NONE',  ( -8.000000000000000000, -10.24999999999999112, -9.797174393178825657E-16 ) ) ;
#73178=CARTESIAN_POINT ( 'NONE',  ( 7.934883677559675164, 101.1316082206244715, 1.051380792122692753 ) ) ;
#73217=CARTESIAN_POINT ( 'NONE',  ( -5.656854249492379694, -16.43749999999999289, -5.656854249492380582 ) ) ;
#73240=CARTESIAN_POINT ( 'NONE',  ( 9.700350089084272653, 15.75268258782372754, -2.455962139888437701 ) ) ;
#73281=CARTESIAN_POINT ( 'NONE',  ( -9.673800154114784888, 15.30085158940939039, -2.563280883359615903 ) ) ;
#73283=CARTESIAN_POINT ( 'NONE',  ( 7.188101187500001821, -31.06250000204838813, -2.977408999572650483 ) ) ;
#73300=CARTESIAN_POINT ( 'NONE',  ( 2.977408999572651815, -10.81250000204838457, 7.188101187500000933 ) ) ;
#73302=COLOUR_RGB ( '', 0.40784314, 0.44705882, 0.49803922) ;
#73317=ORIENTED_EDGE ( 'NONE', *, *, #86312, .T. ) ;
#73343=CARTESIAN_POINT ( 'NONE',  ( -5.656854249492381470, -31.06249999999999645, 5.656854249492379694 ) ) ;
#73367=CARTESIAN_POINT ( 'NONE',  ( 7.188101187500000044, -14.65625000204838457, 0.000000000000000000 ) ) ;
#73421=CARTESIAN_POINT ( 'NONE',  ( -7.188101187500000044, -11.28125000204838457, -8.802885111219163269E-16 ) ) ;
#73433=CARTESIAN_POINT ( 'NONE',  ( 7.188101187500001821, -28.43750000204839168, -2.977408999572650483 ) ) ;
#73465=EDGE_CURVE ( 'NONE', #76534, #28165, #26036, .T. ) ;
#73472=CARTESIAN_POINT ( 'NONE',  ( 7.188101187499999156, -24.12500000204838457, 2.977408999572654924 ) ) ;
#73486=CARTESIAN_POINT ( 'NONE',  ( -7.188101187500002709, -15.31250000204838813, 2.977408999572647819 ) ) ;
#73487=CARTESIAN_POINT ( 'NONE',  ( 7.618844049274132502, 26.82764101070540264, 2.450177051822847840 ) ) ;
#73497=EDGE_CURVE ( 'NONE', #9794, #25439, #10738, .T. ) ;
#73499=CARTESIAN_POINT ( 'NONE',  ( -7.188101187500000044, -28.90625000204838813, -8.802885111219163269E-16 ) ) ;
#73548=CARTESIAN_POINT ( 'NONE',  ( 7.213352437320216914, 87.01836473007681150, -3.463014597543481621 ) ) ;
#73560=CARTESIAN_POINT ( 'NONE',  ( 2.977408999572650927, -17.37500000204838457, -7.188101187500001821 ) ) ;
#73562=CARTESIAN_POINT ( 'NONE',  ( 9.645512969475857901, 81.98896849324276559, -2.645801731561386205 ) ) ;
#73618=CARTESIAN_POINT ( 'NONE',  ( 7.188101187499999156, -29.75000000204838813, 2.977408999572654924 ) ) ;
#73626=CARTESIAN_POINT ( 'NONE',  ( -8.000000000000000000, -24.03125000409677270, -3.313708498984762496 ) ) ;
#73634=CARTESIAN_POINT ( 'NONE',  ( -3.827754797006719834, 15.98931925350938243, -9.240220675753395341 ) ) ;
#73645=CARTESIAN_POINT ( 'NONE',  ( 7.999999999999998224, -15.78125000409677092, 3.313708498984766049 ) ) ;
#73680=CARTESIAN_POINT ( 'NONE',  ( -7.869731216972585486, -29.99999999999999645, 0.3816394668114562738 ) ) ;
#73724=ORIENTED_EDGE ( 'NONE', *, *, #2506, .T. ) ;
#73737=CARTESIAN_POINT ( 'NONE',  ( 9.699189539447123920, 108.1769222824671175, -2.444343703917212007 ) ) ;
#73746=DIRECTION ( 'NONE',  ( -0.000000000000000000, -1.000000000000000000, -0.000000000000000000 ) ) ;
#73752=ORIENTED_EDGE ( 'NONE', *, *, #74125, .T. ) ;
#73758=CARTESIAN_POINT ( 'NONE',  ( -3.313708498984760720, -10.53124999999999112, -8.000000000000000000 ) ) ;
#73761=CARTESIAN_POINT ( 'NONE',  ( -8.000113193197769590, 100.9997736135413788, -0.2613481123984672250 ) ) ;
#73804=CARTESIAN_POINT ( 'NONE',  ( -5.656854249492381470, -29.56249999999999645, 5.656854249492379694 ) ) ;
#73828=CARTESIAN_POINT ( 'NONE',  ( 2.977408999572650927, -29.37500000204838457, -7.188101187500001821 ) ) ;
#73885=CARTESIAN_POINT ( 'NONE',  ( -8.000000000000000000, -32.84375000000000000, -3.313708498984762496 ) ) ;
#73907=CARTESIAN_POINT ( 'NONE',  ( 5.082755093536325930, -15.96875000204838635, -5.082755093536325042 ) ) ;
#73939=ORIENTED_EDGE ( 'NONE', *, *, #91432, .F. ) ;
#73961=CARTESIAN_POINT ( 'NONE',  ( -2.977408999572650039, -13.06250000204838280, -7.188101187500000933 ) ) ;
#73964=CARTESIAN_POINT ( 'NONE',  ( 6.817771574508174837, -30.00000000000000000, 2.289596480420060143 ) ) ;
#73968=CARTESIAN_POINT ( 'NONE',  ( 7.188101187500001821, -20.93750000204838457, -2.977408999572650483 ) ) ;
#73984=CARTESIAN_POINT ( 'NONE',  ( -7.986452802927059835, 88.97309757691886034, 0.5332468218996367915 ) ) ;
#74010=DIRECTION ( 'NONE',  ( -0.000000000000000000, -1.000000000000000000, -0.000000000000000000 ) ) ;
#74011=CARTESIAN_POINT ( 'NONE',  ( 9.948561005166128624, 26.13009726251801723, -1.045755304005140607 ) ) ;
#74012=CARTESIAN_POINT ( 'NONE',  ( 2.977408999572651815, -25.81250000204838813, 7.188101187500000933 ) ) ;
#74018=LINE ( 'NONE', #56765, #2962 ) ;
#74022=VECTOR ( 'NONE', #37720, 1000.000000000000000 ) ;
#74024=CARTESIAN_POINT ( 'NONE',  ( 9.797372177749755551, 88.46509494847563815, 2.014953862275842944 ) ) ;
#74028=CARTESIAN_POINT ( 'NONE',  ( -7.188101187500000933, -11.00000000204838635, -2.977408999572651371 ) ) ;
#74039=CARTESIAN_POINT ( 'NONE',  ( -5.082755093536326818, -33.21875000204838813, 5.082755093536325042 ) ) ;
#74095=CARTESIAN_POINT ( 'NONE',  ( -1.320432766682874540E-15, -21.03125000204838457, 7.188101187500000044 ) ) ;
#74125=EDGE_CURVE ( 'NONE', #60867, #63010, #104306, .T. ) ;
#74163=CARTESIAN_POINT ( 'NONE',  ( 4.898587196589412829E-16, -21.31250000409676915, -8.000000000000000000 ) ) ;
#74170=CARTESIAN_POINT ( 'NONE',  ( -0.7768758660234609259, 15.00000000000000000, -9.999999999999998224 ) ) ;
#74201=CARTESIAN_POINT ( 'NONE',  ( -6.943926999490791729, 30.53300992626148158, -3.973092371898545139 ) ) ;
#74248=CARTESIAN_POINT ( 'NONE',  ( -5.656854249492381470, -28.25000000409677270, 5.656854249492379694 ) ) ;
#74258=CARTESIAN_POINT ( 'NONE',  ( 6.943926999490790841, 104.4669900737385291, -3.973092371898547803 ) ) ;
#74271=CARTESIAN_POINT ( 'NONE',  ( 9.989690267985800176, 108.9744441659491088, -0.5238310916885804414 ) ) ;
#74322=( NAMED_UNIT ( * ) PLANE_ANGLE_UNIT ( ) SI_UNIT ( $, .RADIAN. ) );
#74353=CARTESIAN_POINT ( 'NONE',  ( -5.082755093536325042, -32.09375000204838813, -5.082755093536325930 ) ) ;
#74385=ORIENTED_EDGE ( 'NONE', *, *, #21019, .T. ) ;
#74411=CARTESIAN_POINT ( 'NONE',  ( -8.000000000000000000, -28.24999999999999645, -9.797174393178825657E-16 ) ) ;
#74431=CARTESIAN_POINT ( 'NONE',  ( 7.619753052866894194, 108.1745150280717382, -2.447276542590450354 ) ) ;
#74435=CARTESIAN_POINT ( 'NONE',  ( 7.188101187500001821, -13.06250000204838280, -2.977408999572650483 ) ) ;
#74492=CARTESIAN_POINT ( 'NONE',  ( 7.188101187500000044, -15.03125000204838457, 0.000000000000000000 ) ) ;
#74501=CARTESIAN_POINT ( 'NONE',  ( -2.977408999572654480, -18.50000000204838457, 7.188101187499999156 ) ) ;
#74525=FACE_OUTER_BOUND ( 'NONE', #42649, .T. ) ;
#74526=AXIS2_PLACEMENT_3D ( 'NONE', #19385, #83000, #68424 ) ;
#74541=CARTESIAN_POINT ( 'NONE',  ( 9.989435848181784650, 26.02619707471574273, -0.5278651953176120015 ) ) ;
#74543=CARTESIAN_POINT ( 'NONE',  ( 7.188101187499999156, -16.62500000204838457, 2.977408999572654924 ) ) ;
#74563=DIRECTION ( 'NONE',  ( 1.000000000000000000, -0.000000000000000000, -0.000000000000000000 ) ) ;
#74565=COLOUR_RGB ( '', 0.72549020, 0.75294118, 0.79215686) ;
#74569=DIRECTION ( 'NONE',  ( -0.000000000000000000, 1.000000000000000000, -0.000000000000000000 ) ) ;
#74570=CARTESIAN_POINT ( 'NONE',  ( -5.082755093536326818, -31.71875000204838457, 5.082755093536325042 ) ) ;
#74575=CARTESIAN_POINT ( 'NONE',  ( -9.380871178326124493, 32.01116379798327216, 3.467392232194196566 ) ) ;
#74612=ORIENTED_EDGE ( 'NONE', *, *, #47518, .T. ) ;
#74614=CARTESIAN_POINT ( 'NONE',  ( 7.046357527897575856, 86.30615650601002642, -3.789683693877207826 ) ) ;
#74624=DIRECTION ( 'NONE',  ( -0.000000000000000000, -1.000000000000000000, -0.000000000000000000 ) ) ;
#74625=CARTESIAN_POINT ( 'NONE',  ( 5.082755093536324154, -10.34375000204838457, 5.082755093536326818 ) ) ;
#74654=DIRECTION ( 'NONE',  ( 0.9090909090909091717, -7.226819671346018786E-16, 0.4165977904505309137 ) ) ;
#74680=CARTESIAN_POINT ( 'NONE',  ( 5.082755093536324154, -26.84375000204838813, 5.082755093536326818 ) ) ;
#74681=ADVANCED_FACE ( 'NONE', ( #10632 ), #17688, .T. ) ;
#74688=CARTESIAN_POINT ( 'NONE',  ( -3.313708498984760720, -24.21875000409677625, -8.000000000000000000 ) ) ;
#74693=CARTESIAN_POINT ( 'NONE',  ( 9.537291425704607306, 32.64404377332772356, 3.012810007365997578 ) ) ;
#74697=CARTESIAN_POINT ( 'NONE',  ( -3.409011323176792896, 15.24615751665884744, -9.403185743875123848 ) ) ;
#74700=DIRECTION ( 'NONE',  ( 0.000000000000000000, 0.000000000000000000, 1.000000000000000000 ) ) ;
#74715=FACE_OUTER_BOUND ( 'NONE', #61627, .T. ) ;
#74730=CARTESIAN_POINT ( 'NONE',  ( -7.800703710507059796, 33.58595692657940646, 1.791736796405271281 ) ) ;
#74746=B_SPLINE_CURVE_WITH_KNOTS ( 'NONE', 3,
 ( #70711, #29753, #104659, #87963, #86910, #47476, #23238, #12980, #103602, #105199, #7019, #56076, #71229, #30811, #21656, #62627, #96584, #14044, #45908, #80373, #89018, #55556, #14570, #38365, #88492, #22718, #96053, #6486, #15114, #95515, #54492, #104125, #39417, #87437 ),
 .UNSPECIFIED., .F., .F.,
 ( 4, 2, 2, 2, 2, 2, 2, 2, 2, 2, 2, 2, 2, 2, 2, 2, 4 ),
 ( 0.01272238763756220956, 0.01351613129786392691, 0.01430987495816564425, 0.01510361861846736334, 0.01589736227876908242, 0.01669110593907079804, 0.01748484959937251712, 0.01827859325967423620, 0.01907233691997595182, 0.01986608058027766743, 0.02065982424057938652, 0.02145356790088110560, 0.02224731156118282122, 0.02304105522148454030, 0.02383479888178625938, 0.02462854254208797500, 0.02542228620238969408 ),
 .UNSPECIFIED. ) ;
#74770=FACE_OUTER_BOUND ( 'NONE', #70565, .T. ) ;
#74785=CARTESIAN_POINT ( 'NONE',  ( 7.801339272325196639, 101.4126852804029966, -1.788609912539668834 ) ) ;
#74795=CARTESIAN_POINT ( 'NONE',  ( 9.646083234704169840, 108.0129060902347646, -2.643797197754291783 ) ) ;
#74825=CARTESIAN_POINT ( 'NONE',  ( 0.000000000000000000, -30.00000000000000000, 0.000000000000000000 ) ) ;
#74860=DIRECTION ( 'NONE',  ( 0.000000000000000000, 0.000000000000000000, 1.000000000000000000 ) ) ;
#74875=CARTESIAN_POINT ( 'NONE',  ( 5.082755093536325930, -33.96875000204838813, -5.082755093536325042 ) ) ;
#74903=CARTESIAN_POINT ( 'NONE',  ( -10.00000000000000000, 0.000000000000000000, 10.00000000000000000 ) ) ;
#74926=ORIENTED_EDGE ( 'NONE', *, *, #91001, .T. ) ;
#74938=CARTESIAN_POINT ( 'NONE',  ( 8.000000000000000000, -25.90624999999999645, -3.313708498984761608 ) ) ;
#74951=CARTESIAN_POINT ( 'NONE',  ( 0.000000000000000000, 15.00000000000000000, 0.000000000000000000 ) ) ;
#74961=CARTESIAN_POINT ( 'NONE',  ( -1.469576158976823947E-15, -15.87499999999999289, 8.000000000000000000 ) ) ;
#74962=CARTESIAN_POINT ( 'NONE',  ( -5.082755093536326818, -10.71875000204838457, 5.082755093536325042 ) ) ;
#74991=ORIENTED_EDGE ( 'NONE', *, *, #15864, .F. ) ;
#75016=CARTESIAN_POINT ( 'NONE',  ( 5.082755093536325930, -13.34375000204838457, -5.082755093536325042 ) ) ;
#75023=CARTESIAN_POINT ( 'NONE',  ( -1.320432766682874540E-15, -18.40625000204838457, 7.188101187500000044 ) ) ;
#75068=CARTESIAN_POINT ( 'NONE',  ( -7.188101187500000044, -20.28125000204838813, -8.802885111219163269E-16 ) ) ;
#75090=CARTESIAN_POINT ( 'NONE',  ( 2.977408999572651815, -31.43750000204839168, 7.188101187500000933 ) ) ;
#75095=CARTESIAN_POINT ( 'NONE',  ( -9.165151389911679658, 30.00000000000000000, 4.000000000000000000 ) ) ;
#75154=CARTESIAN_POINT ( 'NONE',  ( 7.188101187500001821, -13.06250000204838280, -2.977408999572650483 ) ) ;
#75159=CARTESIAN_POINT ( 'NONE',  ( 6.928203230275509661, 105.0000000000000000, 4.000000000000001776 ) ) ;
#75189=CARTESIAN_POINT ( 'NONE',  ( 7.986539162393899716, 81.02672828942547767, -0.5321833565149893808 ) ) ;
#75214=CARTESIAN_POINT ( 'NONE',  ( 7.188101187500000933, -23.56250000204838457, -2.977408999572650483 ) ) ;
#75221=CARTESIAN_POINT ( 'NONE',  ( -1.469576158976823947E-15, -23.56250000409677270, 8.000000000000000000 ) ) ;
#75226=CARTESIAN_POINT ( 'NONE',  ( 9.221346651730838673, 31.04834020068337708, -3.869102247876034184 ) ) ;
#75236=B_SPLINE_CURVE_WITH_KNOTS ( 'NONE', 3,
 ( #39829, #24197, #48426, #81316, #16065, #48948, #59203, #67817, #92613, #91570 ),
 .UNSPECIFIED., .F., .F.,
 ( 4, 2, 2, 2, 4 ),
 ( 0.000000000000000000, 0.001118707926289530140, 0.002237415852579060279, 0.003356123778868591503, 0.004474831705158123160 ),
 .UNSPECIFIED. ) ;
#75372=CARTESIAN_POINT ( 'NONE',  ( -8.000000000000001776, -29.84375000409677270, 3.313708498984759387 ) ) ;
#75389=FILL_AREA_STYLE_COLOUR ( '', #33219 ) ;
#75481=CARTESIAN_POINT ( 'NONE',  ( 3.313708498984704320, -22.71874999999999645, -8.000000000000056843 ) ) ;
#75482=CARTESIAN_POINT ( 'NONE',  ( -8.000000000000000000, -29.84374999999999289, -3.313708498984762496 ) ) ;
#75506=CARTESIAN_POINT ( 'NONE',  ( -1.469576158976823947E-15, -28.06250000409677270, 8.000000000000000000 ) ) ;
#75574=CARTESIAN_POINT ( 'NONE',  ( 4.401442555609581635E-16, -19.15625000204838457, -7.188101187500000044 ) ) ;
#75590=EDGE_CURVE ( 'NONE', #97744, #66787, #21547, .T. ) ;
#75598=CARTESIAN_POINT ( 'NONE',  ( 9.246279647933182133, 15.99999999999999645, -3.826931552919425439 ) ) ;
#75613=CARTESIAN_POINT ( 'NONE',  ( 4.401442555609581635E-16, -19.15625000204838457, -7.188101187500000044 ) ) ;
#75629=EDGE_CURVE ( 'NONE', #54822, #13028, #64917, .T. ) ;
#75637=CARTESIAN_POINT ( 'NONE',  ( 7.188101187499999156, -32.75000000204839523, 2.977408999572654924 ) ) ;
#75643=ORIENTED_EDGE ( 'NONE', *, *, #57229, .T. ) ;
#75665=CARTESIAN_POINT ( 'NONE',  ( 4.898587196589412829E-16, -25.62499999999999645, -8.000000000000000000 ) ) ;
#75689=CARTESIAN_POINT ( 'NONE',  ( 2.977408999572652260, -25.81250000204838813, 7.188101187500000044 ) ) ;
#75697=CARTESIAN_POINT ( 'NONE',  ( -5.082755093536325042, -12.59375000204838280, -5.082755093536325930 ) ) ;
#75698=CARTESIAN_POINT ( 'NONE',  ( -8.000000000000000000, -17.93750000409676915, -9.797174393178825657E-16 ) ) ;
#75699=( BOUNDED_CURVE ( )  B_SPLINE_CURVE ( 2, ( #17849, #93322, #85223, #101932, #67979, #44785, #27028, #60967, #92233 ),
 .UNSPECIFIED., .F., .F. ) 
 B_SPLINE_CURVE_WITH_KNOTS ( ( 3, 2, 2, 2, 3 ),
 ( 0.3676470588235294379, 0.3750000000000000000, 0.3823529411764705621, 0.3897058823529412352, 0.3970588235294117974 ),
 .UNSPECIFIED. ) 
 CURVE ( )  GEOMETRIC_REPRESENTATION_ITEM ( )  RATIONAL_B_SPLINE_CURVE ( ( 1.000000000000000000, 0.9238795325112867385, 1.000000000000000000, 0.9238795325112867385, 1.000000000000000000, 0.9238795325112867385, 1.000000000000000000, 0.9238795325112861834, 1.000000000000000666 ) ) 
 REPRESENTATION_ITEM ( '' )  );
#75735=CARTESIAN_POINT ( 'NONE',  ( 7.150053860865849487, 83.21734546086022988, 3.590189269391289351 ) ) ;
#75755=CARTESIAN_POINT ( 'NONE',  ( 7.188101187500000044, -23.65625000204838457, 0.000000000000000000 ) ) ;
#75768=CARTESIAN_POINT ( 'NONE',  ( -3.313708498984765161, -23.65625000409676915, 7.999999999999998224 ) ) ;
#75772=CARTESIAN_POINT ( 'NONE',  ( 0.000000000000000000, -30.00000000000000000, 8.000000000000000000 ) ) ;
#75780=DIRECTION ( 'NONE',  ( 0.000000000000000000, 0.000000000000000000, 1.000000000000000000 ) ) ;
#75805=EDGE_CURVE ( 'NONE', #103615, #44667, #62177, .T. ) ;
#75834=DIRECTION ( 'NONE',  ( 0.000000000000000000, 0.000000000000000000, -1.000000000000000000 ) ) ;
#75886=ADVANCED_FACE ( 'NONE', ( #31904 ), #81467, .T. ) ;
#75904=DIRECTION ( 'NONE',  ( -0.000000000000000000, 1.000000000000000000, -0.000000000000000000 ) ) ;
#75928=CARTESIAN_POINT ( 'NONE',  ( -7.986711519608433285, 81.02638096376567489, -0.5300249774147574033 ) ) ;
#75933=ORIENTED_EDGE ( 'NONE', *, *, #7820, .T. ) ;
#75942=FACE_BOUND ( 'NONE', #56091, .T. ) ;
#75970=CARTESIAN_POINT ( 'NONE',  ( -8.000000000000001776, -13.15624999999999467, 3.313708498984759387 ) ) ;
#76011=CARTESIAN_POINT ( 'NONE',  ( -8.000000000000001776, -29.65625000000000000, 3.313708498984758943 ) ) ;
#76036=CARTESIAN_POINT ( 'NONE',  ( -9.948561005166130400, 88.86990273748200764, -1.045755304005127284 ) ) ;
#76037=CARTESIAN_POINT ( 'NONE',  ( -7.188101187500002709, -9.312500002048384573, 2.977408999572648707 ) ) ;
#76091=CARTESIAN_POINT ( 'NONE',  ( -1.469576158976823947E-15, -19.06250000409677270, 8.000000000000000000 ) ) ;
#76098=CARTESIAN_POINT ( 'NONE',  ( 2.977408999572650927, -19.25000000204838813, -7.188101187500001821 ) ) ;
#76116=CARTESIAN_POINT ( 'NONE',  ( -6.928203230275511437, 85.26526156932591505, 4.000000000000001776 ) ) ;
#76139=CARTESIAN_POINT ( 'NONE',  ( 5.082755093536324154, -21.21875000204838813, 5.082755093536326818 ) ) ;
#76165=CARTESIAN_POINT ( 'NONE',  ( 7.188101187499999156, -26.75000000204838457, 2.977408999572654924 ) ) ;
#76215=CARTESIAN_POINT ( 'NONE',  ( -2.977408999572650039, -25.06250000204838813, -7.188101187500000933 ) ) ;
#76226=CARTESIAN_POINT ( 'NONE',  ( 7.188101187500001821, -16.06250000204838457, -2.977408999572650483 ) ) ;
#76232=ADVANCED_FACE ( 'NONE', ( #10256 ), #60960, .T. ) ;
#76264=CARTESIAN_POINT ( 'NONE',  ( 6.943482370013978944, 84.47151629739275336, 3.973876482044366387 ) ) ;
#76284=CARTESIAN_POINT ( 'NONE',  ( 5.082755093536324154, -22.34375000204838457, 5.082755093536326818 ) ) ;
#76286=EDGE_CURVE ( 'NONE', #4323, #93999, #100268, .T. ) ;
#76294=CARTESIAN_POINT ( 'NONE',  ( -8.000000000000001776, -19.34375000409676915, 3.313708498984758943 ) ) ;
#76409=CARTESIAN_POINT ( 'NONE',  ( -5.656854249492379694, -20.93749999999999289, -5.656854249492380582 ) ) ;
#76449=CARTESIAN_POINT ( 'NONE',  ( -9.645512969475854348, 108.0110315067572770, -2.645801731561390646 ) ) ;
#76458=DIRECTION ( 'NONE',  ( 0.000000000000000000, 0.000000000000000000, 1.000000000000000000 ) ) ;
#76473=CARTESIAN_POINT ( 'NONE',  ( -3.313708498984779371, -28.53124999999999289, -7.999999999999981348 ) ) ;
#76534=VERTEX_POINT ( 'NONE', #64875 ) ;
#76538=CARTESIAN_POINT ( 'NONE',  ( 8.000000000000000000, -22.99999999999999289, 0.000000000000000000 ) ) ;
#76539=CARTESIAN_POINT ( 'NONE',  ( 4.898587196589412829E-16, -24.12499999999999289, -8.000000000000000000 ) ) ;
#76543=ORIENTED_EDGE ( 'NONE', *, *, #94713, .F. ) ;
#76547=ORIENTED_EDGE ( 'NONE', *, *, #35494, .T. ) ;
#76558=CARTESIAN_POINT ( 'NONE',  ( 7.744168461338428955, 108.4625406171515465, 2.019395720771551606 ) ) ;
#76602=EDGE_LOOP ( 'NONE', ( #51871, #73031, #39455, #103020 ) ) ;
#76620=CARTESIAN_POINT ( 'NONE',  ( -5.082755093536325042, -9.968750002048384573, -5.082755093536325930 ) ) ;
#76627=CARTESIAN_POINT ( 'NONE',  ( 2.977408999572651815, -12.31250000204838635, 7.188101187500000933 ) ) ;
#76648=DIRECTION ( 'NONE',  ( 1.000000000000000000, -0.000000000000000000, -0.000000000000000000 ) ) ;
#76654=CARTESIAN_POINT ( 'NONE',  ( -1.469576158976823947E-15, -18.87499999999999289, 8.000000000000000000 ) ) ;
#76669=CARTESIAN_POINT ( 'NONE',  ( -7.188101187500002709, -18.68750000204838102, 2.977408999572648707 ) ) ;
#76675=CARTESIAN_POINT ( 'NONE',  ( 0.000000000000000000, 15.00000000000000000, 0.000000000000000000 ) ) ;
#76682=CARTESIAN_POINT ( 'NONE',  ( 9.948688207305194098, 88.87023149490184437, -1.044946705213433358 ) ) ;
#76697=CARTESIAN_POINT ( 'NONE',  ( -7.188101187500002709, -22.81250000204838813, 2.977408999572648707 ) ) ;
#76731=AXIS2_PLACEMENT_3D ( 'NONE', #60234, #52101, #26289 ) ;
#76744=AXIS2_PLACEMENT_3D ( 'NONE', #35838, #94034, #103716 ) ;
#76748=CARTESIAN_POINT ( 'NONE',  ( -7.188101187500002709, -27.68750000204838457, 2.977408999572647819 ) ) ;
#76758=CARTESIAN_POINT ( 'NONE',  ( -5.082755093536325042, -11.09375000204838457, -5.082755093536325930 ) ) ;
#76760=AXIS2_PLACEMENT_3D ( 'NONE', #13136, #12605, #62783 ) ;
#76791=EDGE_LOOP ( 'NONE', ( #77791, #62430, #25047, #56997 ) ) ;
#76814=CARTESIAN_POINT ( 'NONE',  ( 7.188101187499999156, -26.75000000204838457, 2.977408999572654924 ) ) ;
#76825=CARTESIAN_POINT ( 'NONE',  ( -8.000000000000001776, -16.34375000409677270, 3.313708498984758943 ) ) ;
#76885=CARTESIAN_POINT ( 'NONE',  ( -1.320432766682874540E-15, -30.03125000204838813, 7.188101187500000044 ) ) ;
#76972=CARTESIAN_POINT ( 'NONE',  ( 0.000000000000000000, -30.00000000000000000, 0.000000000000000000 ) ) ;
#76981=( NAMED_UNIT ( * ) SI_UNIT ( $, .STERADIAN. ) SOLID_ANGLE_UNIT ( ) );
#76992=CARTESIAN_POINT ( 'NONE',  ( -9.165151389911679658, 105.0000000000000000, 4.000000000000001776 ) ) ;
#77035=STYLED_ITEM ( 'NONE', ( #69961 ), #7331 ) ;
#77049=EDGE_CURVE ( 'NONE', #49442, #99488, #27487, .T. ) ;
#77074=CARTESIAN_POINT ( 'NONE',  ( -9.090909090909093493, 16.00000000000000000, -4.165977904505304252 ) ) ;
#77080=DIRECTION ( 'NONE',  ( 0.000000000000000000, 0.000000000000000000, -1.000000000000000000 ) ) ;
#77082=CARTESIAN_POINT ( 'NONE',  ( -3.313708498984765161, -23.46875000000000000, 7.999999999999998224 ) ) ;
#77126=VECTOR ( 'NONE', #51799, 1000.000000000000000 ) ;
#77130=CARTESIAN_POINT ( 'NONE',  ( -10.00000000000000000, 15.00000000000000000, 10.00000000000000000 ) ) ;
#77155=CARTESIAN_POINT ( 'NONE',  ( -9.797936955406314041, 101.5332831022951865, -2.012343231877593563 ) ) ;
#77157=SURFACE_STYLE_FILL_AREA ( #62067 ) ;
#77168=CARTESIAN_POINT ( 'NONE',  ( 2.977408999572650927, -10.25000000204838813, -7.188101187500000933 ) ) ;
#77175=CARTESIAN_POINT ( 'NONE',  ( -7.188101187500001821, -17.37500000204838813, -2.977408999572651371 ) ) ;
#77215=CARTESIAN_POINT ( 'NONE',  ( -2.977408999572654480, -11.00000000204838635, 7.188101187499999156 ) ) ;
#77228=CARTESIAN_POINT ( 'NONE',  ( 4.898587196589412829E-16, -28.62499999999999289, -8.000000000000000000 ) ) ;
#77243=CARTESIAN_POINT ( 'NONE',  ( 5.082755093536324154, -25.34375000204838813, 5.082755093536326818 ) ) ;
#77258=ORIENTED_EDGE ( 'NONE', *, *, #1063, .F. ) ;
#77296=CARTESIAN_POINT ( 'NONE',  ( -5.082755093536326818, -23.09375000204838457, 5.082755093536325042 ) ) ;
#77303=CARTESIAN_POINT ( 'NONE',  ( -2.977408999572650039, -9.687500002048384573, -7.188101187500001821 ) ) ;
#77346=CARTESIAN_POINT ( 'NONE',  ( -7.188101187500002709, -29.18750000204839523, 2.977408999572648707 ) ) ;
#77350=CARTESIAN_POINT ( 'NONE',  ( -10.00000000000000355, 15.00000000000000000, -10.00000000000000000 ) ) ;
#77360=CARTESIAN_POINT ( 'NONE',  ( 5.082755093536325930, -17.46875000204838457, -5.082755093536325042 ) ) ;
#77369=CARTESIAN_POINT ( 'NONE',  ( 3.313708498984762496, -20.46875000409677270, 7.999999999999998224 ) ) ;
#77373=CARTESIAN_POINT ( 'NONE',  ( 9.334514330295428763, 31.78622737681786958, -3.588704711590615215 ) ) ;
#77376=CARTESIAN_POINT ( 'NONE',  ( 6.522118525112259313, -30.00000000000000355, -3.363504998894041975 ) ) ;
#77379=FACE_OUTER_BOUND ( 'NONE', #78472, .T. ) ;
#77384=EDGE_CURVE ( 'NONE', #72737, #76534, #243, .T. ) ;
#77405=VERTEX_POINT ( 'NONE', #770 ) ;
#77419=EDGE_LOOP ( 'NONE', ( #43336, #3521, #70452, #91689, #27018, #91660, #48490, #61189, #97381, #66137, #97954, #37154, #51301, #96709, #79532, #88898, #61112, #36001, #12159, #81427, #49265, #9921, #27768, #12342, #13430, #71211, #466, #57897, #20714, #37038, #57308, #28383 ) ) ;
#77421=DIRECTION ( 'NONE',  ( 0.000000000000000000, 0.000000000000000000, 1.000000000000000000 ) ) ;
#77431=CARTESIAN_POINT ( 'NONE',  ( 2.977408999572651815, -22.43750000204838813, 7.188101187500000933 ) ) ;
#77434=CARTESIAN_POINT ( 'NONE',  ( 1.544939622599074580, 15.00000000000000000, 9.999999999999998224 ) ) ;
#77504=CARTESIAN_POINT ( 'NONE',  ( 9.246271506234593929, 16.00000000000000000, 3.826949319562315655 ) ) ;
#77530=CARTESIAN_POINT ( 'NONE',  ( -9.918579450955565591, 108.7930391296868891, 1.297207292923863164 ) ) ;
#77552=ORIENTED_EDGE ( 'NONE', *, *, #67729, .T. ) ;
#77612=ORIENTED_EDGE ( 'NONE', *, *, #29073, .T. ) ;
#77622=CARTESIAN_POINT ( 'NONE',  ( 4.898587196589412829E-16, -21.12499999999999289, -8.000000000000000000 ) ) ;
#77679=CARTESIAN_POINT ( 'NONE',  ( -9.381593208289377372, 27.98561361880494047, -3.465401811657804476 ) ) ;
#77690=SURFACE_SIDE_STYLE ('',( #44801 ) ) ;
#77694=CARTESIAN_POINT ( 'NONE',  ( -9.165151389911679658, 105.0000000000000000, 4.000000000000001776 ) ) ;
#77710=CARTESIAN_POINT ( 'NONE',  ( 5.082755093536324154, -16.71875000204838813, 5.082755093536326818 ) ) ;
#77751=CARTESIAN_POINT ( 'NONE',  ( 7.188101187500001821, -13.43750000204838457, -2.977408999572650483 ) ) ;
#77760=CARTESIAN_POINT ( 'NONE',  ( 9.165151389911679658, 85.26710781282915264, -4.000000000000000000 ) ) ;
#77778=CARTESIAN_POINT ( 'NONE',  ( 2.977408999572650927, -24.87500000204838457, -7.188101187500001821 ) ) ;
#77791=ORIENTED_EDGE ( 'NONE', *, *, #31487, .F. ) ;
#77797=CARTESIAN_POINT ( 'NONE',  ( 9.176645556628256983, 104.4726096759327021, 3.973966573947712799 ) ) ;
#77829=CARTESIAN_POINT ( 'NONE',  ( -5.082755093536325042, -24.96875000204838813, -5.082755093536325930 ) ) ;
#77837=CARTESIAN_POINT ( 'NONE',  ( 2.977408999572650927, -31.25000000204838813, -7.188101187500001821 ) ) ;
#77841=CARTESIAN_POINT ( 'NONE',  ( -7.550180524134848525, 108.0055924721318519, 2.651855549982493176 ) ) ;
#77880=CARTESIAN_POINT ( 'NONE',  ( 4.401442555609581635E-16, -31.15625000204838813, -7.188101187500000044 ) ) ;
#77893=CARTESIAN_POINT ( 'NONE',  ( -7.188101187500002709, -16.81250000204838813, 2.977408999572647819 ) ) ;
#77899=CARTESIAN_POINT ( 'NONE',  ( -9.989113211954167681, 81.02700726451004698, 0.5334031035449062763 ) ) ;
#77903=CARTESIAN_POINT ( 'NONE',  ( 5.656854249492380582, -20.00000000409677270, -5.656854249492379694 ) ) ;
#77912=CARTESIAN_POINT ( 'NONE',  ( 5.154030868011758137, -30.00000000000000711, -5.413958715054342896 ) ) ;
#77930=ADVANCED_FACE ( 'NONE', ( #34692 ), #42743, .T. ) ;
#77933=VECTOR ( 'NONE', #104681, 1000.000000000000000 ) ;
#77960=CARTESIAN_POINT ( 'NONE',  ( -2.977408999572650039, -24.68750000204838457, -7.188101187500001821 ) ) ;
#77994=EDGE_LOOP ( 'NONE', ( #37242, #102511, #13890, #64449 ) ) ;
#78009=CARTESIAN_POINT ( 'NONE',  ( 3.313708498984724304, -11.46875000409677092, 8.000000000000039080 ) ) ;
#78034=EDGE_LOOP ( 'NONE', ( #32054, #66842, #77612 ) ) ;
#78040=EDGE_CURVE ( 'NONE', #59320, #42837, #41155, .T. ) ;
#78049=FILL_AREA_STYLE ('',( #78567 ) ) ;
#78067=CARTESIAN_POINT ( 'NONE',  ( 0.000000000000000000, 115.0000000000000000, 0.000000000000000000 ) ) ;
#78133=CARTESIAN_POINT ( 'NONE',  ( -10.00000000000000178, 15.11738935798242345, -0.3539438260497499433 ) ) ;
#78141=CARTESIAN_POINT ( 'NONE',  ( -5.656854249492379694, -20.93749999999999289, -5.656854249492380582 ) ) ;
#78182=VERTEX_POINT ( 'NONE', #44890 ) ;
#78188=DIRECTION ( 'NONE',  ( 1.000000000000000000, -0.000000000000000000, -0.000000000000000000 ) ) ;
#78192=CARTESIAN_POINT ( 'NONE',  ( -1.469576158976823947E-15, -28.06250000409677270, 8.000000000000000000 ) ) ;
#78214=CARTESIAN_POINT ( 'NONE',  ( -9.948181520647855436, 101.1310719723962137, 1.049088206181489014 ) ) ;
#78230=CARTESIAN_POINT ( 'NONE',  ( 4.401442555609581635E-16, -16.15625000204838457, -7.188101187500000044 ) ) ;
#78246=CARTESIAN_POINT ( 'NONE',  ( -7.896571385775229324, 88.78997999345754977, 1.305932416347436176 ) ) ;
#78254=CARTESIAN_POINT ( 'NONE',  ( -1.469576158976823947E-15, -26.56250000409677270, 8.000000000000000000 ) ) ;
#78262=CARTESIAN_POINT ( 'NONE',  ( 7.002990960197236880, 31.05266818383456240, 3.868040364119522678 ) ) ;
#78271=CARTESIAN_POINT ( 'NONE',  ( 7.188101187500001821, -10.43750000204838457, -2.977408999572650483 ) ) ;
#78278=CARTESIAN_POINT ( 'NONE',  ( 9.646083234704169840, 88.01290609023480727, -2.643797197754290451 ) ) ;
#78283=CARTESIAN_POINT ( 'NONE',  ( 6.928203230275510549, 30.00000000000000355, -4.000000000000000000 ) ) ;
#78292=CARTESIAN_POINT ( 'NONE',  ( 2.977408999572650927, -23.37500000204838813, -7.188101187500001821 ) ) ;
#78322=ADVANCED_FACE ( 'NONE', ( #54003, #56109 ), #21690, .F. ) ;
#78343=CARTESIAN_POINT ( 'NONE',  ( -5.082755093536326818, -21.59375000204838457, 5.082755093536325042 ) ) ;
#78352=CARTESIAN_POINT ( 'NONE',  ( 5.082755093536324154, -33.21875000204838813, 5.082755093536326818 ) ) ;
#78375=CARTESIAN_POINT ( 'NONE',  ( 9.999999999999996447, 15.00000000000000000, -10.00000000000000000 ) ) ;
#78380=LINE ( 'NONE', #63810, #34554 ) ;
#78397=CARTESIAN_POINT ( 'NONE',  ( -1.320432766682874540E-15, -30.40625000204838813, 7.188101187500000044 ) ) ;
#78400=( BOUNDED_CURVE ( )  B_SPLINE_CURVE ( 2, ( #82247, #40731, #16454, #73618, #106521, #235, #66072, #80651, #98949, #25109, #31613, #57970, #90891, #17006, #49882, #6232, #72046, #63974, #64496, #23527, #96862, #22990, #34809, #1308, #2393, #27258, #50932, #43925, #9404, #67677, #19172, #9956, #68201, #83316, #74680, #76814, #41794, #100561, #60144, #93553, #35339, #26721, #17541, #51478, #59593, #92467, #91943, #1852, #27795, #42320, #35878, #18616, #33727, #50402, #84393, #84923, #26197, #42862, #93008, #100027, #101101, #11009, #10482, #52006, #2925, #99485, #68758, #101638, #75755, #75214, #60666, #59056, #58524, #34269, #19702, #83848, #82788, #760, #8890, #43402, #66607, #25662, #76284, #91429, #67146, #18073, #5064, #11541, #29892, #95147, #21806, #54646, #28309, #85455, #28859, #79472, #86542, #61185, #37998, #70861, #94627, #13668, #20772, #36414, #46058, #71374, #21280, #4004, #63311, #69799, #95666, #94072, #4525, #69284, #45538, #102159, #87058, #20240, #78411, #30417, #96207, #62778, #52535, #78942, #13130, #44465, #87580, #3472, #46576, #5583, #103752, #104275, #38508, #102696, #77360, #12078, #62262, #53086, #54117, #86008, #45009, #77893, #61732, #36934, #53607, #12601, #37471, #70332, #103230, #29373, #32006, #79996, #40603, #81051, #30962, #6105, #22863, #73486, #56775, #15798, #72442, #90220, #89164, #39031, #64370, #88109, #106384, #24466, #97243, #16324, #7165, #97766, #64881, #71912, #48152, #55700, #23933, #56226, #14190, #32546, #49215, #81563, #65418, #23388, #7692, #89698, #105345, #48679, #105864, #47620, #63838, #15269, #98313, #96731, #88631, #57301, #47094, #104813, #82113, #8233, #40077, #41144, #33079, #74028, #14721, #107, #65944, #22336, #55183, #31490, #80522, #72957, #6640, #39567, #34680, #66472, #58929, #67552, #630, #91824, #67020, #99900, #26073, #27123, #91301 ),
 .UNSPECIFIED., .F., .F. ) 
 B_SPLINE_CURVE_WITH_KNOTS ( ( 3, 2, 2, 2, 2, 2, 2, 2, 2, 2, 2, 2, 2, 2, 2, 2, 2, 2, 2, 2, 2, 2, 2, 2, 2, 2, 2, 2, 2, 2, 2, 2, 2, 2, 2, 2, 2, 2, 2, 2, 2, 2, 2, 2, 2, 2, 2, 2, 2, 2, 2, 2, 2, 2, 2, 2, 2, 2, 2, 2, 2, 2, 2, 2, 2, 2, 2, 2, 2, 2, 2, 2, 2, 2, 2, 2, 2, 2, 2, 2, 2, 2, 2, 2, 2, 2, 2, 2, 2, 2, 2, 2, 2, 2, 2, 2, 2, 2, 2, 2, 2, 2, 2, 2, 2, 2, 2, 2, 2, 2, 2, 2, 3 ),
 ( 0.1630438152594470835, 0.1691176470588235392, 0.1764705882352941291, 0.1838235294117647189, 0.1911764705882352811, 0.1985294117647058709, 0.2058823529411764608, 0.2132352941176470507, 0.2205882352941176405, 0.2279411764705882304, 0.2352941176470588203, 0.2426470588235294101, 0.2500000000000000000, 0.2573529411764705621, 0.2647058823529411797, 0.2720588235294117418, 0.2794117647058823595, 0.2867647058823529216, 0.2941176470588235392, 0.3014705882352941013, 0.3088235294117647189, 0.3161764705882352811, 0.3235294117647058987, 0.3308823529411764608, 0.3382352941176470784, 0.3455882352941176405, 0.3529411764705882582, 0.3602941176470588203, 0.3676470588235294379, 0.3750000000000000000, 0.3823529411764705621, 0.3897058823529411242, 0.3970588235294117418, 0.4044117647058823595, 0.4117647058823529216, 0.4191176470588235947, 0.4264705882352941568, 0.4338235294117647189, 0.4411764705882352811, 0.4485294117647059542, 0.4558823529411765163, 0.4632352941176470784, 0.4705882352941176405, 0.4779411764705883137, 0.4852941176470588758, 0.4926470588235294379, 0.5000000000000000000, 0.5073529411764705621, 0.5147058823529411242, 0.5220588235294117974, 0.5294117647058823595, 0.5367647058823529216, 0.5441176470588234837, 0.5514705882352941568, 0.5588235294117647189, 0.5661764705882352811, 0.5735294117647058432, 0.5808823529411765163, 0.5882352941176470784, 0.5955882352941176405, 0.6029411764705882026, 0.6102941176470588758, 0.6176470588235294379, 0.6250000000000000000, 0.6323529411764705621, 0.6397058823529410132, 0.6470588235294117974, 0.6544117647058823595, 0.6617647058823528106, 0.6691176470588234837, 0.6764705882352941568, 0.6838235294117647189, 0.6911764705882352811, 0.6985294117647058432, 0.7058823529411765163, 0.7132352941176470784, 0.7205882352941176405, 0.7279411764705882026, 0.7352941176470588758, 0.7426470588235294379, 0.7500000000000000000, 0.7573529411764705621, 0.7647058823529411242, 0.7720588235294117974, 0.7794117647058823595, 0.7867647058823529216, 0.7941176470588234837, 0.8014705882352941568, 0.8088235294117647189, 0.8161764705882352811, 0.8235294117647058432, 0.8308823529411765163, 0.8382352941176470784, 0.8455882352941176405, 0.8529411764705880916, 0.8602941176470588758, 0.8676470588235294379, 0.8750000000000000000, 0.8823529411764704511, 0.8897058823529411242, 0.8970588235294117974, 0.9044117647058823595, 0.9117647058823528106, 0.9191176470588234837, 0.9264705882352941568, 0.9338235294117647189, 0.9411764705882351700, 0.9485294117647058432, 0.9558823529411765163, 0.9632352941176470784, 0.9705882352941175295, 0.9779411764705882026, 0.9804062415945057340 ),
 .UNSPECIFIED. ) 
 CURVE ( )  GEOMETRIC_REPRESENTATION_ITEM ( )  RATIONAL_B_SPLINE_CURVE ( ( 0.9781234062028207887, 0.9371213634217766542, 1.000000000000000000, 0.9238795325112867385, 1.000000000000000000, 0.9238795325112867385, 1.000000000000000000, 0.9238795325112867385, 1.000000000000000000, 0.9238795325112867385, 1.000000000000000000, 0.9238795325112867385, 1.000000000000000000, 0.9238795325112867385, 1.000000000000000000, 0.9238795325112867385, 1.000000000000000000, 0.9238795325112867385, 1.000000000000000000, 0.9238795325112867385, 1.000000000000000000, 0.9238795325112867385, 1.000000000000000000, 0.9238795325112867385, 1.000000000000000000, 0.9238795325112867385, 1.000000000000000000, 0.9238795325112867385, 1.000000000000000000, 0.9238795325112867385, 1.000000000000000000, 0.9238795325112867385, 1.000000000000000000, 0.9238795325112867385, 1.000000000000000000, 0.9238795325112867385, 1.000000000000000000, 0.9238795325112867385, 1.000000000000000000, 0.9238795325112867385, 1.000000000000000000, 0.9238795325112867385, 1.000000000000000000, 0.9238795325112867385, 1.000000000000000000, 0.9238795325112867385, 1.000000000000000000, 0.9238795325112867385, 1.000000000000000000, 0.9238795325112867385, 1.000000000000000000, 0.9238795325112867385, 1.000000000000000000, 0.9238795325112867385, 1.000000000000000000, 0.9238795325112867385, 1.000000000000000000, 0.9238795325112867385, 1.000000000000000000, 0.9238795325112867385, 1.000000000000000000, 0.9238795325112867385, 1.000000000000000000, 0.9238795325112867385, 1.000000000000000000, 0.9238795325112867385, 1.000000000000000000, 0.9238795325112867385, 1.000000000000000000, 0.9238795325112867385, 1.000000000000000000, 0.9238795325112867385, 1.000000000000000000, 0.9238795325112867385, 1.000000000000000000, 0.9238795325112867385, 1.000000000000000000, 0.9238795325112867385, 1.000000000000000000, 0.9238795325112867385, 1.000000000000000000, 0.9238795325112867385, 1.000000000000000000, 0.9238795325112867385, 1.000000000000000000, 0.9238795325112867385, 1.000000000000000000, 0.9238795325112867385, 1.000000000000000000, 0.9238795325112867385, 1.000000000000000000, 0.9238795325112867385, 1.000000000000000000, 0.9238795325112867385, 1.000000000000000000, 0.9238795325112867385, 1.000000000000000000, 0.9238795325112867385, 1.000000000000000000, 0.9238795325112867385, 1.000000000000000000, 0.9238795325112867385, 1.000000000000000000, 0.9238795325112867385, 1.000000000000000000, 0.9238795325112867385, 1.000000000000000000, 0.9238795325112867385, 1.000000000000000000, 0.9238795325112867385, 1.000000000000000000, 0.9238795325112867385, 1.000000000000000000, 0.9238795325112867385, 1.000000000000000000, 0.9238795325112867385, 1.000000000000000000, 0.9238795325112867385, 1.000000000000000000, 0.9238795325112867385, 1.000000000000000000, 0.9238795325112867385, 1.000000000000000000, 0.9238795325112867385, 1.000000000000000000, 0.9238795325112867385, 1.000000000000000000, 0.9238795325112867385, 1.000000000000000000, 0.9238795325112867385, 1.000000000000000000, 0.9238795325112867385, 1.000000000000000000, 0.9238795325112867385, 1.000000000000000000, 0.9238795325112867385, 1.000000000000000000, 0.9238795325112867385, 1.000000000000000000, 0.9238795325112867385, 1.000000000000000000, 0.9238795325112867385, 1.000000000000000000, 0.9238795325112867385, 1.000000000000000000, 0.9238795325112867385, 1.000000000000000000, 0.9238795325112867385, 1.000000000000000000, 0.9238795325112867385, 1.000000000000000000, 0.9238795325112867385, 1.000000000000000000, 0.9238795325112867385, 1.000000000000000000, 0.9238795325112867385, 1.000000000000000000, 0.9238795325112867385, 1.000000000000000000, 0.9238795325112867385, 1.000000000000000000, 0.9238795325112867385, 1.000000000000000000, 0.9238795325112867385, 1.000000000000000000, 0.9238795325112867385, 1.000000000000000000, 0.9238795325112867385, 1.000000000000000000, 0.9238795325112867385, 1.000000000000000000, 0.9238795325112867385, 1.000000000000000000, 0.9238795325112867385, 1.000000000000000000, 0.9238795325112867385, 1.000000000000000000, 0.9238795325112867385, 1.000000000000000000, 0.9238795325112867385, 1.000000000000000000, 0.9238795325112867385, 1.000000000000000000, 0.9238795325112867385, 1.000000000000000000, 0.9238795325112867385, 1.000000000000000000, 0.9238795325112867385, 1.000000000000000000, 0.9238795325112867385, 1.000000000000000000, 0.9238795325112867385, 1.000000000000000000, 0.9238795325112867385, 1.000000000000000000, 0.9238795325112867385, 1.000000000000000000, 0.9238795325112867385, 1.000000000000000000, 0.9238795325112867385, 1.000000000000000000, 0.9238795325112867385, 1.000000000000000000, 0.9238795325112867385, 1.000000000000000000, 0.9238795325112867385, 1.000000000000000000, 0.9238795325112867385, 1.000000000000000000, 0.9238795325112867385, 1.000000000000000000, 0.9238795325112867385, 1.000000000000000000, 0.9238795325112867385, 1.000000000000000000, 0.9238795325112867385, 1.000000000000000000, 0.9238795325112867385, 1.000000000000000000, 0.9238795325112867385, 1.000000000000000000, 0.9238795325112867385, 1.000000000000000000, 0.9744807002913096206, 0.9660720326926630630 ) ) 
 REPRESENTATION_ITEM ( '' )  );
#78404=( BOUNDED_CURVE ( )  B_SPLINE_CURVE ( 2, ( #24326, #1584, #9151, #82528, #49620, #83573, #15658, #9680, #81440 ),
 .UNSPECIFIED., .F., .F. ) 
 B_SPLINE_CURVE_WITH_KNOTS ( ( 3, 2, 2, 2, 3 ),
 ( 0.9558823529411764053, 0.9632352941176469674, 0.9705882352941176405, 0.9779411764705882026, 0.9804062224232821254 ),
 .UNSPECIFIED. ) 
 CURVE ( )  GEOMETRIC_REPRESENTATION_ITEM ( )  RATIONAL_B_SPLINE_CURVE ( ( 1.000000000000001110, 0.9238795325112856283, 1.000000000000000000, 0.9238795325112867385, 1.000000000000000000, 0.9238795325112867385, 1.000000000000000000, 0.9744808987591700999, 0.9660721634849256390 ) ) 
 REPRESENTATION_ITEM ( '' )  );
#78407=ORIENTED_EDGE ( 'NONE', *, *, #43638, .F. ) ;
#78411=CARTESIAN_POINT ( 'NONE',  ( 5.082755093536325930, -18.96875000204838457, -5.082755093536325042 ) ) ;
#78416=CARTESIAN_POINT ( 'NONE',  ( -9.797936955406314041, 81.53328310229518650, -2.012343231877590899 ) ) ;
#78418=CARTESIAN_POINT ( 'NONE',  ( 3.313708498984762496, -15.96875000409677270, 7.999999999999998224 ) ) ;
#78472=EDGE_LOOP ( 'NONE', ( #60353, #18478, #64284 ) ) ;
#78479=ORIENTED_EDGE ( 'NONE', *, *, #97861, .T. ) ;
#78482=CARTESIAN_POINT ( 'NONE',  ( 7.188101187500000044, -26.65625000204838813, 0.000000000000000000 ) ) ;
#78484=CARTESIAN_POINT ( 'NONE',  ( -3.594033448928638297, -9.156975712238446974, 6.225088131883843801 ) ) ;
#78494=ORIENTED_EDGE ( 'NONE', *, *, #63071, .F. ) ;
#78518=CARTESIAN_POINT ( 'NONE',  ( -8.000000000000000000, -16.53125000409677270, -3.313708498984762496 ) ) ;
#78526=CARTESIAN_POINT ( 'NONE',  ( -1.400734872026641709, 15.45478884909084272, -9.907647895771706459 ) ) ;
#78541=( BOUNDED_CURVE ( )  B_SPLINE_CURVE ( 2, ( #49015, #97566, #23730, #48489, #81384, #43079, #91635, #58740, #99711 ),
 .UNSPECIFIED., .F., .F. ) 
 B_SPLINE_CURVE_WITH_KNOTS ( ( 3, 2, 2, 2, 3 ),
 ( 0.2794117647058823040, 0.2867647058823528661, 0.2941176470588234837, 0.3014705882352940458, 0.3088235294117646634 ),
 .UNSPECIFIED. ) 
 CURVE ( )  GEOMETRIC_REPRESENTATION_ITEM ( )  RATIONAL_B_SPLINE_CURVE ( ( 1.000000000000000666, 0.9238795325112861834, 1.000000000000000000, 0.9238795325112867385, 1.000000000000000000, 0.9238795325112867385, 1.000000000000000000, 0.9238795325112872936, 0.9999999999999994449 ) ) 
 REPRESENTATION_ITEM ( '' )  );
#78567=FILL_AREA_STYLE_COLOUR ( '', #42534 ) ;
#78642=CARTESIAN_POINT ( 'NONE',  ( 7.999999999999998224, -24.78125000409677270, 3.313708498984766049 ) ) ;
#78656=CARTESIAN_POINT ( 'NONE',  ( -3.313708498984765161, -18.96875000000000000, 7.999999999999998224 ) ) ;
#78709=CARTESIAN_POINT ( 'NONE',  ( -9.918512371096300129, 26.20717007729448511, -1.297150762882706143 ) ) ;
#78727=CARTESIAN_POINT ( 'NONE',  ( -9.253800200985681457, 103.6998966891182761, -3.791983798715486298 ) ) ;
#78747=CARTESIAN_POINT ( 'NONE',  ( -2.977408999572654480, -17.00000000204838457, 7.188101187499999156 ) ) ;
#78757=CARTESIAN_POINT ( 'NONE',  ( 4.898587196589412829E-16, -24.12499999999999289, -8.000000000000000000 ) ) ;
#78760=ORIENTED_EDGE ( 'NONE', *, *, #12769, .T. ) ;
#78788=CARTESIAN_POINT ( 'NONE',  ( 5.656854249492378806, -21.68749999999999645, 5.656854249492381470 ) ) ;
#78791=CARTESIAN_POINT ( 'NONE',  ( 7.188101187499999156, -15.12500000204838457, 2.977408999572654924 ) ) ;
#78807=CARTESIAN_POINT ( 'NONE',  ( 7.999999999999998224, -29.09374999999999289, 3.313708498984766049 ) ) ;
#78819=CARTESIAN_POINT ( 'NONE',  ( 2.977408999572651815, -20.93750000204838457, 7.188101187500000933 ) ) ;
#78872=CARTESIAN_POINT ( 'NONE',  ( -7.188101187500000044, -17.28125000204838813, -8.802885111219163269E-16 ) ) ;
#78879=DIRECTION ( 'NONE',  ( -0.000000000000000000, 1.000000000000000000, -0.000000000000000000 ) ) ;
#78883=CARTESIAN_POINT ( 'NONE',  ( -2.977408999572650039, -31.06250000204838813, -7.188101187500001821 ) ) ;
#78888=CARTESIAN_POINT ( 'NONE',  ( -7.412906595240168706, 107.6418827285225603, 3.014362223629234006 ) ) ;
#78890=FACE_OUTER_BOUND ( 'NONE', #103531, .T. ) ;
#78896=VECTOR ( 'NONE', #68415, 1000.000000000000000 ) ;
#78924=CYLINDRICAL_SURFACE ( 'NONE', #41920, 8.000000000000000000 ) ;
#78927=CARTESIAN_POINT ( 'NONE',  ( -7.188101187500002709, -32.18750000204838813, 2.977408999572648707 ) ) ;
#78932=ORIENTED_EDGE ( 'NONE', *, *, #90578, .F. ) ;
#78942=CARTESIAN_POINT ( 'NONE',  ( -7.188101187500000933, -18.50000000204838457, -2.977408999572651371 ) ) ;
#78952=CARTESIAN_POINT ( 'NONE',  ( 8.000000000000000000, -9.593750004096769146, -3.313708498984761608 ) ) ;
#79004=VECTOR ( 'NONE', #94096, 1000.000000000000000 ) ;
#79020=CARTESIAN_POINT ( 'NONE',  ( -2.977408999572654480, -22.62500000204838813, 7.188101187499999156 ) ) ;
#79033=CARTESIAN_POINT ( 'NONE',  ( -10.00000000000000355, 105.0000000000000000, 0.000000000000000000 ) ) ;
#79080=VERTEX_POINT ( 'NONE', #55850 ) ;
#79085=CARTESIAN_POINT ( 'NONE',  ( 8.000000000000000000, -27.68750000409677270, 0.000000000000000000 ) ) ;
#79088=MECHANICAL_DESIGN_GEOMETRIC_PRESENTATION_REPRESENTATION('',(#5036),#39454);
#79107=CARTESIAN_POINT ( 'NONE',  ( -10.00000000000000000, 15.00000000000000000, 1.544939622598903828 ) ) ;
#79109=DIRECTION ( 'NONE',  ( 0.000000000000000000, 0.000000000000000000, -1.000000000000000000 ) ) ;
#79119=EDGE_CURVE ( 'NONE', #7939, #94793, #95247, .T. ) ;
#79153=DIRECTION ( 'NONE',  ( 0.000000000000000000, -1.000000000000000000, 0.000000000000000000 ) ) ;
#79166=( BOUNDED_CURVE ( )  B_SPLINE_CURVE ( 2, ( #54728, #40152, #96811, #73029, #64961, #56855, #7774, #89775, #81647 ),
 .UNSPECIFIED., .F., .F. ) 
 B_SPLINE_CURVE_WITH_KNOTS ( ( 3, 2, 2, 2, 3 ),
 ( 0.7794117647058823595, 0.7867647058823529216, 0.7941176470588234837, 0.8014705882352941568, 0.8088235294117647189 ),
 .UNSPECIFIED. ) 
 CURVE ( )  GEOMETRIC_REPRESENTATION_ITEM ( )  RATIONAL_B_SPLINE_CURVE ( ( 1.000000000000000000, 0.9238795325112867385, 1.000000000000000000, 0.9238795325112867385, 1.000000000000000000, 0.9238795325112867385, 1.000000000000000000, 0.9238795325112867385, 1.000000000000000000 ) ) 
 REPRESENTATION_ITEM ( '' )  );
#79175=DIRECTION ( 'NONE',  ( 0.000000000000000000, 0.000000000000000000, -1.000000000000000000 ) ) ;
#79206=CARTESIAN_POINT ( 'NONE',  ( -8.000000000000001776, -13.15624999999999467, 3.313708498984758943 ) ) ;
#79213=FACE_OUTER_BOUND ( 'NONE', #7269, .T. ) ;
#79251=CARTESIAN_POINT ( 'NONE',  ( 3.313708498984771378, -27.96875000409677270, 7.999999999999988454 ) ) ;
#79253=CARTESIAN_POINT ( 'NONE',  ( -9.646032546913145822, 26.98719671525633501, 2.644051433538242790 ) ) ;
#79312=CARTESIAN_POINT ( 'NONE',  ( 5.656854249492378806, -17.37500000409676915, 5.656854249492381470 ) ) ;
#79322=CARTESIAN_POINT ( 'NONE',  ( 7.986468734911285949, 33.97313679723078650, 0.5341897780976184729 ) ) ;
#79330=CARTESIAN_POINT ( 'NONE',  ( 7.188101187500001821, -14.93750000204838457, -2.977408999572650483 ) ) ;
#79356=CARTESIAN_POINT ( 'NONE',  ( -1.320432766682874540E-15, -19.53125000204838457, 7.188101187500000044 ) ) ;
#79408=CARTESIAN_POINT ( 'NONE',  ( 5.082755093536324154, -16.71875000204838813, 5.082755093536326818 ) ) ;
#79418=CARTESIAN_POINT ( 'NONE',  ( -5.082755093536325042, -30.96875000204838813, -5.082755093536325930 ) ) ;
#79425=ORIENTED_EDGE ( 'NONE', *, *, #10358, .F. ) ;
#79457=CARTESIAN_POINT ( 'NONE',  ( -7.188101187500000044, -33.78125000204838813, -8.802885111219163269E-16 ) ) ;
#79472=CARTESIAN_POINT ( 'NONE',  ( -2.977408999572654480, -21.12500000204838813, 7.188101187499999156 ) ) ;
#79486=CARTESIAN_POINT ( 'NONE',  ( 8.000000000000000000, -11.18750000409677092, 0.000000000000000000 ) ) ;
#79491=( NAMED_UNIT ( * ) PLANE_ANGLE_UNIT ( ) SI_UNIT ( $, .RADIAN. ) );
#79496=CARTESIAN_POINT ( 'NONE',  ( -3.572352985695287586, 15.21714514899109894, 9.341953373613243627 ) ) ;
#79532=ORIENTED_EDGE ( 'NONE', *, *, #71304, .F. ) ;
#79546=CARTESIAN_POINT ( 'NONE',  ( -5.082755093536326818, -22.71875000204838457, 5.082755093536325042 ) ) ;
#79547=CARTESIAN_POINT ( 'NONE',  ( 8.000000000000000000, -20.09375000409677270, -3.313708498984761164 ) ) ;
#79608=CARTESIAN_POINT ( 'NONE',  ( -1.469576158976823947E-15, -28.06250000409677270, 8.000000000000000000 ) ) ;
#79615=( NAMED_UNIT ( * ) SI_UNIT ( $, .STERADIAN. ) SOLID_ANGLE_UNIT ( ) );
#79629=CARTESIAN_POINT ( 'NONE',  ( -9.403185743875129177, 15.24615751665902685, 3.409011323176729835 ) ) ;
#79647=CARTESIAN_POINT ( 'NONE',  ( -1.469576158976823947E-15, -14.56250000409677092, 8.000000000000000000 ) ) ;
#79670=CARTESIAN_POINT ( 'NONE',  ( 8.000000000000000000, -12.59375000409676915, -3.313708498984761164 ) ) ;
#79711=CARTESIAN_POINT ( 'NONE',  ( 9.165151389911683211, 105.2629551091633857, 4.000000000000002665 ) ) ;
#79736=CARTESIAN_POINT ( 'NONE',  ( 4.898587196589412829E-16, -15.12499999999999289, -8.000000000000000000 ) ) ;
#79756=CARTESIAN_POINT ( 'NONE',  ( 9.999999999999998224, 15.00000000000000000, -1.544939622599252438 ) ) ;
#79816=CARTESIAN_POINT ( 'NONE',  ( -7.188101187500002709, -11.18750000204838457, 2.977408999572648707 ) ) ;
#79836=CARTESIAN_POINT ( 'NONE',  ( 8.000000000000000000, -26.18750000409677270, 0.000000000000000000 ) ) ;
#79848=CARTESIAN_POINT ( 'NONE',  ( 7.413471587080155523, 32.64352159168327461, -3.013058070223547880 ) ) ;
#79853=CARTESIAN_POINT ( 'NONE',  ( 9.999999999999998224, 15.00000000000000000, -4.582575694955843382 ) ) ;
#79855=CARTESIAN_POINT ( 'NONE',  ( -7.188101187500000044, -9.781250002048384573, -8.802885111219163269E-16 ) ) ;
#79858=ORIENTED_EDGE ( 'NONE', *, *, #31916, .T. ) ;
#79880=CARTESIAN_POINT ( 'NONE',  ( -5.082755093536326818, -21.21875000204838457, 5.082755093536325042 ) ) ;
#79898=CARTESIAN_POINT ( 'NONE',  ( 9.797174393178825657E-16, 15.00000000000000000, 8.000000000000000000 ) ) ;
#79929=CARTESIAN_POINT ( 'NONE',  ( 7.188101187500000933, -19.43750000204838457, -2.977408999572650483 ) ) ;
#79935=CARTESIAN_POINT ( 'NONE',  ( -5.082755093536325042, -29.46875000204838813, -5.082755093536325930 ) ) ;
#79938=CARTESIAN_POINT ( 'NONE',  ( -7.188101187500001821, -27.87500000204838457, -2.977408999572651371 ) ) ;
#79979=CARTESIAN_POINT ( 'NONE',  ( -7.188101187500002709, -23.18750000204838813, 2.977408999572648707 ) ) ;
#79987=CYLINDRICAL_SURFACE ( 'NONE', #61592, 8.000000000000000000 ) ;
#79996=CARTESIAN_POINT ( 'NONE',  ( 2.977408999572650927, -15.87500000204838635, -7.188101187500000933 ) ) ;
#80004=CARTESIAN_POINT ( 'NONE',  ( -9.918512371096301905, 81.20717007729450643, -1.297150762882695263 ) ) ;
#80007=CARTESIAN_POINT ( 'NONE',  ( -8.000000000000000000, -8.937500004096769146, -9.797174393178825657E-16 ) ) ;
#80034=ORIENTED_EDGE ( 'NONE', *, *, #3327, .T. ) ;
#80049=CARTESIAN_POINT ( 'NONE',  ( 9.999999999999996447, 0.000000000000000000, -10.00000000000000000 ) ) ;
#80069=CARTESIAN_POINT ( 'NONE',  ( 7.188101187500000044, -20.65625000204838813, 0.000000000000000000 ) ) ;
#80072=CARTESIAN_POINT ( 'NONE',  ( -8.000000000000000000, -23.84374999999999645, -3.313708498984762496 ) ) ;
#80109=CARTESIAN_POINT ( 'NONE',  ( -3.313708498984765161, -16.15625000409677270, 7.999999999999998224 ) ) ;
#80133=CARTESIAN_POINT ( 'NONE',  ( 3.313708498984762496, -30.96875000409677980, 7.999999999999998224 ) ) ;
#80147=CARTESIAN_POINT ( 'NONE',  ( -4.912112805545315375, -10.03270266009703526, 6.401595693439444901 ) ) ;
#80239=( GEOMETRIC_REPRESENTATION_CONTEXT ( 3 ) GLOBAL_UNCERTAINTY_ASSIGNED_CONTEXT ( ( #2750 ) ) GLOBAL_UNIT_ASSIGNED_CONTEXT ( ( #102451, #86817, #52831 ) ) REPRESENTATION_CONTEXT ( 'NONE', 'WORKASPACE' ) );
#80251=CARTESIAN_POINT ( 'NONE',  ( -5.656854249492381470, -16.06249999999999289, 5.656854249492379694 ) ) ;
#80277=CARTESIAN_POINT ( 'NONE',  ( 9.926810856659445292, 15.46725112412266512, -1.404490565848973027 ) ) ;
#80299=CARTESIAN_POINT ( 'NONE',  ( -9.701736001019305888, 15.75130202679985914, 2.450449656239128693 ) ) ;
#80305=AXIS2_PLACEMENT_3D ( 'NONE', #63248, #78879, #88574 ) ;
#80373=CARTESIAN_POINT ( 'NONE',  ( -7.934996450857311423, 26.13137543527469830, -1.050865690281772569 ) ) ;
#80381=CARTESIAN_POINT ( 'NONE',  ( 2.977408999572650927, -10.25000000204838813, -7.188101187500001821 ) ) ;
#80384=EDGE_CURVE ( 'NONE', #30765, #7449, #16142, .T. ) ;
#80403=CARTESIAN_POINT ( 'NONE',  ( -7.188101187500002709, -21.31250000204838813, 2.977408999572648707 ) ) ;
#80453=ORIENTED_EDGE ( 'NONE', *, *, #46857, .T. ) ;
#80455=CARTESIAN_POINT ( 'NONE',  ( 2.977408999572650927, -17.75000000204838457, -7.188101187500000933 ) ) ;
#80465=CARTESIAN_POINT ( 'NONE',  ( 7.188101187500000044, -25.53125000204838813, 0.000000000000000000 ) ) ;
#80479=AXIS2_PLACEMENT_3D ( 'NONE', #68285, #94153, #75834 ) ;
#80485=LINE ( 'NONE', #78375, #32787 ) ;
#80499=CARTESIAN_POINT ( 'NONE',  ( 4.582575694955843382, 15.00000000000000000, -10.00000000000000000 ) ) ;
#80505=CARTESIAN_POINT ( 'NONE',  ( 5.082755093536324154, -22.71875000204838457, 5.082755093536326818 ) ) ;
#80522=CARTESIAN_POINT ( 'NONE',  ( 5.082755093536324154, -10.34375000204838457, 5.082755093536326818 ) ) ;
#80523=CARTESIAN_POINT ( 'NONE',  ( 6.928203230275509661, 29.73069070304461192, -4.000000000000000000 ) ) ;
#80534=CARTESIAN_POINT ( 'NONE',  ( -5.656854249492381470, -13.25000000409676915, 5.656854249492379694 ) ) ;
#80536=CARTESIAN_POINT ( 'NONE',  ( 9.999999999999998224, 15.00000000000000000, -1.734723475976806306E-15 ) ) ;
#80539=CARTESIAN_POINT ( 'NONE',  ( -9.176645556628256983, 85.52739032406731212, 3.973966573947710135 ) ) ;
#80540=CARTESIAN_POINT ( 'NONE',  ( 5.656854249492378806, -20.18749999999999289, 5.656854249492381470 ) ) ;
#80543=VERTEX_POINT ( 'NONE', #61296 ) ;
#80545=CARTESIAN_POINT ( 'NONE',  ( -3.997425403567957503, 15.99999999372935022, 9.168149550321043506 ) ) ;
#80550=CARTESIAN_POINT ( 'NONE',  ( 8.000000000000000000, -9.593750004096769146, -3.313708498984761164 ) ) ;
#80591=EDGE_LOOP ( 'NONE', ( #35325, #78932, #13083 ) ) ;
#80594=DIRECTION ( 'NONE',  ( 1.000000000000000000, -0.000000000000000000, -0.000000000000000000 ) ) ;
#80596=CARTESIAN_POINT ( 'NONE',  ( 7.188101187500001821, -20.56250000204838457, -2.977408999572650483 ) ) ;
#80598=CARTESIAN_POINT ( 'NONE',  ( 9.699016383038308931, 81.82361828551655947, 2.444973590251036999 ) ) ;
#80627=VECTOR ( 'NONE', #54676, 1000.000000000000000 ) ;
#80629=CARTESIAN_POINT ( 'NONE',  ( -10.00000000000000355, 30.00000000000000000, 0.000000000000000000 ) ) ;
#80632=FACE_OUTER_BOUND ( 'NONE', #92396, .T. ) ;
#80651=CARTESIAN_POINT ( 'NONE',  ( 2.977408999572650927, -29.37500000204838457, -7.188101187500000933 ) ) ;
#80660=CARTESIAN_POINT ( 'NONE',  ( 3.313708498984762496, -32.46875000409677625, 7.999999999999998224 ) ) ;
#80666=CARTESIAN_POINT ( 'NONE',  ( 9.999952458099484076, 33.99988114523864624, 0.2653554233229051817 ) ) ;
#80739=VECTOR ( 'NONE', #34546, 1000.000000000000000 ) ;
#80790=CARTESIAN_POINT ( 'NONE',  ( 3.313708498984762052, -16.71874999999999289, -8.000000000000000000 ) ) ;
#80815=CARTESIAN_POINT ( 'NONE',  ( 9.571198553003402054, 15.30040232763730756, -2.918503601030738359 ) ) ;
#80838=DIRECTION ( 'NONE',  ( -0.000000000000000000, 1.000000000000000000, -0.000000000000000000 ) ) ;
#80840=ADVANCED_FACE ( 'NONE', ( #80632 ), #81163, .T. ) ;
#80917=CARTESIAN_POINT ( 'NONE',  ( 5.656854249492380582, -34.81249999999999289, -5.656854249492379694 ) ) ;
#80934=ORIENTED_EDGE ( 'NONE', *, *, #55419, .T. ) ;
#80941=CARTESIAN_POINT ( 'NONE',  ( -7.188101187500000044, -10.90625000204838457, -8.802885111219163269E-16 ) ) ;
#80986=CARTESIAN_POINT ( 'NONE',  ( 4.401442555609581635E-16, -13.15625000204838280, -7.188101187500000044 ) ) ;
#80991=CARTESIAN_POINT ( 'NONE',  ( -2.977408999572650039, -29.56250000204838813, -7.188101187500000933 ) ) ;
#80994=CARTESIAN_POINT ( 'NONE',  ( 7.188101187500000044, -28.53125000204838813, 0.000000000000000000 ) ) ;
#81002=CARTESIAN_POINT ( 'NONE',  ( -7.150053860865850375, 106.7826545391397843, 3.590189269391291571 ) ) ;
#81035=CARTESIAN_POINT ( 'NONE',  ( 9.220915120640583496, 28.95545113567915507, -3.870126578504840431 ) ) ;
#81036=CARTESIAN_POINT ( 'NONE',  ( -5.082755093536326818, -24.59375000204838813, 5.082755093536325042 ) ) ;
#81045=ORIENTED_EDGE ( 'NONE', *, *, #52011, .T. ) ;
#81051=CARTESIAN_POINT ( 'NONE',  ( -2.977408999572650039, -15.68750000204838635, -7.188101187500000933 ) ) ;
#81052=CARTESIAN_POINT ( 'NONE',  ( 7.934883677559678716, 26.13160822062449995, 1.051380792122691421 ) ) ;
#81057=ADVANCED_FACE ( 'NONE', ( #41126 ), #39550, .T. ) ;
#81061=FACE_OUTER_BOUND ( 'NONE', #19029, .T. ) ;
#81066=CARTESIAN_POINT ( 'NONE',  ( 5.656854249492378806, -14.37500000409677092, 5.656854249492381470 ) ) ;
#81071=CARTESIAN_POINT ( 'NONE',  ( -3.594033448928638741, -9.156975712238445197, 6.225088131883843801 ) ) ;
#81078=CARTESIAN_POINT ( 'NONE',  ( -3.884543032214208491, 15.13241195026071928, 9.216463528758552570 ) ) ;
#81115=EDGE_CURVE ( 'NONE', #49442, #3603, #24451, .T. ) ;
#81119=EDGE_LOOP ( 'NONE', ( #67347, #48284, #39980, #87485 ) ) ;
#81128=CARTESIAN_POINT ( 'NONE',  ( -2.977408999572650039, -21.68750000204838813, -7.188101187500001821 ) ) ;
#81152=VECTOR ( 'NONE', #74010, 1000.000000000000000 ) ;
#81163=CYLINDRICAL_SURFACE ( 'NONE', #32834, 8.000000000000000000 ) ;
#81173=VERTEX_POINT ( 'NONE', #105846 ) ;
#81188=CARTESIAN_POINT ( 'NONE',  ( -5.656854249492379694, -30.12500000409677270, -5.656854249492380582 ) ) ;
#81193=CARTESIAN_POINT ( 'NONE',  ( 9.381394091586571449, 32.01349605581611257, 3.465950112474259992 ) ) ;
#81197=CARTESIAN_POINT ( 'NONE',  ( -3.313708498984760276, -10.53124999999999289, -8.000000000000000000 ) ) ;
#81233=CARTESIAN_POINT ( 'NONE',  ( -1.217592056924591271, -29.99999999999998934, 7.214394986259497600 ) ) ;
#81253=DIRECTION ( 'NONE',  ( -0.000000000000000000, 1.000000000000000000, -0.000000000000000000 ) ) ;
#81277=CARTESIAN_POINT ( 'NONE',  ( 7.896165657598944065, 101.2108886862802564, -1.307894402814545387 ) ) ;
#81308=CARTESIAN_POINT ( 'NONE',  ( -3.313708498984760720, -15.03124999999999289, -8.000000000000000000 ) ) ;
#81316=CARTESIAN_POINT ( 'NONE',  ( 2.797297131808757609, 15.83452282593334282, -9.607612890400021755 ) ) ;
#81335=CARTESIAN_POINT ( 'NONE',  ( 9.999999999999998224, 15.00000000000000000, -2.701558353794592193 ) ) ;
#81364=STYLED_ITEM ( 'NONE', ( #50564 ), #51906 ) ;
#81372=CARTESIAN_POINT ( 'NONE',  ( -9.240220675753752388, 15.98931925350938243, -3.827754797005808562 ) ) ;
#81384=CARTESIAN_POINT ( 'NONE',  ( 8.000000000000000000, -27.49999999999999645, 0.000000000000000000 ) ) ;
#81392=CARTESIAN_POINT ( 'NONE',  ( 4.401442555609581635E-16, -11.65625000204838635, -7.188101187500000044 ) ) ;
#81427=ORIENTED_EDGE ( 'NONE', *, *, #75805, .F. ) ;
#81433=CARTESIAN_POINT ( 'NONE',  ( -8.000000000000001776, -31.15625000000000355, 3.313708498984758943 ) ) ;
#81440=CARTESIAN_POINT ( 'NONE',  ( -3.999995229665001428, -8.688226215992830959, 6.928205984420947594 ) ) ;
#81456=CARTESIAN_POINT ( 'NONE',  ( 7.188101187500000044, -16.15625000204838457, 0.000000000000000000 ) ) ;
#81467=PLANE ( 'NONE',  #44471 ) ;
#81483=VERTEX_POINT ( 'NONE', #79853 ) ;
#81501=CARTESIAN_POINT ( 'NONE',  ( 5.082755093536324154, -13.71875000204838457, 5.082755093536326818 ) ) ;
#81507=CARTESIAN_POINT ( 'NONE',  ( -1.469576158976823947E-15, -24.87499999999999289, 8.000000000000000000 ) ) ;
#81509=CARTESIAN_POINT ( 'NONE',  ( 7.188101187500001821, -25.43750000204838813, -2.977408999572650483 ) ) ;
#81524=CARTESIAN_POINT ( 'NONE',  ( -7.801339272325196639, 88.58731471959703185, -1.788609912539676161 ) ) ;
#81526=EDGE_LOOP ( 'NONE', ( #27165, #25096, #66177, #14766 ) ) ;
#81551=CARTESIAN_POINT ( 'NONE',  ( 7.188101187500000044, -24.03125000204838457, 0.000000000000000000 ) ) ;
#81554=ORIENTED_EDGE ( 'NONE', *, *, #89191, .F. ) ;
#81563=CARTESIAN_POINT ( 'NONE',  ( 7.188101187500000933, -13.06250000204838280, -2.977408999572650483 ) ) ;
#81564=CARTESIAN_POINT ( 'NONE',  ( 7.211357414135268762, 27.98853460065558707, 3.467230644691330355 ) ) ;
#81574=CARTESIAN_POINT ( 'NONE',  ( -1.469576158976823947E-15, -18.87499999999999289, 8.000000000000000000 ) ) ;
#81576=CARTESIAN_POINT ( 'NONE',  ( 0.000000000000000000, -30.00000000000000000, 0.000000000000000000 ) ) ;
#81578=CARTESIAN_POINT ( 'NONE',  ( -2.977408999572650039, -29.18750000204839523, -7.188101187500001821 ) ) ;
#81583=CARTESIAN_POINT ( 'NONE',  ( -5.656854249492381470, -16.06249999999999289, 5.656854249492379694 ) ) ;
#81587=CARTESIAN_POINT ( 'NONE',  ( -9.536842176398147686, 32.64235369883989790, 3.014135744008175966 ) ) ;
#81621=EDGE_LOOP ( 'NONE', ( #59658, #41732, #42839, #21217, #64916, #92615, #54749, #80453, #70669, #58347, #86600, #50793, #92436, #14416, #77552, #70910, #66717, #24656, #56025, #14295, #21141, #82747, #65515, #15382, #13734, #43571, #96140, #94947, #29498, #89239 ) ) ;
#81632=CARTESIAN_POINT ( 'NONE',  ( 7.551560007654696705, 88.00910351806992082, -2.648022159607839487 ) ) ;
#81642=CARTESIAN_POINT ( 'NONE',  ( -1.320432766682874540E-15, -18.03125000204838457, 7.188101187500000044 ) ) ;
#81647=CARTESIAN_POINT ( 'NONE',  ( -1.469576158976823947E-15, -13.06250000409676915, 8.000000000000000000 ) ) ;
#81708=CARTESIAN_POINT ( 'NONE',  ( 8.000000000000000000, -24.68750000409677270, 0.000000000000000000 ) ) ;
#81710=DIRECTION ( 'NONE',  ( -0.000000000000000000, 1.000000000000000000, -0.000000000000000000 ) ) ;
#81717=EDGE_CURVE ( 'NONE', #80543, #72025, #46675, .T. ) ;
#81739=CARTESIAN_POINT ( 'NONE',  ( 7.999999999999998224, -12.59374999999999467, 3.313708498984766049 ) ) ;
#81748=CARTESIAN_POINT ( 'NONE',  ( -7.212408192734266699, 32.01517089320368825, -3.465038817813884453 ) ) ;
#81757=CARTESIAN_POINT ( 'NONE',  ( -7.719366823438956970, -29.99999999999998579, 1.311865339813678588 ) ) ;
#81765=CARTESIAN_POINT ( 'NONE',  ( -8.000000000000000000, -22.24999999999999289, -9.797174393178825657E-16 ) ) ;
#81773=CARTESIAN_POINT ( 'NONE',  ( -10.00000000000000355, 15.00000000000000000, -10.00000000000000000 ) ) ;
#81787=FILL_AREA_STYLE ('',( #40815 ) ) ;
#81801=CARTESIAN_POINT ( 'NONE',  ( 7.986539162393897939, 101.0267282894254635, -0.5321833565149908241 ) ) ;
#81812=CARTESIAN_POINT ( 'NONE',  ( 9.482993638194542996, 107.4434872025367724, -3.177441187500465780 ) ) ;
#81823=LINE ( 'NONE', #7946, #61438 ) ;
#81835=CARTESIAN_POINT ( 'NONE',  ( -3.313708498984760720, -12.03124999999999289, -8.000000000000000000 ) ) ;
#81869=( LENGTH_UNIT ( ) NAMED_UNIT ( * ) SI_UNIT ( .MILLI., .METRE. ) );
#81878=CARTESIAN_POINT ( 'NONE',  ( -10.00000000000000355, 15.00000000000000000, -10.00000000000000000 ) ) ;
#81882=CARTESIAN_POINT ( 'NONE',  ( -8.000000000000000000, -29.84374999999999645, -3.313708498984762496 ) ) ;
#81908=CARTESIAN_POINT ( 'NONE',  ( -2.977408999572654480, -33.12500000204838813, 7.188101187499999156 ) ) ;
#81927=STYLED_ITEM ( 'NONE', ( #86292 ), #99717 ) ;
#81947=DIRECTION ( 'NONE',  ( 1.000000000000000000, -0.000000000000000000, -0.000000000000000000 ) ) ;
#81965=CARTESIAN_POINT ( 'NONE',  ( -5.656854249492379694, -31.43749999999999289, -5.656854249492380582 ) ) ;
#81966=CIRCLE ( 'NONE', #45801, 11.00000000000000000 ) ;
#81984=( BOUNDED_CURVE ( )  B_SPLINE_CURVE ( 2, ( #91621, #76473, #43065, #27452, #60332, #41986, #66805, #17730, #956 ),
 .UNSPECIFIED., .F., .F. ) 
 B_SPLINE_CURVE_WITH_KNOTS ( ( 3, 2, 2, 2, 3 ),
 ( 0.2500000000000000555, 0.2573529411764705621, 0.2647058823529411797, 0.2720588235294116863, 0.2794117647058823040 ),
 .UNSPECIFIED. ) 
 CURVE ( )  GEOMETRIC_REPRESENTATION_ITEM ( )  RATIONAL_B_SPLINE_CURVE ( ( 0.9999999999999994449, 0.9238795325112872936, 1.000000000000000000, 0.9238795325112867385, 1.000000000000000000, 0.9238795325112867385, 1.000000000000000000, 0.9238795325112872936, 0.9999999999999994449 ) ) 
 REPRESENTATION_ITEM ( '' )  );
#81993=CARTESIAN_POINT ( 'NONE',  ( 7.188101187500000044, -13.15625000204838280, 0.000000000000000000 ) ) ;
#82048=CARTESIAN_POINT ( 'NONE',  ( 4.401442555609581635E-16, -11.65625000204838635, -7.188101187500000044 ) ) ;
#82059=CARTESIAN_POINT ( 'NONE',  ( -1.320432766682874540E-15, -27.40625000204838813, 7.188101187500000044 ) ) ;
#82067=CARTESIAN_POINT ( 'NONE',  ( -7.045965687440312486, 106.3039246378603480, 3.790395326974321133 ) ) ;
#82099=CARTESIAN_POINT ( 'NONE',  ( 9.645512969475850795, 26.98896849324273717, -2.645801731561390646 ) ) ;
#82100=CARTESIAN_POINT ( 'NONE',  ( 4.401442555609581635E-16, -28.15625000204838813, -7.188101187500000044 ) ) ;
#82113=CARTESIAN_POINT ( 'NONE',  ( 5.082755093536325930, -11.46875000204838635, -5.082755093536325042 ) ) ;
#82114=CARTESIAN_POINT ( 'NONE',  ( 6.943926999490791729, 29.46699007373851842, -3.973092371898545139 ) ) ;
#82126=CARTESIAN_POINT ( 'NONE',  ( 2.977408999572650927, -29.37500000204838457, -7.188101187500001821 ) ) ;
#82130=CARTESIAN_POINT ( 'NONE',  ( 9.926810856659656679, 15.46725112412266334, 1.404490565847983152 ) ) ;
#82135=CARTESIAN_POINT ( 'NONE',  ( -9.918579450955565591, 33.79303912968686774, 1.297207292923860056 ) ) ;
#82178=CARTESIAN_POINT ( 'NONE',  ( 6.944031699373470978, 85.53460654556131715, 3.972913591453821613 ) ) ;
#82187=CARTESIAN_POINT ( 'NONE',  ( -7.188101187500000044, -19.90625000204838457, -8.802885111219163269E-16 ) ) ;
#82247=CARTESIAN_POINT ( 'NONE',  ( 0.9654893961777153422, -30.00000000000000355, 7.122964895856731538 ) ) ;
#82258=CARTESIAN_POINT ( 'NONE',  ( 8.000000000000000000, -23.18750000409677270, 0.000000000000000000 ) ) ;
#82310=CARTESIAN_POINT ( 'NONE',  ( -3.030991683532509029, -29.99999999999999645, 6.776004774809743836 ) ) ;
#82369=CARTESIAN_POINT ( 'NONE',  ( 9.537291425704607306, 107.6440437733276951, 3.012810007366001130 ) ) ;
#82388=CARTESIAN_POINT ( 'NONE',  ( -5.656854249492379694, -10.43749999999999112, -5.656854249492380582 ) ) ;
#82458=CARTESIAN_POINT ( 'NONE',  ( -2.977408999572654480, -28.62500000204838457, 7.188101187499999156 ) ) ;
#82464=EDGE_CURVE ( 'NONE', #82728, #58245, #12083, .T. ) ;
#82518=CARTESIAN_POINT ( 'NONE',  ( -5.656854249492381470, -25.06249999999999289, 5.656854249492379694 ) ) ;
#82528=CARTESIAN_POINT ( 'NONE',  ( -8.000000000000000000, -9.031250004096769146, -3.313708498984762496 ) ) ;
#82533=FACE_OUTER_BOUND ( 'NONE', #50510, .T. ) ;
#82543=CARTESIAN_POINT ( 'NONE',  ( 4.401442555609581635E-16, -15.78125000204838635, -7.188101187500000044 ) ) ;
#82549=EDGE_CURVE ( 'NONE', #106390, #72737, #10874, .T. ) ;
#82593=VERTEX_POINT ( 'NONE', #68073 ) ;
#82597=CARTESIAN_POINT ( 'NONE',  ( 7.188101187499999156, -13.62500000204838457, 2.977408999572654924 ) ) ;
#82605=CARTESIAN_POINT ( 'NONE',  ( -7.188101187500001821, -20.37500000204838457, -2.977408999572651371 ) ) ;
#82617=AXIS2_PLACEMENT_3D ( 'NONE', #86069, #13729, #20300 ) ;
#82637=( BOUNDED_SURFACE ( )  B_SPLINE_SURFACE ( 3, 2, ( 
 ( #22886, #64910, #7714 ),
 ( #80545, #31510, #23957 ),
 ( #55723, #81078, #63337 ),
 ( #88653, #79496, #7188 ),
 ( #96232, #63866, #105371 ),
 ( #15822, #40623, #21829 ),
 ( #104293, #39057, #23412 ),
 ( #71937, #13687, #95686 ),
 ( #48702, #64391, #71392 ),
 ( #56256, #30983, #89189 ) ),
 .UNSPECIFIED., .F., .F., .F. ) 
 B_SPLINE_SURFACE_WITH_KNOTS ( ( 4, 2, 2, 2, 4 ),
 ( 3, 3 ),
 ( 0.002450517525418908181, 0.003060732775749477712, 0.003670948026080046809, 0.004891378526741185437, 0.007332239528063463560 ),
 ( 0.000000000000000000, 1.000000000000000000 ),
 .UNSPECIFIED. ) 
 GEOMETRIC_REPRESENTATION_ITEM ( )  RATIONAL_B_SPLINE_SURFACE ( (
 ( 1.000000000000000000, 0.7071067811865481278, 1.000000000000000000),
 ( 1.000000000000000000, 0.7344063550101855853, 1.000000000000000000),
 ( 1.000000000000000000, 0.7590375248711123124, 1.000000000000000000),
 ( 1.000000000000000000, 0.8038331608703979114, 1.000000000000000000),
 ( 1.000000000000000000, 0.8240352460865458806, 1.000000000000000000),
 ( 1.000000000000000000, 0.8791017378334128329, 1.000000000000000000),
 ( 1.000000000000000000, 0.9085032776980890290, 1.000000000000000000),
 ( 1.000000000000000000, 0.9784170511696809180, 1.000000000000000000),
 ( 1.000000000000000000, 0.9996598051696596876, 1.000000000000000000),
 ( 1.000000000000000000, 1.000000000000000000, 1.000000000000000000) ) ) 
 REPRESENTATION_ITEM ( '' )  SURFACE ( )  );
#82648=CARTESIAN_POINT ( 'NONE',  ( 9.918010731619567366, 26.20848315156774788, -1.300854425901584621 ) ) ;
#82649=CARTESIAN_POINT ( 'NONE',  ( -5.082755093536326818, -20.09375000204838457, 5.082755093536325042 ) ) ;
#82657=CARTESIAN_POINT ( 'NONE',  ( 9.537291425704605530, 87.64404377332773777, 3.012810007365998022 ) ) ;
#82672=CARTESIAN_POINT ( 'NONE',  ( -2.977408999572650039, -32.18750000204838813, -7.188101187500001821 ) ) ;
#82722=CARTESIAN_POINT ( 'NONE',  ( 7.744329845603314944, 88.46288230153457732, -2.018701143083231120 ) ) ;
#82728=VERTEX_POINT ( 'NONE', #78283 ) ;
#82732=CARTESIAN_POINT ( 'NONE',  ( -2.977408999572654480, -10.62500000204838813, 7.188101187499999156 ) ) ;
#82747=ORIENTED_EDGE ( 'NONE', *, *, #62176, .T. ) ;
#82766=ORIENTED_EDGE ( 'NONE', *, *, #68601, .T. ) ;
#82767=CARTESIAN_POINT ( 'NONE',  ( 7.999912353029502654, 81.00017529396907889, -0.2691822806795008405 ) ) ;
#82788=CARTESIAN_POINT ( 'NONE',  ( -7.188101187500000044, -22.90625000204838457, -8.802885111219163269E-16 ) ) ;
#82794=SURFACE_STYLE_USAGE ( .BOTH. , #93011 ) ;
#82799=CARTESIAN_POINT ( 'NONE',  ( 5.656854249492380582, -24.50000000409677270, -5.656854249492379694 ) ) ;
#82803=CARTESIAN_POINT ( 'NONE',  ( 9.482945380845299255, 32.44333058778931189, 3.177595346755239802 ) ) ;
#82806=CARTESIAN_POINT ( 'NONE',  ( -3.572352985694997152, 15.21714514899093018, -9.341953373613581135 ) ) ;
#82817=CARTESIAN_POINT ( 'NONE',  ( 3.313708498984762496, -15.96875000409677270, 7.999999999999998224 ) ) ;
#82844=ORIENTED_EDGE ( 'NONE', *, *, #47594, .F. ) ;
#82859=SURFACE_SIDE_STYLE ('',( #105535 ) ) ;
#82892=CARTESIAN_POINT ( 'NONE',  ( 7.211357414135266986, 102.9885346006555551, 3.467230644691329911 ) ) ;
#82936=( BOUNDED_CURVE ( )  B_SPLINE_CURVE ( 2, ( #3251, #60449, #36722, #85225, #19479, #44244, #37244, #69587, #62043 ),
 .UNSPECIFIED., .F., .F. ) 
 B_SPLINE_CURVE_WITH_KNOTS ( ( 3, 2, 2, 2, 3 ),
 ( 0.8970588235294119084, 0.9044117647058824705, 0.9117647058823530326, 0.9191176470588235947, 0.9264705882352942679 ),
 .UNSPECIFIED. ) 
 CURVE ( )  GEOMETRIC_REPRESENTATION_ITEM ( )  RATIONAL_B_SPLINE_CURVE ( ( 0.9999999999999988898, 0.9238795325112878487, 1.000000000000000000, 0.9238795325112867385, 1.000000000000000000, 0.9238795325112867385, 1.000000000000000000, 0.9238795325112856283, 1.000000000000001110 ) ) 
 REPRESENTATION_ITEM ( '' )  );
#82955=EDGE_CURVE ( 'NONE', #93124, #44948, #47499, .T. ) ;
#82959=CARTESIAN_POINT ( 'NONE',  ( -7.934996450857313199, 81.13137543527471962, -1.050865690281774123 ) ) ;
#82991=CARTESIAN_POINT ( 'NONE',  ( -2.977408999572650039, -33.68750000204839523, -7.188101187500001821 ) ) ;
#83000=DIRECTION ( 'NONE',  ( 0.000000000000000000, 1.000000000000000000, 0.000000000000000000 ) ) ;
#83026=ADVANCED_FACE ( 'NONE', ( #82533 ), #10226, .T. ) ;
#83050=CARTESIAN_POINT ( 'NONE',  ( -10.00000000000000355, 15.00000000000000000, -10.00000000000000000 ) ) ;
#83051=CARTESIAN_POINT ( 'NONE',  ( 8.000000000000000000, -27.40625000000000000, -3.313708498984761608 ) ) ;
#83074=CARTESIAN_POINT ( 'NONE',  ( -5.082755093536325042, -11.09375000204838457, -5.082755093536325930 ) ) ;
#83079=AXIS2_PLACEMENT_3D ( 'NONE', #9686, #1041, #42596 ) ;
#83106=CARTESIAN_POINT ( 'NONE',  ( -10.00000000000000355, 15.00000000000000000, -10.00000000000000000 ) ) ;
#83127=CARTESIAN_POINT ( 'NONE',  ( 4.401442555609581635E-16, -14.65625000204838457, -7.188101187500000044 ) ) ;
#83135=CARTESIAN_POINT ( 'NONE',  ( 4.401442555609581635E-16, -20.65625000204838813, -7.188101187500000044 ) ) ;
#83174=CARTESIAN_POINT ( 'NONE',  ( 9.843039827103243766, 26.40916497491665993, -1.781495459429551786 ) ) ;
#83176=CARTESIAN_POINT ( 'NONE',  ( -7.188101187500001821, -17.37500000204838813, -2.977408999572651371 ) ) ;
#83183=CARTESIAN_POINT ( 'NONE',  ( 9.253500431420432548, 86.29771549917710161, 3.792688295761950101 ) ) ;
#83190=CARTESIAN_POINT ( 'NONE',  ( -10.00000000000000355, 85.00000000000000000, 0.000000000000000000 ) ) ;
#83192=( GEOMETRIC_REPRESENTATION_CONTEXT ( 3 ) GLOBAL_UNCERTAINTY_ASSIGNED_CONTEXT ( ( #100971 ) ) GLOBAL_UNIT_ASSIGNED_CONTEXT ( ( #35881, #33731, #58529 ) ) REPRESENTATION_CONTEXT ( 'NONE', 'WORKASPACE' ) );
#83200=CARTESIAN_POINT ( 'NONE',  ( 7.188101187500000044, -34.15625000204838813, 0.000000000000000000 ) ) ;
#83205=CARTESIAN_POINT ( 'NONE',  ( -9.333079356992103115, 31.77833080074871930, 3.592383266237781037 ) ) ;
#83214=ADVANCED_FACE ( 'NONE', ( #9031 ), #51079, .T. ) ;
#83230=CIRCLE ( 'NONE', #97013, 10.00000000000000000 ) ;
#83248=CARTESIAN_POINT ( 'NONE',  ( 6.944371705245973025, 85.53899691424548735, -3.972324460300564297 ) ) ;
#83258=CARTESIAN_POINT ( 'NONE',  ( 2.977408999572650927, -14.37500000204838635, -7.188101187500001821 ) ) ;
#83295=CARTESIAN_POINT ( 'NONE',  ( 6.928203230275510549, 84.73473843067414180, 4.000000000000000000 ) ) ;
#83316=CARTESIAN_POINT ( 'NONE',  ( 2.977408999572652260, -26.93750000204838457, 7.188101187500000044 ) ) ;
#83323=CARTESIAN_POINT ( 'NONE',  ( -8.000000000000001776, -25.34375000409676915, 3.313708498984758943 ) ) ;
#83330=CARTESIAN_POINT ( 'NONE',  ( -3.979266480701241449, -30.00000000000000000, -6.940132439339150139 ) ) ;
#83354=CARTESIAN_POINT ( 'NONE',  ( 8.000000000000000000, -12.49999999999999289, 0.000000000000000000 ) ) ;
#83364=CARTESIAN_POINT ( 'NONE',  ( -6.928203230275512325, 30.26930929695538808, -3.999999999999999112 ) ) ;
#83376=VECTOR ( 'NONE', #42093, 1000.000000000000000 ) ;
#83422=VECTOR ( 'NONE', #9142, 1000.000000000000000 ) ;
#83431=CARTESIAN_POINT ( 'NONE',  ( 9.221346651730840449, 106.0483402006833984, -3.869102247876033740 ) ) ;
#83481=CARTESIAN_POINT ( 'NONE',  ( -7.002990960197238657, 83.94733181616544471, 3.868040364119522234 ) ) ;
#83567=CARTESIAN_POINT ( 'NONE',  ( 7.999999999999998224, -29.09374999999999289, 3.313708498984766493 ) ) ;
#83573=CARTESIAN_POINT ( 'NONE',  ( -8.000000000000001776, -8.843750004096769146, 3.313708498984759387 ) ) ;
#83584=CARTESIAN_POINT ( 'NONE',  ( 6.944371705245971249, 105.5389969142454731, -3.972324460300566962 ) ) ;
#83649=CARTESIAN_POINT ( 'NONE',  ( 5.082755093536325930, -22.34375000204838457, -5.082755093536325042 ) ) ;
#83666=ADVANCED_FACE ( 'NONE', ( #89314 ), #105613, .F. ) ;
#83687=CARTESIAN_POINT ( 'NONE',  ( 4.898587196589412829E-16, -21.12499999999999289, -8.000000000000000000 ) ) ;
#83696=CARTESIAN_POINT ( 'NONE',  ( -5.082755093536325042, -21.96875000204838457, -5.082755093536325930 ) ) ;
#83705=CYLINDRICAL_SURFACE ( 'NONE', #106454, 8.000000000000000000 ) ;
#83718=EDGE_CURVE ( 'NONE', #18153, #68507, #64620, .T. ) ;
#83721=CARTESIAN_POINT ( 'NONE',  ( 2.977408999572651815, -32.93750000204839523, 7.188101187500000933 ) ) ;
#83732=EDGE_LOOP ( 'NONE', ( #82844, #10223 ) ) ;
#83776=ORIENTED_EDGE ( 'NONE', *, *, #37754, .F. ) ;
#83782=CARTESIAN_POINT ( 'NONE',  ( 5.082755093536325930, -15.96875000204838635, -5.082755093536325042 ) ) ;
#83822=CARTESIAN_POINT ( 'NONE',  ( 7.618844049274130725, 81.82764101070543461, 2.450177051822845620 ) ) ;
#83848=CARTESIAN_POINT ( 'NONE',  ( -7.188101187500000933, -23.00000000204839523, -2.977408999572651371 ) ) ;
#83856=CARTESIAN_POINT ( 'NONE',  ( -3.313708498984760720, -25.71875000409677625, -8.000000000000000000 ) ) ;
#83921=CARTESIAN_POINT ( 'NONE',  ( 0.7408669144222883585, 15.11700796859930307, 9.999999999997886135 ) ) ;
#83976=CARTESIAN_POINT ( 'NONE',  ( -1.469576158976823947E-15, -10.06250000409677092, 8.000000000000000000 ) ) ;
#83979=ORIENTED_EDGE ( 'NONE', *, *, #77049, .F. ) ;
#83989=EDGE_CURVE ( 'NONE', #14996, #91623, #45328, .T. ) ;
#83996=CARTESIAN_POINT ( 'NONE',  ( 4.898587196589412829E-16, -25.81250000409677270, -8.000000000000000000 ) ) ;
#84023=CARTESIAN_POINT ( 'NONE',  ( -9.843039827103241990, 108.5908350250833649, -1.781495459429543127 ) ) ;
#84032=DIRECTION ( 'NONE',  ( -0.000000000000000000, 1.000000000000000000, -0.000000000000000000 ) ) ;
#84036=CARTESIAN_POINT ( 'NONE',  ( -1.469576158976823947E-15, -23.56250000409677270, 8.000000000000000000 ) ) ;
#84041=DIRECTION ( 'NONE',  ( 0.000000000000000000, 1.000000000000000000, 0.000000000000000000 ) ) ;
#84114=CARTESIAN_POINT ( 'NONE',  ( -8.000000000000000000, -26.74999999999999645, -9.797174393178825657E-16 ) ) ;
#84118=CARTESIAN_POINT ( 'NONE',  ( -10.00000000000000178, 16.00000000000000000, -4.582575694955835388 ) ) ;
#84143=CARTESIAN_POINT ( 'NONE',  ( -7.188101187500001821, -9.500000002048386349, -2.977408999572651371 ) ) ;
#84193=VERTEX_POINT ( 'NONE', #29935 ) ;
#84197=CARTESIAN_POINT ( 'NONE',  ( 7.188101187500000933, -10.43750000204838457, -2.977408999572650483 ) ) ;
#84204=CARTESIAN_POINT ( 'NONE',  ( 5.082755093536324154, -22.71875000204838457, 5.082755093536326818 ) ) ;
#84211=CARTESIAN_POINT ( 'NONE',  ( -8.000000000000001776, -14.84375000409677092, 3.313708498984759387 ) ) ;
#84238=AXIS2_PLACEMENT_3D ( 'NONE', #78067, #94807, #38180 ) ;
#84244=CARTESIAN_POINT ( 'NONE',  ( 2.977408999572650927, -22.25000000204839168, -7.188101187500001821 ) ) ;
#84269=CARTESIAN_POINT ( 'NONE',  ( 7.188101187500000044, -28.15625000204838813, 0.000000000000000000 ) ) ;
#84289=CARTESIAN_POINT ( 'NONE',  ( 9.989435848181784650, 101.0261970747157250, -0.5278651953176017875 ) ) ;
#84323=CARTESIAN_POINT ( 'NONE',  ( -5.082755093536325042, -23.46875000204838457, -5.082755093536325930 ) ) ;
#84332=CARTESIAN_POINT ( 'NONE',  ( -7.188101187500000044, -12.40625000204838635, -8.802885111219163269E-16 ) ) ;
#84337=CARTESIAN_POINT ( 'NONE',  ( 0.000000000000000000, 15.00000000000000000, 0.000000000000000000 ) ) ;
#84340=B_SPLINE_CURVE_WITH_KNOTS ( 'NONE', 3,
 ( #90699, #49148, #15201, #48089, #106318, #16263, #73964, #44, #33017, #65883, #98764, #24917, #57771, #33536, #101965, #26534, #18423, #100896, #69091, #85260, #84730, #35688 ),
 .UNSPECIFIED., .F., .F.,
 ( 4, 2, 2, 2, 2, 2, 2, 2, 2, 2, 4 ),
 ( 2.543397799394530001E-16, 0.001421275008199062145, 0.002842550016397869719, 0.003553187520497273506, 0.004263825024596677726, 0.005685100032795484433, 0.007106375040994290272, 0.007817012545093694059, 0.008527650049193096979, 0.009948925057391901083, 0.01137020006559070519 ),
 .UNSPECIFIED. ) ;
#84371=CARTESIAN_POINT ( 'NONE',  ( 7.896571385775229324, 81.21002000654247865, 1.305932416347436620 ) ) ;
#84393=CARTESIAN_POINT ( 'NONE',  ( 5.082755093536325930, -24.96875000204838813, -5.082755093536325042 ) ) ;
#84402=CARTESIAN_POINT ( 'NONE',  ( -3.313708498984760720, -19.71875000409677270, -8.000000000000000000 ) ) ;
#84406=DIRECTION ( 'NONE',  ( -0.000000000000000000, 1.000000000000000000, -0.000000000000000000 ) ) ;
#84410=CARTESIAN_POINT ( 'NONE',  ( 0.2291258134149000425, -29.99999999999999645, -7.774924953687139428 ) ) ;
#84434=VERTEX_POINT ( 'NONE', #87362 ) ;
#84526=CARTESIAN_POINT ( 'NONE',  ( -5.656854249492381470, -20.56249999999999289, 5.656854249492379694 ) ) ;
#84534=CARTESIAN_POINT ( 'NONE',  ( -7.003653396366579464, 103.9429379444032264, -3.866846144092870752 ) ) ;
#84601=EDGE_CURVE ( 'NONE', #94586, #3543, #82936, .T. ) ;
#84651=CARTESIAN_POINT ( 'NONE',  ( 5.656854249492380582, -25.81249999999999645, -5.656854249492379694 ) ) ;
#84657=EDGE_CURVE ( 'NONE', #77405, #6205, #7847, .T. ) ;
#84669=CARTESIAN_POINT ( 'NONE',  ( 7.801777176595949825, 108.5882798581263131, -1.786991866639918936 ) ) ;
#84730=CARTESIAN_POINT ( 'NONE',  ( 1.435596609963271764, -30.00000000000001066, 7.059243743694297635 ) ) ;
#84735=CARTESIAN_POINT ( 'NONE',  ( -7.188101187500001821, -23.37500000204839168, -2.977408999572651371 ) ) ;
#84776=CARTESIAN_POINT ( 'NONE',  ( -5.082755093536325042, -20.46875000204838813, -5.082755093536325930 ) ) ;
#84780=FACE_OUTER_BOUND ( 'NONE', #105450, .T. ) ;
#84792=CARTESIAN_POINT ( 'NONE',  ( -10.00000000000000355, 15.00000000000000000, -10.00000000000000000 ) ) ;
#84804=CARTESIAN_POINT ( 'NONE',  ( 4.401442555609581635E-16, -23.28125000204838457, -7.188101187500000044 ) ) ;
#84809=ORIENTED_EDGE ( 'NONE', *, *, #34277, .F. ) ;
#84852=CARTESIAN_POINT ( 'NONE',  ( -7.188101187500000933, -27.87500000204838457, -2.977408999572651371 ) ) ;
#84863=CARTESIAN_POINT ( 'NONE',  ( 4.401442555609581635E-16, -11.28125000204838457, -7.188101187500000044 ) ) ;
#84864=CARTESIAN_POINT ( 'NONE',  ( -8.000000000000000000, -18.03125000409677270, -3.313708498984762496 ) ) ;
#84883=CARTESIAN_POINT ( 'NONE',  ( 5.656854249492378806, -23.37500000409677270, 5.656854249492381470 ) ) ;
#84901=CARTESIAN_POINT ( 'NONE',  ( 7.896165657598944065, 81.21088868628027058, -1.307894402814552937 ) ) ;
#84923=CARTESIAN_POINT ( 'NONE',  ( 2.977408999572650927, -24.87500000204838813, -7.188101187500000933 ) ) ;
#84931=CARTESIAN_POINT ( 'NONE',  ( 7.999999999999998224, -20.28125000409677625, 3.313708498984766493 ) ) ;
#84970=CARTESIAN_POINT ( 'NONE',  ( -3.313708498984746065, -29.46874999999999645, 8.000000000000017764 ) ) ;
#84991=CARTESIAN_POINT ( 'NONE',  ( 7.188101187499999156, -31.25000000204838813, 2.977408999572654924 ) ) ;
#84994=CARTESIAN_POINT ( 'NONE',  ( 3.409011323177081998, 15.24615751665884922, 9.403185743875308589 ) ) ;
#85069=DIRECTION ( 'NONE',  ( 1.000000000000000000, -0.000000000000000000, -0.000000000000000000 ) ) ;
#85071=DIRECTION ( 'NONE',  ( 1.000000000000000000, -0.000000000000000000, -0.000000000000000000 ) ) ;
#85072=CARTESIAN_POINT ( 'NONE',  ( 3.313708498984800688, -18.78124999999998934, 7.999999999999960032 ) ) ;
#85079=EDGE_CURVE ( 'NONE', #44667, #33604, #31307, .T. ) ;
#85153=ORIENTED_EDGE ( 'NONE', *, *, #60456, .T. ) ;
#85178=CARTESIAN_POINT ( 'NONE',  ( 3.313708498984762052, -19.71874999999999645, -8.000000000000000000 ) ) ;
#85180=DIRECTION ( 'NONE',  ( -0.000000000000000000, -1.000000000000000000, -0.000000000000000000 ) ) ;
#85202=CARTESIAN_POINT ( 'NONE',  ( -4.413590570192278406, -9.188952443232103917, 5.751919616880371677 ) ) ;
#85223=CARTESIAN_POINT ( 'NONE',  ( -5.656854249492379694, -25.43749999999999645, -5.656854249492380582 ) ) ;
#85225=CARTESIAN_POINT ( 'NONE',  ( -8.000000000000000000, -11.84374999999999289, -3.313708498984762496 ) ) ;
#85243=ORIENTED_EDGE ( 'NONE', *, *, #67703, .F. ) ;
#85248=CARTESIAN_POINT ( 'NONE',  ( -9.165151389911679658, 104.9999999999999858, -4.000000000000001776 ) ) ;
#85260=CARTESIAN_POINT ( 'NONE',  ( 1.899847863968399331, -30.00000000000001066, 6.948366715868964150 ) ) ;
#85265=CARTESIAN_POINT ( 'NONE',  ( 2.977408999572651815, -15.31250000204838457, 7.188101187500000933 ) ) ;
#85307=CARTESIAN_POINT ( 'NONE',  ( 7.188101187499999156, -13.62500000204838457, 2.977408999572654924 ) ) ;
#85319=CARTESIAN_POINT ( 'NONE',  ( 9.537927238823508347, 87.64626857118182102, -3.010735687602429156 ) ) ;
#85336=CARTESIAN_POINT ( 'NONE',  ( 7.188101187500001821, -26.56250000204838457, -2.977408999572650483 ) ) ;
#85352=CARTESIAN_POINT ( 'NONE',  ( -8.000000000000001776, -22.34375000409677270, 3.313708498984759387 ) ) ;
#85382=AXIS2_PLACEMENT_3D ( 'NONE', #9072, #84041, #74860 ) ;
#85391=CARTESIAN_POINT ( 'NONE',  ( -5.082755093536326818, -27.59375000204838813, 5.082755093536325042 ) ) ;
#85398=CARTESIAN_POINT ( 'NONE',  ( 7.188101187500000044, -30.03125000204838813, 0.000000000000000000 ) ) ;
#85436=DIRECTION ( 'NONE',  ( 0.000000000000000000, 0.000000000000000000, 1.000000000000000000 ) ) ;
#85455=CARTESIAN_POINT ( 'NONE',  ( -7.188101187500002709, -21.31250000204838813, 2.977408999572647819 ) ) ;
#85458=AXIS2_PLACEMENT_3D ( 'NONE', #86280, #102439, #87329 ) ;
#85463=CARTESIAN_POINT ( 'NONE',  ( -9.165151389911679658, 85.00000000000000000, 4.000000000000000000 ) ) ;
#85467=CARTESIAN_POINT ( 'NONE',  ( 8.000000000000000000, -17.18750000409676915, 0.000000000000000000 ) ) ;
#85477=CARTESIAN_POINT ( 'NONE',  ( 6.643741133345863581, -29.99999999999999645, -3.073381310751047035 ) ) ;
#85482=CARTESIAN_POINT ( 'NONE',  ( 0.000000000000000000, -30.00000000000000000, 8.000000000000000000 ) ) ;
#85488=VECTOR ( 'NONE', #95927, 1000.000000000000000 ) ;
#85534=CARTESIAN_POINT ( 'NONE',  ( 4.401442555609581635E-16, -26.28125000204838813, -7.188101187500000044 ) ) ;
#85559=PRESENTATION_STYLE_ASSIGNMENT (( #26811 ) ) ;
#85579=CARTESIAN_POINT ( 'NONE',  ( 8.000000000000000000, -15.49999999999999289, 0.000000000000000000 ) ) ;
#85635=CARTESIAN_POINT ( 'NONE',  ( -9.333892298909264085, 106.7827573162503541, -3.590295303293453255 ) ) ;
#85730=CARTESIAN_POINT ( 'NONE',  ( 5.656854249492380582, -21.31249999999999289, -5.656854249492379694 ) ) ;
#85753=AXIS2_PLACEMENT_3D ( 'NONE', #35561, #68436, #94306 ) ;
#85766=CARTESIAN_POINT ( 'NONE',  ( -1.469576158976823947E-15, -29.56250000409677270, 8.000000000000000000 ) ) ;
#85772=CARTESIAN_POINT ( 'NONE',  ( -3.999994092537668244, -10.00072617203139380, 6.928206640937045080 ) ) ;
#85792=EDGE_CURVE ( 'NONE', #90051, #56071, #45143, .T. ) ;
#85800=FACE_OUTER_BOUND ( 'NONE', #92569, .T. ) ;
#85804=CARTESIAN_POINT ( 'NONE',  ( -9.918325909156571640, 101.2076476829256819, 1.298699613733151015 ) ) ;
#85820=CARTESIAN_POINT ( 'NONE',  ( 5.082755093536325930, -16.34375000204838813, -5.082755093536325042 ) ) ;
#85835=CARTESIAN_POINT ( 'NONE',  ( -7.150053860865851263, 86.78265453913975591, 3.590189269391290239 ) ) ;
#85861=LINE ( 'NONE', #92319, #2419 ) ;
#85863=CARTESIAN_POINT ( 'NONE',  ( -7.188101187500002709, -12.68750000204838635, 2.977408999572648707 ) ) ;
#85877=CARTESIAN_POINT ( 'NONE',  ( 3.313708498984742512, -28.71874999999999289, -8.000000000000019540 ) ) ;
#85889=CARTESIAN_POINT ( 'NONE',  ( -2.977408999572654480, -27.12500000204838457, 7.188101187499999156 ) ) ;
#85903=CARTESIAN_POINT ( 'NONE',  ( 7.999999999999998224, -21.78125000409677625, 3.313708498984766049 ) ) ;
#85907=CARTESIAN_POINT ( 'NONE',  ( 9.333892298909264085, 103.2172426837496602, -3.590295303293454587 ) ) ;
#85941=LINE ( 'NONE', #45992, #40727 ) ;
#85942=CARTESIAN_POINT ( 'NONE',  ( 4.401442555609581635E-16, -26.65625000204838813, -7.188101187500000044 ) ) ;
#85951=CARTESIAN_POINT ( 'NONE',  ( 2.977408999572651815, -31.81250000204839168, 7.188101187500000933 ) ) ;
#85956=CARTESIAN_POINT ( 'NONE',  ( -7.800703710507054467, 108.5859569265794136, 1.791736796405269505 ) ) ;
#85992=CARTESIAN_POINT ( 'NONE',  ( -7.188101187500001821, -29.37500000204838457, -2.977408999572651371 ) ) ;
#86008=CARTESIAN_POINT ( 'NONE',  ( -7.188101187500000933, -17.00000000204838813, -2.977408999572651371 ) ) ;
#86015=CARTESIAN_POINT ( 'NONE',  ( -9.334514330295430540, 83.21377262318209489, -3.588704711590609442 ) ) ;
#86017=CARTESIAN_POINT ( 'NONE',  ( -5.656854249492381470, -19.25000000409677270, 5.656854249492379694 ) ) ;
#86019=( NAMED_UNIT ( * ) PLANE_ANGLE_UNIT ( ) SI_UNIT ( $, .RADIAN. ) );
#86022=CARTESIAN_POINT ( 'NONE',  ( -9.380894568449075877, 87.01130633110940948, -3.467341429141164610 ) ) ;
#86065=VECTOR ( 'NONE', #92951, 1000.000000000000000 ) ;
#86069=CARTESIAN_POINT ( 'NONE',  ( 0.000000000000000000, 15.00000000000000000, 0.000000000000000000 ) ) ;
#86078=CARTESIAN_POINT ( 'NONE',  ( -5.082755093536325042, -24.59375000204838813, -5.082755093536325930 ) ) ;
#86094=ADVANCED_FACE ( 'NONE', ( #72241 ), #86431, .T. ) ;
#86108=CARTESIAN_POINT ( 'NONE',  ( 3.826931552919423218, 16.00000000000000000, 9.246279647933185686 ) ) ;
#86141=EDGE_CURVE ( 'NONE', #14996, #44397, #96017, .T. ) ;
#86176=CARTESIAN_POINT ( 'NONE',  ( -9.482856158761272525, 107.4430711585472409, 3.177891129109647217 ) ) ;
#86181=ORIENTED_EDGE ( 'NONE', *, *, #22223, .T. ) ;
#86264=CARTESIAN_POINT ( 'NONE',  ( 3.313708498984762496, -21.78124999999999645, 7.999999999999998224 ) ) ;
#86280=CARTESIAN_POINT ( 'NONE',  ( 0.000000000000000000, 115.0000000000000000, 0.000000000000000000 ) ) ;
#86292=PRESENTATION_STYLE_ASSIGNMENT (( #19457 ) ) ;
#86312=EDGE_CURVE ( 'NONE', #96386, #64846, #8580, .T. ) ;
#86321=CARTESIAN_POINT ( 'NONE',  ( -9.948181520647858989, 26.13107197239622081, 1.049088206181488792 ) ) ;
#86337=CARTESIAN_POINT ( 'NONE',  ( -9.221216839714873714, 103.9524025183102083, 3.869414262756992517 ) ) ;
#86339=( NAMED_UNIT ( * ) SI_UNIT ( $, .STERADIAN. ) SOLID_ANGLE_UNIT ( ) );
#86355=CARTESIAN_POINT ( 'NONE',  ( -7.188101187500001821, -15.87500000204838635, -2.977408999572651371 ) ) ;
#86380=CARTESIAN_POINT ( 'NONE',  ( 8.000000000000000000, -17.09375000409676915, -3.313708498984761164 ) ) ;
#86385=CARTESIAN_POINT ( 'NONE',  ( 7.003653396366580353, 31.05706205559676647, -3.866846144092864090 ) ) ;
#86394=CARTESIAN_POINT ( 'NONE',  ( 2.977408999572651815, -10.81250000204838457, 7.188101187500000933 ) ) ;
#86405=CARTESIAN_POINT ( 'NONE',  ( 9.177080501238306098, 85.53346942854270196, -3.972956046786645601 ) ) ;
#86423=CARTESIAN_POINT ( 'NONE',  ( -5.082755093536325042, -24.59375000204838813, -5.082755093536325930 ) ) ;
#86431=( BOUNDED_SURFACE ( )  B_SPLINE_SURFACE ( 1, 2, ( 
 ( #64172, #431, #74875, #16661, #40401, #82991, #52604, #65748, #106722, #98628, #16123, #81908, #58175, #33400, #35952, #58729, #91628, #91102, #7485, #8024, #50598, #32871, #74353, #9086, #33943, #90018, #41995, #41463, #106178, #99158, #17738, #84991, #66271, #73283, #50085, #963, #3001, #43999, #57104, #11074, #32341, #24778, #27867, #40934, #76885, #98105, #24256, #68824, #99702, #49007, #57627, #73828, #93621, #101704, #66812, #60732, #49551, #19775, #90552, #82458, #65211, #8561, #25316, #25872, #17210, #38072, #70407, #45608, #22413, #28931, #21880, #37541, #46132, #69353, #87657, #53161, #95217, #104343, #12149, #36485, #78482, #71445, #70927, #45080, #85534, #20846, #86611, #62324, #12675, #102232, #28382, #54721, #13739, #103306, #61257, #30492, #46646, #29451, #63393, #87128, #20315, #77960, #86078, #62853, #103820, #94143, #3546, #11612, #4075, #44541, #29964, #37006, #61805, #69873, #102767, #94698, #95739, #5138, #13205, #53677, #4609, #96288, #79546, #79020, #21350, #77431, #5658, #54190, #38580, #73024, #41209, #49284, #24532, #81128, #16401, #66015, #98380, #32079, #7238, #96805, #74095, #47696, #71988, #47168, #80069, #80596, #7769, #6717, #33146, #97315, #105932, #6176, #82187, #64955, #57376, #90292, #8305, #39643, #64442, #40673, #181, #98894, #55257, #97848, #88182, #39109, #24006, #104899, #14267, #31038, #63918, #22936, #81642, #55774, #88709, #56850, #14802, #32620, #72513, #73560, #105419, #31559, #106462, #40146, #23467, #89772, #56304, #89243, #15341, #48225, #15872, #48748, #65493, #76226, #83782, #92407, #99972, #34752, #25604, #27194, #42803, #50347, #25055, #18013, #1796, #9894, #10945, #58462, #26143, #67089, #67625, #83258, #91886, #91371, #26660, #92948, #100503, #59539, #34217, #17485, #10427, #58998, #9351, #19110, #42262, #75154, #50878, #1247, #2866, #18556, #75697, #51419, #84332, #43343, #57909, #2332, #68700, #35274, #68145, #101039, #33674, #99425, #60084, #51948, #84863, #43866, #76758, #35819, #90834, #16949, #49827, #82732, #8834, #41738, #74625, #703, #66547, #28257, #37942, #61681, #62720, #77303, #21751, #94569, #3418, #45481, #5530, #53557, #69229 ),
 ( #70802, #69747, #46521, #46003, #86488, #62211, #102642, #4474, #102098, #103697, #12546, #20178, #101579, #20719, #78352, #37413, #87526, #61127, #28798, #36880, #70277, #53028, #103176, #94018, #29319, #95609, #95094, #21230, #3948, #85951, #87003, #54059, #12022, #54587, #44954, #77837, #13074, #78883, #79418, #5010, #29843, #13608, #38456, #27738, #60609, #93500, #19647, #52480, #85398, #11481, #36360, #44409, #15207, #97185, #98253, #15741, #48624, #90165, #47570, #72383, #31950, #56719, #23329, #105289, #80994, #73433, #47039, #104753, #7630, #31436, #32491, #79938, #24407, #64313, #6048, #48095, #82059, #56170, #38974, #89640, #64831, #7111, #40027, #63784, #23875, #22807, #49154, #6577, #72900, #96145, #65362, #105810, #40549, #106324, #57245, #96671, #80465, #81509, #16269, #8179, #71322, #97710, #104216, #63252, #30361, #22278, #55125, #88055, #71847, #14136, #30904, #55643, #88578, #89111, #14660, #39509, #35146, #67497, #25471, #84735, #59411, #26017, #50233, #58877, #68016, #43214, #84204, #17891, #100902, #33022, #83649, #65887, #18976, #41085, #49701, #24923, #100376, #51820, #8709, #91769, #48, #18429, #27070, #26539, #58327, #73968, #92275, #50743, #83135, #9761, #98770, #82605, #17359, #57777, #10300, #9232, #92819, #51283, #99845, #1669, #42137, #42675, #41617, #76098, #75574, #66415, #90705, #34094, #34626, #2199, #59953, #74501, #75023, #1121, #16814, #99298, #66967, #577, #33541, #91251, #94437, #20597, #20049, #77175, #103051, #44824, #69097, #78747, #101970, #28130, #77710, #61008, #95477, #12420, #85820, #3821, #78230, #52897, #43739, #86355, #54453, #93892, #3287, #11897, #19518, #85265, #61543, #36758, #37817, #62080, #94970, #29718, #69624, #102515, #4345, #29206, #28659, #53435, #45351, #12948, #93366, #44281, #53939, #37280, #4881, #52353, #70675, #70146, #11349, #21108, #21621, #86874, #36227, #45868, #103569, #62593, #10818, #76627, #2738, #35693, #68568, #101453, #27605, #60486, #81392, #31304, #23741, #56592, #48497, #79816, #96548, #72774, #64190, #73300, #88980, #22144, #14006, #54995, #64703, #39900, #30229, #5410, #13478, #63116, #24272, #105680, #5920, #30774, #104090 ) ),
 .UNSPECIFIED., .F., .F., .T. ) 
 B_SPLINE_SURFACE_WITH_KNOTS ( ( 2, 2 ),
 ( 3, 2, 2, 2, 2, 2, 2, 2, 2, 2, 2, 2, 2, 2, 2, 2, 2, 2, 2, 2, 2, 2, 2, 2, 2, 2, 2, 2, 2, 2, 2, 2, 2, 2, 2, 2, 2, 2, 2, 2, 2, 2, 2, 2, 2, 2, 2, 2, 2, 2, 2, 2, 2, 2, 2, 2, 2, 2, 2, 2, 2, 2, 2, 2, 2, 2, 2, 2, 2, 2, 2, 2, 2, 2, 2, 2, 2, 2, 2, 2, 2, 2, 2, 2, 2, 2, 2, 2, 2, 2, 2, 2, 2, 2, 2, 2, 2, 2, 2, 2, 2, 2, 2, 2, 2, 2, 2, 2, 2, 2, 2, 2, 2, 2, 2, 2, 2, 2, 2, 2, 2, 2, 2, 2, 2, 2, 2, 2, 2, 2, 2, 2, 2, 2, 3 ),
 ( 0.000000000000000000, 1.000000000000000000 ),
 ( 0.000000000000000000, 0.007352941176470588133, 0.01470588235294117627, 0.02205882352941176613, 0.02941176470588235253, 0.03676470588235294240, 0.04411764705882353227, 0.05147058823529411520, 0.05882352941176470507, 0.06617647058823529493, 0.07352941176470588480, 0.08088235294117647467, 0.08823529411764706454, 0.09558823529411764053, 0.1029411764705882304, 0.1102941176470588203, 0.1176470588235294101, 0.1250000000000000000, 0.1323529411764705899, 0.1397058823529411797, 0.1470588235294117696, 0.1544117647058823595, 0.1617647058823529493, 0.1691176470588235392, 0.1764705882352941291, 0.1838235294117647189, 0.1911764705882352811, 0.1985294117647058709, 0.2058823529411764608, 0.2132352941176470507, 0.2205882352941176405, 0.2279411764705882304, 0.2352941176470588203, 0.2426470588235294101, 0.2500000000000000000, 0.2573529411764705621, 0.2647058823529411797, 0.2720588235294117418, 0.2794117647058823595, 0.2867647058823529216, 0.2941176470588235392, 0.3014705882352941013, 0.3088235294117647189, 0.3161764705882352811, 0.3235294117647058987, 0.3308823529411764608, 0.3382352941176470784, 0.3455882352941176405, 0.3529411764705882582, 0.3602941176470588203, 0.3676470588235294379, 0.3750000000000000000, 0.3823529411764705621, 0.3897058823529411797, 0.3970588235294117418, 0.4044117647058823595, 0.4117647058823529216, 0.4191176470588235392, 0.4264705882352941013, 0.4338235294117647189, 0.4411764705882352811, 0.4485294117647058987, 0.4558823529411764608, 0.4632352941176470784, 0.4705882352941176405, 0.4779411764705882582, 0.4852941176470588203, 0.4926470588235294379, 0.5000000000000000000, 0.5073529411764705621, 0.5147058823529411242, 0.5220588235294117974, 0.5294117647058823595, 0.5367647058823529216, 0.5441176470588234837, 0.5514705882352941568, 0.5588235294117647189, 0.5661764705882352811, 0.5735294117647058432, 0.5808823529411765163, 0.5882352941176470784, 0.5955882352941176405, 0.6029411764705882026, 0.6102941176470588758, 0.6176470588235294379, 0.6250000000000000000, 0.6323529411764705621, 0.6397058823529411242, 0.6470588235294117974, 0.6544117647058823595, 0.6617647058823529216, 0.6691176470588234837, 0.6764705882352941568, 0.6838235294117647189, 0.6911764705882352811, 0.6985294117647058432, 0.7058823529411765163, 0.7132352941176470784, 0.7205882352941176405, 0.7279411764705882026, 0.7352941176470588758, 0.7426470588235294379, 0.7500000000000000000, 0.7573529411764705621, 0.7647058823529411242, 0.7720588235294117974, 0.7794117647058823595, 0.7867647058823529216, 0.7941176470588234837, 0.8014705882352941568, 0.8088235294117647189, 0.8161764705882352811, 0.8235294117647058432, 0.8308823529411765163, 0.8382352941176470784, 0.8455882352941176405, 0.8529411764705882026, 0.8602941176470588758, 0.8676470588235294379, 0.8750000000000000000, 0.8823529411764705621, 0.8897058823529411242, 0.8970588235294117974, 0.9044117647058823595, 0.9117647058823529216, 0.9191176470588234837, 0.9264705882352941568, 0.9338235294117647189, 0.9411764705882352811, 0.9485294117647058432, 0.9558823529411765163, 0.9632352941176470784, 0.9705882352941176405, 0.9779411764705882026, 0.9804062476879973342 ),
 .UNSPECIFIED. ) 
 GEOMETRIC_REPRESENTATION_ITEM ( )  RATIONAL_B_SPLINE_SURFACE ( (
 ( 1.000000000000000000, 0.9238795325112867385, 1.000000000000000000, 0.9238795325112867385, 1.000000000000000000, 0.9238795325112867385, 1.000000000000000000, 0.9238795325112867385, 1.000000000000000000, 0.9238795325112867385, 1.000000000000000000, 0.9238795325112867385, 1.000000000000000000, 0.9238795325112867385, 1.000000000000000000, 0.9238795325112867385, 1.000000000000000000, 0.9238795325112867385, 1.000000000000000000, 0.9238795325112867385, 1.000000000000000000, 0.9238795325112867385, 1.000000000000000000, 0.9238795325112867385, 1.000000000000000000, 0.9238795325112867385, 1.000000000000000000, 0.9238795325112867385, 1.000000000000000000, 0.9238795325112867385, 1.000000000000000000, 0.9238795325112867385, 1.000000000000000000, 0.9238795325112867385, 1.000000000000000000, 0.9238795325112867385, 1.000000000000000000, 0.9238795325112867385, 1.000000000000000000, 0.9238795325112867385, 1.000000000000000000, 0.9238795325112867385, 1.000000000000000000, 0.9238795325112867385, 1.000000000000000000, 0.9238795325112867385, 1.000000000000000000, 0.9238795325112867385, 1.000000000000000000, 0.9238795325112867385, 1.000000000000000000, 0.9238795325112867385, 1.000000000000000000, 0.9238795325112867385, 1.000000000000000000, 0.9238795325112867385, 1.000000000000000000, 0.9238795325112867385, 1.000000000000000000, 0.9238795325112867385, 1.000000000000000000, 0.9238795325112867385, 1.000000000000000000, 0.9238795325112867385, 1.000000000000000000, 0.9238795325112867385, 1.000000000000000000, 0.9238795325112867385, 1.000000000000000000, 0.9238795325112867385, 1.000000000000000000, 0.9238795325112867385, 1.000000000000000000, 0.9238795325112867385, 1.000000000000000000, 0.9238795325112867385, 1.000000000000000000, 0.9238795325112867385, 1.000000000000000000, 0.9238795325112867385, 1.000000000000000000, 0.9238795325112867385, 1.000000000000000000, 0.9238795325112867385, 1.000000000000000000, 0.9238795325112867385, 1.000000000000000000, 0.9238795325112867385, 1.000000000000000000, 0.9238795325112867385, 1.000000000000000000, 0.9238795325112867385, 1.000000000000000000, 0.9238795325112867385, 1.000000000000000000, 0.9238795325112867385, 1.000000000000000000, 0.9238795325112867385, 1.000000000000000000, 0.9238795325112867385, 1.000000000000000000, 0.9238795325112867385, 1.000000000000000000, 0.9238795325112867385, 1.000000000000000000, 0.9238795325112867385, 1.000000000000000000, 0.9238795325112867385, 1.000000000000000000, 0.9238795325112867385, 1.000000000000000000, 0.9238795325112867385, 1.000000000000000000, 0.9238795325112867385, 1.000000000000000000, 0.9238795325112867385, 1.000000000000000000, 0.9238795325112867385, 1.000000000000000000, 0.9238795325112867385, 1.000000000000000000, 0.9238795325112867385, 1.000000000000000000, 0.9238795325112867385, 1.000000000000000000, 0.9238795325112867385, 1.000000000000000000, 0.9238795325112867385, 1.000000000000000000, 0.9238795325112867385, 1.000000000000000000, 0.9238795325112867385, 1.000000000000000000, 0.9238795325112867385, 1.000000000000000000, 0.9238795325112867385, 1.000000000000000000, 0.9238795325112867385, 1.000000000000000000, 0.9238795325112867385, 1.000000000000000000, 0.9238795325112867385, 1.000000000000000000, 0.9238795325112867385, 1.000000000000000000, 0.9238795325112867385, 1.000000000000000000, 0.9238795325112867385, 1.000000000000000000, 0.9238795325112867385, 1.000000000000000000, 0.9238795325112867385, 1.000000000000000000, 0.9238795325112867385, 1.000000000000000000, 0.9238795325112867385, 1.000000000000000000, 0.9238795325112867385, 1.000000000000000000, 0.9238795325112867385, 1.000000000000000000, 0.9238795325112867385, 1.000000000000000000, 0.9238795325112867385, 1.000000000000000000, 0.9238795325112867385, 1.000000000000000000, 0.9238795325112867385, 1.000000000000000000, 0.9238795325112867385, 1.000000000000000000, 0.9238795325112867385, 1.000000000000000000, 0.9238795325112867385, 1.000000000000000000, 0.9238795325112867385, 1.000000000000000000, 0.9238795325112867385, 1.000000000000000000, 0.9238795325112867385, 1.000000000000000000, 0.9238795325112867385, 1.000000000000000000, 0.9238795325112867385, 1.000000000000000000, 0.9238795325112867385, 1.000000000000000000, 0.9238795325112867385, 1.000000000000000000, 0.9238795325112867385, 1.000000000000000000, 0.9238795325112867385, 1.000000000000000000, 0.9238795325112867385, 1.000000000000000000, 0.9238795325112867385, 1.000000000000000000, 0.9238795325112867385, 1.000000000000000000, 0.9238795325112867385, 1.000000000000000000, 0.9238795325112867385, 1.000000000000000000, 0.9238795325112867385, 1.000000000000000000, 0.9238795325112867385, 1.000000000000000000, 0.9238795325112867385, 1.000000000000000000, 0.9238795325112867385, 1.000000000000000000, 0.9238795325112867385, 1.000000000000000000, 0.9238795325112867385, 1.000000000000000000, 0.9238795325112867385, 1.000000000000000000, 0.9238795325112867385, 1.000000000000000000, 0.9238795325112867385, 1.000000000000000000, 0.9238795325112867385, 1.000000000000000000, 0.9238795325112867385, 1.000000000000000000, 0.9238795325112867385, 1.000000000000000000, 0.9238795325112867385, 1.000000000000000000, 0.9238795325112867385, 1.000000000000000000, 0.9238795325112867385, 1.000000000000000000, 0.9238795325112867385, 1.000000000000000000, 0.9238795325112867385, 1.000000000000000000, 0.9238795325112867385, 1.000000000000000000, 0.9238795325112867385, 1.000000000000000000, 0.9238795325112867385, 1.000000000000000000, 0.9238795325112867385, 1.000000000000000000, 0.9238795325112867385, 1.000000000000000000, 0.9238795325112867385, 1.000000000000000000, 0.9238795325112867385, 1.000000000000000000, 0.9238795325112867385, 1.000000000000000000, 0.9238795325112867385, 1.000000000000000000, 0.9238795325112867385, 1.000000000000000000, 0.9238795325112867385, 1.000000000000000000, 0.9238795325112867385, 1.000000000000000000, 0.9238795325112867385, 1.000000000000000000, 0.9238795325112867385, 1.000000000000000000, 0.9238795325112867385, 1.000000000000000000, 0.9744806372091472380, 0.9660719911213342392),
 ( 1.000000000000000000, 0.9238795325112867385, 1.000000000000000000, 0.9238795325112867385, 1.000000000000000000, 0.9238795325112867385, 1.000000000000000000, 0.9238795325112867385, 1.000000000000000000, 0.9238795325112867385, 1.000000000000000000, 0.9238795325112867385, 1.000000000000000000, 0.9238795325112867385, 1.000000000000000000, 0.9238795325112867385, 1.000000000000000000, 0.9238795325112867385, 1.000000000000000000, 0.9238795325112867385, 1.000000000000000000, 0.9238795325112867385, 1.000000000000000000, 0.9238795325112867385, 1.000000000000000000, 0.9238795325112867385, 1.000000000000000000, 0.9238795325112867385, 1.000000000000000000, 0.9238795325112867385, 1.000000000000000000, 0.9238795325112867385, 1.000000000000000000, 0.9238795325112867385, 1.000000000000000000, 0.9238795325112867385, 1.000000000000000000, 0.9238795325112867385, 1.000000000000000000, 0.9238795325112867385, 1.000000000000000000, 0.9238795325112867385, 1.000000000000000000, 0.9238795325112867385, 1.000000000000000000, 0.9238795325112867385, 1.000000000000000000, 0.9238795325112867385, 1.000000000000000000, 0.9238795325112867385, 1.000000000000000000, 0.9238795325112867385, 1.000000000000000000, 0.9238795325112867385, 1.000000000000000000, 0.9238795325112867385, 1.000000000000000000, 0.9238795325112867385, 1.000000000000000000, 0.9238795325112867385, 1.000000000000000000, 0.9238795325112867385, 1.000000000000000000, 0.9238795325112867385, 1.000000000000000000, 0.9238795325112867385, 1.000000000000000000, 0.9238795325112867385, 1.000000000000000000, 0.9238795325112867385, 1.000000000000000000, 0.9238795325112867385, 1.000000000000000000, 0.9238795325112867385, 1.000000000000000000, 0.9238795325112867385, 1.000000000000000000, 0.9238795325112867385, 1.000000000000000000, 0.9238795325112867385, 1.000000000000000000, 0.9238795325112867385, 1.000000000000000000, 0.9238795325112867385, 1.000000000000000000, 0.9238795325112867385, 1.000000000000000000, 0.9238795325112867385, 1.000000000000000000, 0.9238795325112867385, 1.000000000000000000, 0.9238795325112867385, 1.000000000000000000, 0.9238795325112867385, 1.000000000000000000, 0.9238795325112867385, 1.000000000000000000, 0.9238795325112867385, 1.000000000000000000, 0.9238795325112867385, 1.000000000000000000, 0.9238795325112867385, 1.000000000000000000, 0.9238795325112867385, 1.000000000000000000, 0.9238795325112867385, 1.000000000000000000, 0.9238795325112867385, 1.000000000000000000, 0.9238795325112867385, 1.000000000000000000, 0.9238795325112867385, 1.000000000000000000, 0.9238795325112867385, 1.000000000000000000, 0.9238795325112867385, 1.000000000000000000, 0.9238795325112867385, 1.000000000000000000, 0.9238795325112867385, 1.000000000000000000, 0.9238795325112867385, 1.000000000000000000, 0.9238795325112867385, 1.000000000000000000, 0.9238795325112867385, 1.000000000000000000, 0.9238795325112867385, 1.000000000000000000, 0.9238795325112867385, 1.000000000000000000, 0.9238795325112867385, 1.000000000000000000, 0.9238795325112867385, 1.000000000000000000, 0.9238795325112867385, 1.000000000000000000, 0.9238795325112867385, 1.000000000000000000, 0.9238795325112867385, 1.000000000000000000, 0.9238795325112867385, 1.000000000000000000, 0.9238795325112867385, 1.000000000000000000, 0.9238795325112867385, 1.000000000000000000, 0.9238795325112867385, 1.000000000000000000, 0.9238795325112867385, 1.000000000000000000, 0.9238795325112867385, 1.000000000000000000, 0.9238795325112867385, 1.000000000000000000, 0.9238795325112867385, 1.000000000000000000, 0.9238795325112867385, 1.000000000000000000, 0.9238795325112867385, 1.000000000000000000, 0.9238795325112867385, 1.000000000000000000, 0.9238795325112867385, 1.000000000000000000, 0.9238795325112867385, 1.000000000000000000, 0.9238795325112867385, 1.000000000000000000, 0.9238795325112867385, 1.000000000000000000, 0.9238795325112867385, 1.000000000000000000, 0.9238795325112867385, 1.000000000000000000, 0.9238795325112867385, 1.000000000000000000, 0.9238795325112867385, 1.000000000000000000, 0.9238795325112867385, 1.000000000000000000, 0.9238795325112867385, 1.000000000000000000, 0.9238795325112867385, 1.000000000000000000, 0.9238795325112867385, 1.000000000000000000, 0.9238795325112867385, 1.000000000000000000, 0.9238795325112867385, 1.000000000000000000, 0.9238795325112867385, 1.000000000000000000, 0.9238795325112867385, 1.000000000000000000, 0.9238795325112867385, 1.000000000000000000, 0.9238795325112867385, 1.000000000000000000, 0.9238795325112867385, 1.000000000000000000, 0.9238795325112867385, 1.000000000000000000, 0.9238795325112867385, 1.000000000000000000, 0.9238795325112867385, 1.000000000000000000, 0.9238795325112867385, 1.000000000000000000, 0.9238795325112867385, 1.000000000000000000, 0.9238795325112867385, 1.000000000000000000, 0.9238795325112867385, 1.000000000000000000, 0.9238795325112867385, 1.000000000000000000, 0.9238795325112867385, 1.000000000000000000, 0.9238795325112867385, 1.000000000000000000, 0.9238795325112867385, 1.000000000000000000, 0.9238795325112867385, 1.000000000000000000, 0.9238795325112867385, 1.000000000000000000, 0.9238795325112867385, 1.000000000000000000, 0.9238795325112867385, 1.000000000000000000, 0.9238795325112867385, 1.000000000000000000, 0.9238795325112867385, 1.000000000000000000, 0.9238795325112867385, 1.000000000000000000, 0.9238795325112867385, 1.000000000000000000, 0.9238795325112867385, 1.000000000000000000, 0.9238795325112867385, 1.000000000000000000, 0.9238795325112867385, 1.000000000000000000, 0.9238795325112867385, 1.000000000000000000, 0.9238795325112867385, 1.000000000000000000, 0.9238795325112867385, 1.000000000000000000, 0.9238795325112867385, 1.000000000000000000, 0.9238795325112867385, 1.000000000000000000, 0.9238795325112867385, 1.000000000000000000, 0.9238795325112867385, 1.000000000000000000, 0.9238795325112867385, 1.000000000000000000, 0.9238795325112867385, 1.000000000000000000, 0.9238795325112867385, 1.000000000000000000, 0.9238795325112867385, 1.000000000000000000, 0.9744806372091472380, 0.9660719911213342392) ) ) 
 REPRESENTATION_ITEM ( '' )  SURFACE ( )  );
#86444=CARTESIAN_POINT ( 'NONE',  ( 9.221249107921748234, 103.9517862850151602, 3.869340886054262629 ) ) ;
#86454=DIRECTION ( 'NONE',  ( 0.000000000000000000, 1.000000000000000000, 0.000000000000000000 ) ) ;
#86479=CARTESIAN_POINT ( 'NONE',  ( 2.977408999572650927, -25.25000000204839168, -7.188101187500000933 ) ) ;
#86488=CARTESIAN_POINT ( 'NONE',  ( 4.401442555609581635E-16, -34.15625000204838813, -7.188101187500000044 ) ) ;
#86508=CARTESIAN_POINT ( 'NONE',  ( 8.000000000000000000, -23.18750000409677270, 0.000000000000000000 ) ) ;
#86528=CARTESIAN_POINT ( 'NONE',  ( -7.188101187500001821, -32.37500000204838813, -2.977408999572651371 ) ) ;
#86542=CARTESIAN_POINT ( 'NONE',  ( -1.320432766682874540E-15, -21.03125000204838457, 7.188101187500000044 ) ) ;
#86552=CARTESIAN_POINT ( 'NONE',  ( 7.999999999999998224, -18.78125000409677625, 3.313708498984766493 ) ) ;
#86554=CARTESIAN_POINT ( 'NONE',  ( 9.571198553003723575, 15.30040232763830943, 2.918503601030441708 ) ) ;
#86559=CARTESIAN_POINT ( 'NONE',  ( 6.947681302647271906, -29.99999999999999645, -2.194325991354435068 ) ) ;
#86600=ORIENTED_EDGE ( 'NONE', *, *, #92248, .T. ) ;
#86611=CARTESIAN_POINT ( 'NONE',  ( -5.082755093536325042, -26.09375000204838813, -5.082755093536325930 ) ) ;
#86634=DIRECTION ( 'NONE',  ( -0.000000000000000000, 1.000000000000000000, -0.000000000000000000 ) ) ;
#86677=CARTESIAN_POINT ( 'NONE',  ( 3.313708498984762052, -33.40625000409677625, -8.000000000000000000 ) ) ;
#86702=ORIENTED_EDGE ( 'NONE', *, *, #26509, .T. ) ;
#86729=ORIENTED_EDGE ( 'NONE', *, *, #60456, .F. ) ;
#86760=( BOUNDED_CURVE ( )  B_SPLINE_CURVE ( 2, ( #78192, #79251, #38808, #22105, #54960, #96514, #22647, #55482, #70103 ),
 .UNSPECIFIED., .F., .F. ) 
 B_SPLINE_CURVE_WITH_KNOTS ( ( 3, 2, 2, 2, 3 ),
 ( 0.2205882352941176683, 0.2279411764705882582, 0.2352941176470588758, 0.2426470588235294656, 0.2500000000000000555 ),
 .UNSPECIFIED. ) 
 CURVE ( )  GEOMETRIC_REPRESENTATION_ITEM ( )  RATIONAL_B_SPLINE_CURVE ( ( 0.9999999999999996669, 0.9238795325112870716, 1.000000000000000000, 0.9238795325112867385, 1.000000000000000000, 0.9238795325112867385, 1.000000000000000000, 0.9238795325112861834, 1.000000000000000666 ) ) 
 REPRESENTATION_ITEM ( '' )  );
#86792=CARTESIAN_POINT ( 'NONE',  ( 7.999999999999998224, -21.59374999999999289, 3.313708498984766493 ) ) ;
#86817=( NAMED_UNIT ( * ) PLANE_ANGLE_UNIT ( ) SI_UNIT ( $, .RADIAN. ) );
#86857=CARTESIAN_POINT ( 'NONE',  ( -9.999952458099485852, 101.0001188547613395, 0.2653554233229110104 ) ) ;
#86859=CARTESIAN_POINT ( 'NONE',  ( 3.082707893549470057, 15.00000000000000178, -9.999999999999998224 ) ) ;
#86874=CARTESIAN_POINT ( 'NONE',  ( -7.188101187500001821, -12.87500000204838813, -2.977408999572651371 ) ) ;
#86910=CARTESIAN_POINT ( 'NONE',  ( -7.045755811259133417, 28.69658396986446647, 3.790843699961854441 ) ) ;
#86917=CARTESIAN_POINT ( 'NONE',  ( -7.188101187500001821, -14.37500000204838635, -2.977408999572651371 ) ) ;
#86935=EDGE_CURVE ( 'NONE', #29277, #12516, #56777, .T. ) ;
#86940=DIRECTION ( 'NONE',  ( 1.000000000000000000, -0.000000000000000000, -0.000000000000000000 ) ) ;
#86942=DIRECTION ( 'NONE',  ( 0.000000000000000000, -0.000000000000000000, 1.000000000000000000 ) ) ;
#86945=CARTESIAN_POINT ( 'NONE',  ( -7.188101187500001821, -17.00000000204838457, -2.977408999572651371 ) ) ;
#86994=CARTESIAN_POINT ( 'NONE',  ( 4.401442555609581635E-16, -19.15625000204838457, -7.188101187500000044 ) ) ;
#87003=CARTESIAN_POINT ( 'NONE',  ( 5.082755093536324154, -31.71875000204838457, 5.082755093536326818 ) ) ;
#87047=CARTESIAN_POINT ( 'NONE',  ( 7.188101187500001821, -32.93750000204839523, -2.977408999572650483 ) ) ;
#87058=CARTESIAN_POINT ( 'NONE',  ( 7.188101187500000044, -19.15625000204838457, 0.000000000000000000 ) ) ;
#87067=CARTESIAN_POINT ( 'NONE',  ( -8.000000000000001776, -14.84375000409677092, 3.313708498984758943 ) ) ;
#87072=CARTESIAN_POINT ( 'NONE',  ( -9.483056940782029542, 87.44387790106578962, -3.177305548492604270 ) ) ;
#87075=CARTESIAN_POINT ( 'NONE',  ( -9.176855344542989457, 30.52960426977409725, -3.973472207155926750 ) ) ;
#87128=CARTESIAN_POINT ( 'NONE',  ( 2.977408999572650927, -24.87500000204838457, -7.188101187500001821 ) ) ;
#87131=CARTESIAN_POINT ( 'NONE',  ( 3.313708498984761608, -19.90625000409677270, -8.000000000000000000 ) ) ;
#87172=ORIENTED_EDGE ( 'NONE', *, *, #10896, .T. ) ;
#87215=CYLINDRICAL_SURFACE ( 'NONE', #8822, 8.000000000000000000 ) ;
#87302=CARTESIAN_POINT ( 'NONE',  ( 4.898587196589412829E-16, -19.81250000409677270, -8.000000000000000000 ) ) ;
#87305=ORIENTED_EDGE ( 'NONE', *, *, #103537, .T. ) ;
#87310=CARTESIAN_POINT ( 'NONE',  ( -1.469576158976823947E-15, -21.87499999999999289, 8.000000000000000000 ) ) ;
#87329=DIRECTION ( 'NONE',  ( 0.000000000000000000, 0.000000000000000000, 1.000000000000000000 ) ) ;
#87362=CARTESIAN_POINT ( 'NONE',  ( -1.469576158976823947E-15, -21.87499999999999289, 8.000000000000000000 ) ) ;
#87363=CARTESIAN_POINT ( 'NONE',  ( -9.381394091586571449, 27.98650394418389098, 3.465950112474260880 ) ) ;
#87385=CARTESIAN_POINT ( 'NONE',  ( -9.989690267985800176, 101.0255558340509197, -0.5238310916885776658 ) ) ;
#87436=CARTESIAN_POINT ( 'NONE',  ( 7.801642220026313801, 33.58796826149033166, 1.787233835843581087 ) ) ;
#87437=CARTESIAN_POINT ( 'NONE',  ( -6.928203230275510549, 29.99999999999999645, -4.000000000000000000 ) ) ;
#87444=CARTESIAN_POINT ( 'NONE',  ( 5.082755093536325930, -16.34375000204838813, -5.082755093536325042 ) ) ;
#87469=CARTESIAN_POINT ( 'NONE',  ( -2.977408999572650039, -21.68750000204838813, -7.188101187500001821 ) ) ;
#87482=VECTOR ( 'NONE', #52974, 1000.000000000000000 ) ;
#87485=ORIENTED_EDGE ( 'NONE', *, *, #101340, .F. ) ;
#87517=CARTESIAN_POINT ( 'NONE',  ( -5.082755093536325042, -18.96875000204838457, -5.082755093536325930 ) ) ;
#87526=CARTESIAN_POINT ( 'NONE',  ( 7.188101187500000044, -33.03125000204838813, 0.000000000000000000 ) ) ;
#87542=ORIENTED_EDGE ( 'NONE', *, *, #45808, .T. ) ;
#87567=CARTESIAN_POINT ( 'NONE',  ( -7.188101187500000044, -29.28125000204838813, -8.802885111219163269E-16 ) ) ;
#87580=CARTESIAN_POINT ( 'NONE',  ( -5.082755093536326818, -18.21875000204838457, 5.082755093536325042 ) ) ;
#87582=CYLINDRICAL_SURFACE ( 'NONE', #60708, 4.000000000000000000 ) ;
#87592=CARTESIAN_POINT ( 'NONE',  ( 3.313708498984762496, -14.46875000409676915, 7.999999999999998224 ) ) ;
#87594=( LENGTH_UNIT ( ) NAMED_UNIT ( * ) SI_UNIT ( .MILLI., .METRE. ) );
#87634=VERTEX_POINT ( 'NONE', #36324 ) ;
#87657=CARTESIAN_POINT ( 'NONE',  ( -5.082755093536326818, -27.21875000204838813, 5.082755093536325042 ) ) ;
#87660=DIRECTION ( 'NONE',  ( 1.734723475976807094E-16, 0.000000000000000000, 1.000000000000000000 ) ) ;
#87695=CARTESIAN_POINT ( 'NONE',  ( 4.898587196589412829E-16, -16.81250000409677270, -8.000000000000000000 ) ) ;
#87723=CARTESIAN_POINT ( 'NONE',  ( -5.656854249492379694, -27.12500000409677270, -5.656854249492380582 ) ) ;
#87736=CARTESIAN_POINT ( 'NONE',  ( -5.656854249492381470, -10.06249999999999112, 5.656854249492379694 ) ) ;
#87778=CARTESIAN_POINT ( 'NONE',  ( 5.656854249492380582, -14.00000000409677092, -5.656854249492379694 ) ) ;
#87786=CARTESIAN_POINT ( 'NONE',  ( -10.00000000000000355, 30.00000000000000000, 0.000000000000000000 ) ) ;
#87829=CARTESIAN_POINT ( 'NONE',  ( -1.469576158976823947E-15, -25.06250000409677270, 8.000000000000000000 ) ) ;
#87842=CARTESIAN_POINT ( 'NONE',  ( -5.656854249492379694, -14.93749999999999289, -5.656854249492380582 ) ) ;
#87893=FACE_OUTER_BOUND ( 'NONE', #38303, .T. ) ;
#87900=EDGE_CURVE ( 'NONE', #3711, #70143, #30870, .T. ) ;
#87905=( NAMED_UNIT ( * ) PLANE_ANGLE_UNIT ( ) SI_UNIT ( $, .RADIAN. ) );
#87926=CARTESIAN_POINT ( 'NONE',  ( -10.00000000000000355, 30.00000000000000000, -4.000000000000000000 ) ) ;
#87933=UNCERTAINTY_MEASURE_WITH_UNIT (LENGTH_MEASURE( 1.000000000000000082E-05 ), #29028, 'distance_accuracy_value', 'NONE');
#87962=CARTESIAN_POINT ( 'NONE',  ( 7.619135598915494967, 33.17305367784678083, 2.449260492474801154 ) ) ;
#87963=CARTESIAN_POINT ( 'NONE',  ( -7.002990960197232440, 28.94733181616541984, 3.868040364119522678 ) ) ;
#87971=CARTESIAN_POINT ( 'NONE',  ( 5.656854249492380582, -30.31249999999999645, -5.656854249492379694 ) ) ;
#87996=CARTESIAN_POINT ( 'NONE',  ( 5.082755093536324154, -22.34375000204838457, 5.082755093536326818 ) ) ;
#88046=CARTESIAN_POINT ( 'NONE',  ( -7.188101187500000044, -21.78125000204838457, -8.802885111219163269E-16 ) ) ;
#88055=CARTESIAN_POINT ( 'NONE',  ( -2.977408999572654480, -24.50000000204839168, 7.188101187499999156 ) ) ;
#88078=CARTESIAN_POINT ( 'NONE',  ( 8.000000000000000000, -23.09375000409677270, -3.313708498984761164 ) ) ;
#88094=CARTESIAN_POINT ( 'NONE',  ( 0.000000000000000000, -30.00000000000000000, 0.000000000000000000 ) ) ;
#88096=CARTESIAN_POINT ( 'NONE',  ( 2.977408999572650927, -31.25000000204838813, -7.188101187500001821 ) ) ;
#88109=CARTESIAN_POINT ( 'NONE',  ( 7.188101187500000933, -14.56250000204838457, -2.977408999572650483 ) ) ;
#88123=CARTESIAN_POINT ( 'NONE',  ( -3.313708498984760720, -9.218750004096769146, -8.000000000000000000 ) ) ;
#88125=CARTESIAN_POINT ( 'NONE',  ( 9.999999999999957367, 15.00000000000001066, 3.836411046841756711 ) ) ;
#88129=PRESENTATION_STYLE_ASSIGNMENT (( #63859 ) ) ;
#88130=CARTESIAN_POINT ( 'NONE',  ( -9.537909130738274399, 32.64614830963394354, -3.010726932293863012 ) ) ;
#88169=ORIENTED_EDGE ( 'NONE', *, *, #72475, .T. ) ;
#88182=CARTESIAN_POINT ( 'NONE',  ( 4.401442555609581635E-16, -18.78125000204838457, -7.188101187500000044 ) ) ;
#88247=EDGE_CURVE ( 'NONE', #25439, #24651, #940, .T. ) ;
#88249=CARTESIAN_POINT ( 'NONE',  ( -1.469576158976823947E-15, -32.56250000409677625, 8.000000000000000000 ) ) ;
#88252=EDGE_CURVE ( 'NONE', #81173, #50100, #93197, .T. ) ;
#88257=CARTESIAN_POINT ( 'NONE',  ( -4.582575694955839829, 15.00000000000000000, -9.999999999999998224 ) ) ;
#88296=CARTESIAN_POINT ( 'NONE',  ( -7.853841075665486393, -30.00000000000001066, -1.477988678308346016 ) ) ;
#88351=ORIENTED_EDGE ( 'NONE', *, *, #75629, .F. ) ;
#88376=CARTESIAN_POINT ( 'NONE',  ( 8.000000000000000000, -16.90624999999999645, -3.313708498984761608 ) ) ;
#88401=EDGE_CURVE ( 'NONE', #102469, #53546, #96815, .T. ) ;
#88414=ORIENTED_EDGE ( 'NONE', *, *, #12229, .T. ) ;
#88491=CARTESIAN_POINT ( 'NONE',  ( 7.744168461338430731, 33.46254061715157491, 2.019395720771558267 ) ) ;
#88492=CARTESIAN_POINT ( 'NONE',  ( -7.551560007654700257, 26.99089648193007562, -2.648022159607827497 ) ) ;
#88499=CARTESIAN_POINT ( 'NONE',  ( 3.313708498984762052, -31.71874999999999645, -8.000000000000000000 ) ) ;
#88524=CARTESIAN_POINT ( 'NONE',  ( 7.188101187500001821, -22.06250000204838813, -2.977408999572650483 ) ) ;
#88535=VERTEX_POINT ( 'NONE', #3427 ) ;
#88569=CARTESIAN_POINT ( 'NONE',  ( 2.977408999572652260, -19.81250000204838457, 7.188101187500000044 ) ) ;
#88572=CARTESIAN_POINT ( 'NONE',  ( -5.656854249492379694, -27.12500000409677270, -5.656854249492380582 ) ) ;
#88574=DIRECTION ( 'NONE',  ( 0.000000000000000000, 0.000000000000000000, 1.000000000000000000 ) ) ;
#88578=CARTESIAN_POINT ( 'NONE',  ( 7.188101187500000044, -24.03125000204838457, 0.000000000000000000 ) ) ;
#88617=CARTESIAN_POINT ( 'NONE',  ( 4.401442555609581635E-16, -25.15625000204838813, -7.188101187500000044 ) ) ;
#88631=CARTESIAN_POINT ( 'NONE',  ( 5.082755093536324154, -11.84375000204838635, 5.082755093536326818 ) ) ;
#88633=( BOUNDED_SURFACE ( )  B_SPLINE_SURFACE ( 3, 2, ( 
 ( #99560, #25740, #65615 ),
 ( #58595, #64560, #49418 ),
 ( #91500, #56435, #72633 ),
 ( #17610, #97427, #23588 ),
 ( #89368, #84994, #27336 ),
 ( #11616, #44545, #51002 ),
 ( #93081, #18691, #11077 ),
 ( #77434, #61260, #9482 ),
 ( #35411, #83921, #43472 ),
 ( #1926, #19777, #100100 ) ),
 .UNSPECIFIED., .F., .F., .F. ) 
 B_SPLINE_SURFACE_WITH_KNOTS ( ( 4, 2, 2, 2, 4 ),
 ( 3, 3 ),
 ( 0.002450517525418897339, 0.003060732775749464701, 0.003670948026080031630, 0.004891378526741165488, 0.007332239528063434070 ),
 ( 0.000000000000000000, 1.000000000000000000 ),
 .UNSPECIFIED. ) 
 GEOMETRIC_REPRESENTATION_ITEM ( )  RATIONAL_B_SPLINE_SURFACE ( (
 ( 1.000000000000000000, 0.7071067811865481278, 1.000000000000000000),
 ( 1.000000000000000000, 0.7344063550101938009, 1.000000000000000000),
 ( 1.000000000000000000, 0.7590375248711013212, 1.000000000000000000),
 ( 1.000000000000000000, 0.8038331608704091247, 1.000000000000000000),
 ( 1.000000000000000000, 0.8240352460866575690, 1.000000000000000000),
 ( 1.000000000000000000, 0.8791017378331893450, 1.000000000000000000),
 ( 1.000000000000000000, 0.9085032776980893621, 1.000000000000000000),
 ( 1.000000000000000000, 0.9784170511696810291, 1.000000000000000000),
 ( 1.000000000000000000, 0.9996598051696602427, 1.000000000000000000),
 ( 1.000000000000000000, 1.000000000000000000, 1.000000000000000000) ) ) 
 REPRESENTATION_ITEM ( '' )  SURFACE ( )  );
#88642=CARTESIAN_POINT ( 'NONE',  ( -8.000000000000000000, -10.43750000409677092, -9.797174393178825657E-16 ) ) ;
#88644=CARTESIAN_POINT ( 'NONE',  ( 10.00000000000002132, 14.99999999999997335, 2.701558353794770273 ) ) ;
#88648=DIRECTION ( 'NONE',  ( 0.000000000000000000, 1.000000000000000000, 0.000000000000000000 ) ) ;
#88650=CARTESIAN_POINT ( 'NONE',  ( -10.00005432054556742, 34.00013580137913749, 0.2621623937322678510 ) ) ;
#88653=CARTESIAN_POINT ( 'NONE',  ( -3.487646406148226852, 15.95332971149351842, 9.373884331925033564 ) ) ;
#88661=ORIENTED_EDGE ( 'NONE', *, *, #81115, .F. ) ;
#88665=EDGE_CURVE ( 'NONE', #13028, #63010, #52232, .T. ) ;
#88693=ORIENTED_EDGE ( 'NONE', *, *, #88252, .T. ) ;
#88709=CARTESIAN_POINT ( 'NONE',  ( 5.082755093536324154, -17.84375000204838457, 5.082755093536326818 ) ) ;
#88712=CARTESIAN_POINT ( 'NONE',  ( 9.999945253488242258, 81.00013686629468168, -0.2662901834230905207 ) ) ;
#88772=CARTESIAN_POINT ( 'NONE',  ( 4.898587196589412829E-16, -31.81250000409677270, -8.000000000000000000 ) ) ;
#88797=FILL_AREA_STYLE ('',( #55859 ) ) ;
#88836=LINE ( 'NONE', #96414, #37462 ) ;
#88848=PRESENTATION_STYLE_ASSIGNMENT (( #106611 ) ) ;
#88853=DIRECTION ( 'NONE',  ( -0.000000000000000000, 1.000000000000000000, -0.000000000000000000 ) ) ;
#88856=ORIENTED_EDGE ( 'NONE', *, *, #31916, .F. ) ;
#88895=CARTESIAN_POINT ( 'NONE',  ( -3.313708498984765161, -17.46874999999999645, 7.999999999999998224 ) ) ;
#88898=ORIENTED_EDGE ( 'NONE', *, *, #29499, .F. ) ;
#88933=( BOUNDED_CURVE ( )  B_SPLINE_CURVE ( 2, ( #8928, #802, #97399, #81739, #83354, #98990, #25707, #56405, #7329 ),
 .UNSPECIFIED., .F., .F. ) 
 B_SPLINE_CURVE_WITH_KNOTS ( ( 3, 2, 2, 2, 3 ),
 ( 0.8676470588235294379, 0.8750000000000000000, 0.8823529411764705621, 0.8897058823529412352, 0.8970588235294119084 ),
 .UNSPECIFIED. ) 
 CURVE ( )  GEOMETRIC_REPRESENTATION_ITEM ( )  RATIONAL_B_SPLINE_CURVE ( ( 1.000000000000000000, 0.9238795325112867385, 1.000000000000000000, 0.9238795325112867385, 1.000000000000000000, 0.9238795325112867385, 1.000000000000000000, 0.9238795325112856283, 1.000000000000001110 ) ) 
 REPRESENTATION_ITEM ( '' )  );
#88973=MECHANICAL_DESIGN_GEOMETRIC_PRESENTATION_REPRESENTATION('',(#106190),#51074);
#88980=CARTESIAN_POINT ( 'NONE',  ( 5.082755093536324154, -10.71875000204838457, 5.082755093536326818 ) ) ;
#88988=CARTESIAN_POINT ( 'NONE',  ( 3.313708498984781592, -24.78124999999998934, 7.999999999999979572 ) ) ;
#89014=VERTEX_POINT ( 'NONE', #52386 ) ;
#89018=CARTESIAN_POINT ( 'NONE',  ( -7.897196874019792645, 26.20872795832194058, -1.302055520192085591 ) ) ;
#89025=CARTESIAN_POINT ( 'NONE',  ( -7.188101187500001821, -9.875000002048386349, -2.977408999572651371 ) ) ;
#89047=CARTESIAN_POINT ( 'NONE',  ( 7.188101187500001821, -19.06250000204838813, -2.977408999572650483 ) ) ;
#89101=CARTESIAN_POINT ( 'NONE',  ( 7.188101187499999156, -12.12500000204838635, 2.977408999572654924 ) ) ;
#89107=CYLINDRICAL_SURFACE ( 'NONE', #80305, 8.000000000000000000 ) ;
#89111=CARTESIAN_POINT ( 'NONE',  ( 7.188101187500001821, -23.93750000204838457, -2.977408999572650483 ) ) ;
#89151=CARTESIAN_POINT ( 'NONE',  ( 5.082755093536324154, -25.71875000204838813, 5.082755093536326818 ) ) ;
#89164=CARTESIAN_POINT ( 'NONE',  ( 5.082755093536324154, -14.84375000204838457, 5.082755093536326818 ) ) ;
#89165=CARTESIAN_POINT ( 'NONE',  ( 7.896165657598944065, 26.21088868628027413, -1.307894402814546941 ) ) ;
#89173=DIRECTION ( 'NONE',  ( 0.000000000000000000, 1.000000000000000000, 0.000000000000000000 ) ) ;
#89179=CARTESIAN_POINT ( 'NONE',  ( 4.898587196589412829E-16, -12.31250000409676915, -8.000000000000000000 ) ) ;
#89181=CARTESIAN_POINT ( 'NONE',  ( 9.999999999999998224, 15.23416508903475375, 0.7060372491634900882 ) ) ;
#89183=CARTESIAN_POINT ( 'NONE',  ( -8.000000000000000000, -16.24999999999999289, -9.797174393178825657E-16 ) ) ;
#89186=CARTESIAN_POINT ( 'NONE',  ( -9.380894568449075877, 32.01130633110942370, -3.467341429141165499 ) ) ;
#89189=CARTESIAN_POINT ( 'NONE',  ( 0.000000000000000000, 15.00000000000000000, 9.999999999999998224 ) ) ;
#89191=EDGE_CURVE ( 'NONE', #58245, #82728, #12395, .T. ) ;
#89198=CARTESIAN_POINT ( 'NONE',  ( 3.313708498984762496, -9.968750004096769146, 7.999999999999998224 ) ) ;
#89239=ORIENTED_EDGE ( 'NONE', *, *, #83718, .F. ) ;
#89243=CARTESIAN_POINT ( 'NONE',  ( -2.977408999572654480, -16.62500000204838457, 7.188101187499999156 ) ) ;
#89271=( BOUNDED_SURFACE ( )  B_SPLINE_SURFACE ( 1, 2, ( 
 ( #10993, #91413, #20758, #95655, #96192, #53595, #21792, #103215, #79457, #4513, #12064, #61720, #12590, #36919, #102681, #37453, #104259, #87047, #30405, #21269, #38497, #36402, #44994, #86528, #20221, #78927, #70320, #29360, #71359, #53071, #94611, #62250, #29882, #28296, #5569, #88096, #77880, #45524, #70846, #13652, #95135, #62762, #46563, #63294, #78397, #13116, #22322, #55167, #54104, #37985, #46043, #14175, #5051, #103739, #54628, #85992, #87567, #77346, #3457, #69270, #102143, #61171, #94057, #3992, #69787, #28843, #23375, #7152, #82100, #56213, #90208, #16308, #49200, #56758, #72428, #39015, #63825, #8220, #89685, #40065, #30948, #64867, #15783, #97750, #105848, #32533, #47080, #48139, #39552, #22851, #41129, #55686, #33063, #74012, #89151, #15252, #48666, #24453, #40591, #106370, #88617, #31992, #64359, #47609, #98812, #14708, #81036, #23917, #94, #24966, #65933, #73472, #81551, #72942, #7672, #57287, #65403, #98295, #57821, #71896, #90744, #79979, #6095, #104798, #96714, #105332, #80505, #6625, #31476, #97226, #43255, #84244, #2239, #50784, #83696, #91811, #33582, #26060, #1160, #42180, #49740, #58916, #76139, #34134, #91289, #92855, #59452, #101494, #42720, #68609, #84776, #17931, #75068, #68054, #82649, #9801, #67007, #66461, #51326, #43780, #67539, #10861, #8749, #17398, #75613, #99337, #18469, #1713, #34666, #76669, #25514, #99889, #50273, #100419, #60523, #2782, #59999, #10340, #26584, #27646, #35189, #92320, #100951, #83176, #19023, #58369, #35731, #16862, #27108, #51862, #41656, #74543, #9274, #619, #87444, #21147, #61584, #103091, #103609, #20092, #21662, #70185, #4924, #29241, #13522, #3863, #102011, #78791, #95011, #79330, #4383, #62122, #29759, #62634, #53979, #86917, #19559, #37857, #93409, #37324, #36795, #61047, #52394, #85307, #94477, #77751, #93934, #46441, #28172, #71236, #52936, #45391, #11394, #85863, #45914, #11935, #44863, #69661, #102552, #104131, #12987, #70718, #95522, #28703, #54500, #20634, #5450, #53474, #38372, #30274, #44319, #77215, #3325, #86394, #36272, #69139, #12461, #78271, #97104, #80381, #48008, #63705, #5963, #89025, #79855, #15122, #23787, #38888, #56634 ),
 ( #96059, #8091, #80917, #106241, #65273, #6493, #72815, #57165, #98164, #7027, #64745, #56083, #39944, #90077, #71757, #47483, #96590, #64232, #106780, #16184, #32401, #89555, #105206, #73885, #97621, #105722, #72300, #30818, #24318, #104666, #49070, #40997, #31865, #23245, #15651, #88499, #55563, #22725, #81965, #48542, #31352, #81433, #73343, #14577, #63163, #7547, #40463, #22189, #55039, #39424, #87971, #14050, #46955, #18889, #50649, #75482, #43126, #76011, #9669, #26450, #65805, #51194, #32931, #83567, #50143, #488, #98682, #24836, #1024, #17270, #33457, #26975, #74411, #10735, #41524, #91683, #57690, #66332, #92188, #99215, #25379, #83051, #58236, #43650, #42582, #100288, #10213, #91165, #84114, #9143, #100814, #42054, #51734, #1575, #18339, #90613, #16722, #74938, #84651, #34538, #34004, #67412, #66874, #99760, #17799, #25931, #82518, #58788, #49611, #59317, #2110, #8621, #35061, #67929, #59859, #92730, #76539, #21534, #52804, #53863, #28567, #101886, #3739, #77082, #60918, #44734, #69011, #28046, #69534, #29633, #12338, #62508, #53344, #70593, #68474, #3199, #11802, #52264, #19961, #36142, #87310, #86264, #70054, #86792, #93804, #12863, #85730, #103485, #77622, #54367, #78141, #61992, #101365, #27518, #36669, #13393, #45264, #102426, #37191, #61451, #94346, #20508, #4263, #85178, #102960, #19434, #29123, #94884, #11263, #21024, #45782, #78656, #4794, #37734, #46314, #95394, #2650, #35597, #60395, #93272, #44194, #30690, #14450, #38766, #104535, #39299, #106114, #88895, #32266, #23122, #40337, #38251, #46835, #88376, #22058, #80790, #72179, #105085, #73217, #54916, #63578, #5840, #80251, #16058, #65143, #15524, #72700, #47364, #89951, #6902, #96987, #6358, #79736, #81308, #87842, #98041, #57037, #55964, #31226, #14988, #96468, #71631, #13925, #24191, #39824, #64110, #47882, #89434, #22606, #7422, #105598, #97492, #31740, #79206, #55441, #64626, #23650, #56504, #5328, #48417, #71114, #104002, #30149, #63033, #95931, #81835, #67287, #48940, #99631, #66203, #16594, #7959, #40866, #17143, #33336, #49483, #43005, #90487, #26861, #57560, #896, #73758, #82388, #1452, #8496, #41398, #366, #99088, #100167 ) ),
 .UNSPECIFIED., .F., .F., .F. ) 
 B_SPLINE_SURFACE_WITH_KNOTS ( ( 2, 2 ),
 ( 3, 2, 2, 2, 2, 2, 2, 2, 2, 2, 2, 2, 2, 2, 2, 2, 2, 2, 2, 2, 2, 2, 2, 2, 2, 2, 2, 2, 2, 2, 2, 2, 2, 2, 2, 2, 2, 2, 2, 2, 2, 2, 2, 2, 2, 2, 2, 2, 2, 2, 2, 2, 2, 2, 2, 2, 2, 2, 2, 2, 2, 2, 2, 2, 2, 2, 2, 2, 2, 2, 2, 2, 2, 2, 2, 2, 2, 2, 2, 2, 2, 2, 2, 2, 2, 2, 2, 2, 2, 2, 2, 2, 2, 2, 2, 2, 2, 2, 2, 2, 2, 2, 2, 2, 2, 2, 2, 2, 2, 2, 2, 2, 2, 2, 2, 2, 2, 2, 2, 2, 2, 2, 2, 2, 2, 2, 2, 2, 2, 2, 2, 2, 2, 2, 3 ),
 ( 0.000000000000000000, 1.000000000000000000 ),
 ( 0.000000000000000000, 0.007352941176470588133, 0.01470588235294117627, 0.02205882352941176613, 0.02941176470588235253, 0.03676470588235294240, 0.04411764705882353227, 0.05147058823529411520, 0.05882352941176470507, 0.06617647058823529493, 0.07352941176470588480, 0.08088235294117647467, 0.08823529411764706454, 0.09558823529411764053, 0.1029411764705882304, 0.1102941176470588203, 0.1176470588235294101, 0.1250000000000000000, 0.1323529411764705899, 0.1397058823529411797, 0.1470588235294117696, 0.1544117647058823595, 0.1617647058823529493, 0.1691176470588235392, 0.1764705882352941291, 0.1838235294117647189, 0.1911764705882352811, 0.1985294117647058709, 0.2058823529411764608, 0.2132352941176470507, 0.2205882352941176405, 0.2279411764705882304, 0.2352941176470588203, 0.2426470588235294101, 0.2500000000000000000, 0.2573529411764705621, 0.2647058823529411797, 0.2720588235294117418, 0.2794117647058823595, 0.2867647058823529216, 0.2941176470588235392, 0.3014705882352941013, 0.3088235294117647189, 0.3161764705882352811, 0.3235294117647058987, 0.3308823529411764608, 0.3382352941176470784, 0.3455882352941176405, 0.3529411764705882582, 0.3602941176470588203, 0.3676470588235294379, 0.3750000000000000000, 0.3823529411764705621, 0.3897058823529411797, 0.3970588235294117418, 0.4044117647058823595, 0.4117647058823529216, 0.4191176470588235392, 0.4264705882352941013, 0.4338235294117647189, 0.4411764705882352811, 0.4485294117647058987, 0.4558823529411764608, 0.4632352941176470784, 0.4705882352941176405, 0.4779411764705882582, 0.4852941176470588203, 0.4926470588235294379, 0.5000000000000000000, 0.5073529411764705621, 0.5147058823529411242, 0.5220588235294117974, 0.5294117647058823595, 0.5367647058823529216, 0.5441176470588234837, 0.5514705882352941568, 0.5588235294117647189, 0.5661764705882352811, 0.5735294117647058432, 0.5808823529411765163, 0.5882352941176470784, 0.5955882352941176405, 0.6029411764705882026, 0.6102941176470588758, 0.6176470588235294379, 0.6250000000000000000, 0.6323529411764705621, 0.6397058823529411242, 0.6470588235294117974, 0.6544117647058823595, 0.6617647058823529216, 0.6691176470588234837, 0.6764705882352941568, 0.6838235294117647189, 0.6911764705882352811, 0.6985294117647058432, 0.7058823529411765163, 0.7132352941176470784, 0.7205882352941176405, 0.7279411764705882026, 0.7352941176470588758, 0.7426470588235294379, 0.7500000000000000000, 0.7573529411764705621, 0.7647058823529411242, 0.7720588235294117974, 0.7794117647058823595, 0.7867647058823529216, 0.7941176470588234837, 0.8014705882352941568, 0.8088235294117647189, 0.8161764705882352811, 0.8235294117647058432, 0.8308823529411765163, 0.8382352941176470784, 0.8455882352941176405, 0.8529411764705882026, 0.8602941176470588758, 0.8676470588235294379, 0.8750000000000000000, 0.8823529411764705621, 0.8897058823529411242, 0.8970588235294117974, 0.9044117647058823595, 0.9117647058823529216, 0.9191176470588234837, 0.9264705882352941568, 0.9338235294117647189, 0.9411764705882352811, 0.9485294117647058432, 0.9558823529411765163, 0.9632352941176470784, 0.9705882352941176405, 0.9779411764705882026, 0.9804062476877506427 ),
 .UNSPECIFIED. ) 
 GEOMETRIC_REPRESENTATION_ITEM ( )  RATIONAL_B_SPLINE_SURFACE ( (
 ( 1.000000000000000000, 0.9238795325112867385, 1.000000000000000000, 0.9238795325112867385, 1.000000000000000000, 0.9238795325112867385, 1.000000000000000000, 0.9238795325112867385, 1.000000000000000000, 0.9238795325112867385, 1.000000000000000000, 0.9238795325112867385, 1.000000000000000000, 0.9238795325112867385, 1.000000000000000000, 0.9238795325112867385, 1.000000000000000000, 0.9238795325112867385, 1.000000000000000000, 0.9238795325112867385, 1.000000000000000000, 0.9238795325112867385, 1.000000000000000000, 0.9238795325112867385, 1.000000000000000000, 0.9238795325112867385, 1.000000000000000000, 0.9238795325112867385, 1.000000000000000000, 0.9238795325112867385, 1.000000000000000000, 0.9238795325112867385, 1.000000000000000000, 0.9238795325112867385, 1.000000000000000000, 0.9238795325112867385, 1.000000000000000000, 0.9238795325112867385, 1.000000000000000000, 0.9238795325112867385, 1.000000000000000000, 0.9238795325112867385, 1.000000000000000000, 0.9238795325112867385, 1.000000000000000000, 0.9238795325112867385, 1.000000000000000000, 0.9238795325112867385, 1.000000000000000000, 0.9238795325112867385, 1.000000000000000000, 0.9238795325112867385, 1.000000000000000000, 0.9238795325112867385, 1.000000000000000000, 0.9238795325112867385, 1.000000000000000000, 0.9238795325112867385, 1.000000000000000000, 0.9238795325112867385, 1.000000000000000000, 0.9238795325112867385, 1.000000000000000000, 0.9238795325112867385, 1.000000000000000000, 0.9238795325112867385, 1.000000000000000000, 0.9238795325112867385, 1.000000000000000000, 0.9238795325112867385, 1.000000000000000000, 0.9238795325112867385, 1.000000000000000000, 0.9238795325112867385, 1.000000000000000000, 0.9238795325112867385, 1.000000000000000000, 0.9238795325112867385, 1.000000000000000000, 0.9238795325112867385, 1.000000000000000000, 0.9238795325112867385, 1.000000000000000000, 0.9238795325112867385, 1.000000000000000000, 0.9238795325112867385, 1.000000000000000000, 0.9238795325112867385, 1.000000000000000000, 0.9238795325112867385, 1.000000000000000000, 0.9238795325112867385, 1.000000000000000000, 0.9238795325112867385, 1.000000000000000000, 0.9238795325112867385, 1.000000000000000000, 0.9238795325112867385, 1.000000000000000000, 0.9238795325112867385, 1.000000000000000000, 0.9238795325112867385, 1.000000000000000000, 0.9238795325112867385, 1.000000000000000000, 0.9238795325112867385, 1.000000000000000000, 0.9238795325112867385, 1.000000000000000000, 0.9238795325112867385, 1.000000000000000000, 0.9238795325112867385, 1.000000000000000000, 0.9238795325112867385, 1.000000000000000000, 0.9238795325112867385, 1.000000000000000000, 0.9238795325112867385, 1.000000000000000000, 0.9238795325112867385, 1.000000000000000000, 0.9238795325112867385, 1.000000000000000000, 0.9238795325112867385, 1.000000000000000000, 0.9238795325112867385, 1.000000000000000000, 0.9238795325112867385, 1.000000000000000000, 0.9238795325112867385, 1.000000000000000000, 0.9238795325112867385, 1.000000000000000000, 0.9238795325112867385, 1.000000000000000000, 0.9238795325112867385, 1.000000000000000000, 0.9238795325112867385, 1.000000000000000000, 0.9238795325112867385, 1.000000000000000000, 0.9238795325112867385, 1.000000000000000000, 0.9238795325112867385, 1.000000000000000000, 0.9238795325112867385, 1.000000000000000000, 0.9238795325112867385, 1.000000000000000000, 0.9238795325112867385, 1.000000000000000000, 0.9238795325112867385, 1.000000000000000000, 0.9238795325112867385, 1.000000000000000000, 0.9238795325112867385, 1.000000000000000000, 0.9238795325112867385, 1.000000000000000000, 0.9238795325112867385, 1.000000000000000000, 0.9238795325112867385, 1.000000000000000000, 0.9238795325112867385, 1.000000000000000000, 0.9238795325112867385, 1.000000000000000000, 0.9238795325112867385, 1.000000000000000000, 0.9238795325112867385, 1.000000000000000000, 0.9238795325112867385, 1.000000000000000000, 0.9238795325112867385, 1.000000000000000000, 0.9238795325112867385, 1.000000000000000000, 0.9238795325112867385, 1.000000000000000000, 0.9238795325112867385, 1.000000000000000000, 0.9238795325112867385, 1.000000000000000000, 0.9238795325112867385, 1.000000000000000000, 0.9238795325112867385, 1.000000000000000000, 0.9238795325112867385, 1.000000000000000000, 0.9238795325112867385, 1.000000000000000000, 0.9238795325112867385, 1.000000000000000000, 0.9238795325112867385, 1.000000000000000000, 0.9238795325112867385, 1.000000000000000000, 0.9238795325112867385, 1.000000000000000000, 0.9238795325112867385, 1.000000000000000000, 0.9238795325112867385, 1.000000000000000000, 0.9238795325112867385, 1.000000000000000000, 0.9238795325112867385, 1.000000000000000000, 0.9238795325112867385, 1.000000000000000000, 0.9238795325112867385, 1.000000000000000000, 0.9238795325112867385, 1.000000000000000000, 0.9238795325112867385, 1.000000000000000000, 0.9238795325112867385, 1.000000000000000000, 0.9238795325112867385, 1.000000000000000000, 0.9238795325112867385, 1.000000000000000000, 0.9238795325112867385, 1.000000000000000000, 0.9238795325112867385, 1.000000000000000000, 0.9238795325112867385, 1.000000000000000000, 0.9238795325112867385, 1.000000000000000000, 0.9238795325112867385, 1.000000000000000000, 0.9238795325112867385, 1.000000000000000000, 0.9238795325112867385, 1.000000000000000000, 0.9238795325112867385, 1.000000000000000000, 0.9238795325112867385, 1.000000000000000000, 0.9238795325112867385, 1.000000000000000000, 0.9238795325112867385, 1.000000000000000000, 0.9238795325112867385, 1.000000000000000000, 0.9238795325112867385, 1.000000000000000000, 0.9238795325112867385, 1.000000000000000000, 0.9238795325112867385, 1.000000000000000000, 0.9238795325112867385, 1.000000000000000000, 0.9238795325112867385, 1.000000000000000000, 0.9238795325112867385, 1.000000000000000000, 0.9238795325112867385, 1.000000000000000000, 0.9238795325112867385, 1.000000000000000000, 0.9238795325112867385, 1.000000000000000000, 0.9238795325112867385, 1.000000000000000000, 0.9238795325112867385, 1.000000000000000000, 0.9744806372117011950, 0.9660719911230173373),
 ( 1.000000000000000000, 0.9238795325112867385, 1.000000000000000000, 0.9238795325112867385, 1.000000000000000000, 0.9238795325112867385, 1.000000000000000000, 0.9238795325112867385, 1.000000000000000000, 0.9238795325112867385, 1.000000000000000000, 0.9238795325112867385, 1.000000000000000000, 0.9238795325112867385, 1.000000000000000000, 0.9238795325112867385, 1.000000000000000000, 0.9238795325112867385, 1.000000000000000000, 0.9238795325112867385, 1.000000000000000000, 0.9238795325112867385, 1.000000000000000000, 0.9238795325112867385, 1.000000000000000000, 0.9238795325112867385, 1.000000000000000000, 0.9238795325112867385, 1.000000000000000000, 0.9238795325112867385, 1.000000000000000000, 0.9238795325112867385, 1.000000000000000000, 0.9238795325112867385, 1.000000000000000000, 0.9238795325112867385, 1.000000000000000000, 0.9238795325112867385, 1.000000000000000000, 0.9238795325112867385, 1.000000000000000000, 0.9238795325112867385, 1.000000000000000000, 0.9238795325112867385, 1.000000000000000000, 0.9238795325112867385, 1.000000000000000000, 0.9238795325112867385, 1.000000000000000000, 0.9238795325112867385, 1.000000000000000000, 0.9238795325112867385, 1.000000000000000000, 0.9238795325112867385, 1.000000000000000000, 0.9238795325112867385, 1.000000000000000000, 0.9238795325112867385, 1.000000000000000000, 0.9238795325112867385, 1.000000000000000000, 0.9238795325112867385, 1.000000000000000000, 0.9238795325112867385, 1.000000000000000000, 0.9238795325112867385, 1.000000000000000000, 0.9238795325112867385, 1.000000000000000000, 0.9238795325112867385, 1.000000000000000000, 0.9238795325112867385, 1.000000000000000000, 0.9238795325112867385, 1.000000000000000000, 0.9238795325112867385, 1.000000000000000000, 0.9238795325112867385, 1.000000000000000000, 0.9238795325112867385, 1.000000000000000000, 0.9238795325112867385, 1.000000000000000000, 0.9238795325112867385, 1.000000000000000000, 0.9238795325112867385, 1.000000000000000000, 0.9238795325112867385, 1.000000000000000000, 0.9238795325112867385, 1.000000000000000000, 0.9238795325112867385, 1.000000000000000000, 0.9238795325112867385, 1.000000000000000000, 0.9238795325112867385, 1.000000000000000000, 0.9238795325112867385, 1.000000000000000000, 0.9238795325112867385, 1.000000000000000000, 0.9238795325112867385, 1.000000000000000000, 0.9238795325112867385, 1.000000000000000000, 0.9238795325112867385, 1.000000000000000000, 0.9238795325112867385, 1.000000000000000000, 0.9238795325112867385, 1.000000000000000000, 0.9238795325112867385, 1.000000000000000000, 0.9238795325112867385, 1.000000000000000000, 0.9238795325112867385, 1.000000000000000000, 0.9238795325112867385, 1.000000000000000000, 0.9238795325112867385, 1.000000000000000000, 0.9238795325112867385, 1.000000000000000000, 0.9238795325112867385, 1.000000000000000000, 0.9238795325112867385, 1.000000000000000000, 0.9238795325112867385, 1.000000000000000000, 0.9238795325112867385, 1.000000000000000000, 0.9238795325112867385, 1.000000000000000000, 0.9238795325112867385, 1.000000000000000000, 0.9238795325112867385, 1.000000000000000000, 0.9238795325112867385, 1.000000000000000000, 0.9238795325112867385, 1.000000000000000000, 0.9238795325112867385, 1.000000000000000000, 0.9238795325112867385, 1.000000000000000000, 0.9238795325112867385, 1.000000000000000000, 0.9238795325112867385, 1.000000000000000000, 0.9238795325112867385, 1.000000000000000000, 0.9238795325112867385, 1.000000000000000000, 0.9238795325112867385, 1.000000000000000000, 0.9238795325112867385, 1.000000000000000000, 0.9238795325112867385, 1.000000000000000000, 0.9238795325112867385, 1.000000000000000000, 0.9238795325112867385, 1.000000000000000000, 0.9238795325112867385, 1.000000000000000000, 0.9238795325112867385, 1.000000000000000000, 0.9238795325112867385, 1.000000000000000000, 0.9238795325112867385, 1.000000000000000000, 0.9238795325112867385, 1.000000000000000000, 0.9238795325112867385, 1.000000000000000000, 0.9238795325112867385, 1.000000000000000000, 0.9238795325112867385, 1.000000000000000000, 0.9238795325112867385, 1.000000000000000000, 0.9238795325112867385, 1.000000000000000000, 0.9238795325112867385, 1.000000000000000000, 0.9238795325112867385, 1.000000000000000000, 0.9238795325112867385, 1.000000000000000000, 0.9238795325112867385, 1.000000000000000000, 0.9238795325112867385, 1.000000000000000000, 0.9238795325112867385, 1.000000000000000000, 0.9238795325112867385, 1.000000000000000000, 0.9238795325112867385, 1.000000000000000000, 0.9238795325112867385, 1.000000000000000000, 0.9238795325112867385, 1.000000000000000000, 0.9238795325112867385, 1.000000000000000000, 0.9238795325112867385, 1.000000000000000000, 0.9238795325112867385, 1.000000000000000000, 0.9238795325112867385, 1.000000000000000000, 0.9238795325112867385, 1.000000000000000000, 0.9238795325112867385, 1.000000000000000000, 0.9238795325112867385, 1.000000000000000000, 0.9238795325112867385, 1.000000000000000000, 0.9238795325112867385, 1.000000000000000000, 0.9238795325112867385, 1.000000000000000000, 0.9238795325112867385, 1.000000000000000000, 0.9238795325112867385, 1.000000000000000000, 0.9238795325112867385, 1.000000000000000000, 0.9238795325112867385, 1.000000000000000000, 0.9238795325112867385, 1.000000000000000000, 0.9238795325112867385, 1.000000000000000000, 0.9238795325112867385, 1.000000000000000000, 0.9238795325112867385, 1.000000000000000000, 0.9238795325112867385, 1.000000000000000000, 0.9238795325112867385, 1.000000000000000000, 0.9238795325112867385, 1.000000000000000000, 0.9238795325112867385, 1.000000000000000000, 0.9238795325112867385, 1.000000000000000000, 0.9238795325112867385, 1.000000000000000000, 0.9238795325112867385, 1.000000000000000000, 0.9238795325112867385, 1.000000000000000000, 0.9238795325112867385, 1.000000000000000000, 0.9238795325112867385, 1.000000000000000000, 0.9238795325112867385, 1.000000000000000000, 0.9238795325112867385, 1.000000000000000000, 0.9238795325112867385, 1.000000000000000000, 0.9238795325112867385, 1.000000000000000000, 0.9744806372117011950, 0.9660719911230173373) ) ) 
 REPRESENTATION_ITEM ( '' )  SURFACE ( )  );
#89308=CARTESIAN_POINT ( 'NONE',  ( 8.000000000000000000, -29.09375000409677270, -3.313708498984761608 ) ) ;
#89312=CARTESIAN_POINT ( 'NONE',  ( 9.948688207305192321, 33.87023149490183727, -1.044946705213435800 ) ) ;
#89314=FACE_OUTER_BOUND ( 'NONE', #4918, .T. ) ;
#89330=CARTESIAN_POINT ( 'NONE',  ( -9.999999999999960920, 15.00000000000001066, 3.836411046841925465 ) ) ;
#89350=CARTESIAN_POINT ( 'NONE',  ( -6.928203230275510549, 30.00000000000000000, 4.000000000000000000 ) ) ;
#89368=CARTESIAN_POINT ( 'NONE',  ( 3.648665620917491470, 15.00000000000000000, 9.999999999999998224 ) ) ;
#89388=DIRECTION ( 'NONE',  ( 0.000000000000000000, 0.000000000000000000, 1.000000000000000000 ) ) ;
#89403=CARTESIAN_POINT ( 'NONE',  ( 7.414346147791995634, 102.3541084233773262, -3.010818766110535005 ) ) ;
#89434=CARTESIAN_POINT ( 'NONE',  ( 3.313708498984762052, -13.71874999999999112, -8.000000000000000000 ) ) ;
#89436=( BOUNDED_SURFACE ( )  B_SPLINE_SURFACE ( 3, 2, ( 
 ( #53619, #47107, #29387 ),
 ( #12090, #22352, #95158 ),
 ( #21290, #69810, #46589 ),
 ( #46071, #55197, #88125 ),
 ( #61743, #94639, #14205 ),
 ( #20784, #86554, #5077 ),
 ( #38011, #16341, #88644 ),
 ( #82130, #105877, #6654 ),
 ( #89181, #47636, #23402 ),
 ( #65433, #15282, #80536 ) ),
 .UNSPECIFIED., .F., .F., .F. ) 
 B_SPLINE_SURFACE_WITH_KNOTS ( ( 4, 2, 2, 2, 4 ),
 ( 3, 3 ),
 ( 0.002450517525418899507, 0.003060732775749471640, 0.003670948026080044207, 0.004891378526741188906, 0.007332239528063478305 ),
 ( 0.000000000000000000, 1.000000000000000000 ),
 .UNSPECIFIED. ) 
 GEOMETRIC_REPRESENTATION_ITEM ( )  RATIONAL_B_SPLINE_SURFACE ( (
 ( 1.000000000000000000, 0.7071067811865470176, 1.000000000000000000),
 ( 1.000000000000000000, 0.7344063550101938009, 1.000000000000000000),
 ( 1.000000000000000000, 0.7590375248711010991, 1.000000000000000000),
 ( 1.000000000000000000, 0.8038331608704093467, 1.000000000000000000),
 ( 1.000000000000000000, 0.8240352460866127160, 1.000000000000000000),
 ( 1.000000000000000000, 0.8791017378332789400, 1.000000000000000000),
 ( 1.000000000000000000, 0.9085032776980890290, 1.000000000000000000),
 ( 1.000000000000000000, 0.9784170511696812511, 1.000000000000000000),
 ( 1.000000000000000000, 0.9996598051696619081, 1.000000000000000000),
 ( 1.000000000000000000, 1.000000000000000000, 1.000000000000000000) ) ) 
 REPRESENTATION_ITEM ( '' )  SURFACE ( )  );
#89459=CARTESIAN_POINT ( 'NONE',  ( 9.999999999999998224, 15.23416508903533817, -0.7060372491625556135 ) ) ;
#89480=CARTESIAN_POINT ( 'NONE',  ( -9.981544566921638051, 15.23274035658503145, 0.7016502453916984017 ) ) ;
#89494=CARTESIAN_POINT ( 'NONE',  ( -9.926810856659439963, 15.46725112412266512, -1.404490565848994343 ) ) ;
#89523=EDGE_CURVE ( 'NONE', #28165, #77405, #94780, .T. ) ;
#89525=VERTEX_POINT ( 'NONE', #87302 ) ;
#89544=ORIENTED_EDGE ( 'NONE', *, *, #22127, .T. ) ;
#89555=CARTESIAN_POINT ( 'NONE',  ( -3.313708498984760720, -33.03125000000000000, -8.000000000000000000 ) ) ;
#89563=ORIENTED_EDGE ( 'NONE', *, *, #12795, .F. ) ;
#89576=CARTESIAN_POINT ( 'NONE',  ( 7.551892080562057075, 108.0098770253938341, 2.647003822403973583 ) ) ;
#89578=EDGE_CURVE ( 'NONE', #33604, #1839, #70046, .T. ) ;
#89583=CARTESIAN_POINT ( 'NONE',  ( 5.082755093536324154, -13.34375000204838457, 5.082755093536326818 ) ) ;
#89607=EDGE_CURVE ( 'NONE', #12516, #97744, #4703, .T. ) ;
#89631=CARTESIAN_POINT ( 'NONE',  ( -5.082755093536326818, -12.59375000204838635, 5.082755093536325042 ) ) ;
#89637=CARTESIAN_POINT ( 'NONE',  ( 7.188101187500000044, -28.53125000204838813, 0.000000000000000000 ) ) ;
#89640=CARTESIAN_POINT ( 'NONE',  ( 7.188101187499999156, -27.12500000204838457, 2.977408999572654924 ) ) ;
#89657=CARTESIAN_POINT ( 'NONE',  ( -7.414346147791998298, 87.64589157662267382, -3.010818766110534561 ) ) ;
#89683=CARTESIAN_POINT ( 'NONE',  ( 0.000000000000000000, 115.0000000000000000, -10.00000000000000000 ) ) ;
#89685=CARTESIAN_POINT ( 'NONE',  ( 5.082755093536324154, -27.21875000204838813, 5.082755093536326818 ) ) ;
#89698=CARTESIAN_POINT ( 'NONE',  ( -2.977408999572650039, -12.68750000204838280, -7.188101187500000933 ) ) ;
#89699=CARTESIAN_POINT ( 'NONE',  ( 7.412906595240166929, 27.35811727147745387, 3.014362223629234894 ) ) ;
#89706=PLANE ( 'NONE',  #14769 ) ;
#89712=CARTESIAN_POINT ( 'NONE',  ( 5.082755093536325930, -29.46875000204838813, -5.082755093536325042 ) ) ;
#89716=CARTESIAN_POINT ( 'NONE',  ( -9.699016383038308931, 88.17638171448342632, 2.444973590251037443 ) ) ;
#89723=PRESENTATION_STYLE_ASSIGNMENT (( #6664 ) ) ;
#89764=CARTESIAN_POINT ( 'NONE',  ( 7.212994264445061532, 87.01711344340040455, 3.463766307298585811 ) ) ;
#89769=DIRECTION ( 'NONE',  ( -0.9090909090909089496, 0.000000000000000000, 0.4165977904505313578 ) ) ;
#89772=CARTESIAN_POINT ( 'NONE',  ( -7.188101187500002709, -16.81250000204838457, 2.977408999572648707 ) ) ;
#89774=CARTESIAN_POINT ( 'NONE',  ( 9.221249107921748234, 83.95178628501514595, 3.869340886054257300 ) ) ;
#89775=CARTESIAN_POINT ( 'NONE',  ( -3.313708498984765161, -13.15625000409676915, 7.999999999999998224 ) ) ;
#89795=DIRECTION ( 'NONE',  ( 0.9090909090909090606, 0.000000000000000000, -0.4165977904505313578 ) ) ;
#89835=CARTESIAN_POINT ( 'NONE',  ( 8.000000000000000000, -32.09375000409677625, -3.313708498984761608 ) ) ;
#89841=CARTESIAN_POINT ( 'NONE',  ( -1.927070765752276982, -29.99999999999998934, -7.651354226332538921 ) ) ;
#89865=EDGE_CURVE ( 'NONE', #1287, #42289, #41921, .T. ) ;
#89879=CARTESIAN_POINT ( 'NONE',  ( -7.558582284419547825, -29.99999999999999289, 1.912896512380730218 ) ) ;
#89906=( LENGTH_UNIT ( ) NAMED_UNIT ( * ) SI_UNIT ( .MILLI., .METRE. ) );
#89922=CARTESIAN_POINT ( 'NONE',  ( 7.045965687440312486, 103.6960753621396378, 3.790395326974321133 ) ) ;
#89926=CARTESIAN_POINT ( 'NONE',  ( 9.797174393178825657E-16, 115.0000000000000000, 8.000000000000000000 ) ) ;
#89940=AXIS2_PLACEMENT_3D ( 'NONE', #74825, #75904, #90497 ) ;
#89951=CARTESIAN_POINT ( 'NONE',  ( 8.000000000000000000, -15.49999999999999289, 0.000000000000000000 ) ) ;
#89963=ORIENTED_EDGE ( 'NONE', *, *, #30298, .F. ) ;
#89980=CARTESIAN_POINT ( 'NONE',  ( 9.999999999999857891, 15.00000000000006750, -3.648665620917497243 ) ) ;
#89994=CARTESIAN_POINT ( 'NONE',  ( -5.656854249492379694, -29.93749999999999645, -5.656854249492380582 ) ) ;
#89998=ORIENTED_EDGE ( 'NONE', *, *, #82464, .F. ) ;
#90018=CARTESIAN_POINT ( 'NONE',  ( -7.188101187500002709, -31.81250000204839168, 2.977408999572648707 ) ) ;
#90019=CARTESIAN_POINT ( 'NONE',  ( -4.165977904505308693, 16.00000000000000000, 9.090909090909091717 ) ) ;
#90021=CARTESIAN_POINT ( 'NONE',  ( 0.000000000000000000, 15.00000000000000000, -9.999999999999998224 ) ) ;
#90051=VERTEX_POINT ( 'NONE', #5199 ) ;
#90077=CARTESIAN_POINT ( 'NONE',  ( 3.313708498984762496, -33.78125000000000000, 7.999999999999998224 ) ) ;
#90102=CARTESIAN_POINT ( 'NONE',  ( -2.977408999572650039, -12.68750000204838280, -7.188101187500001821 ) ) ;
#90155=CARTESIAN_POINT ( 'NONE',  ( -7.188101187500000044, -15.78125000204838635, -8.802885111219163269E-16 ) ) ;
#90162=CARTESIAN_POINT ( 'NONE',  ( -7.188101187500000933, -29.37500000204838457, -2.977408999572651371 ) ) ;
#90165=CARTESIAN_POINT ( 'NONE',  ( -7.188101187500002709, -29.18750000204839523, 2.977408999572648707 ) ) ;
#90183=CARTESIAN_POINT ( 'NONE',  ( -7.344505440741527558, 87.44618927298706978, -3.175463080953002226 ) ) ;
#90194=CARTESIAN_POINT ( 'NONE',  ( -5.656854249492381470, -25.25000000409677270, 5.656854249492379694 ) ) ;
#90207=CARTESIAN_POINT ( 'NONE',  ( 9.253817200599833370, 28.70007270083139161, -3.791916801615163202 ) ) ;
#90208=CARTESIAN_POINT ( 'NONE',  ( -5.082755093536325042, -27.96875000204838457, -5.082755093536325930 ) ) ;
#90220=CARTESIAN_POINT ( 'NONE',  ( 2.977408999572652260, -14.93750000204838457, 7.188101187500000044 ) ) ;
#90234=CARTESIAN_POINT ( 'NONE',  ( 4.401442555609581635E-16, -30.78125000204838813, -7.188101187500000044 ) ) ;
#90292=CARTESIAN_POINT ( 'NONE',  ( -2.977408999572654480, -19.62500000204838457, 7.188101187499999156 ) ) ;
#90294=CARTESIAN_POINT ( 'NONE',  ( 9.380871178326117388, 82.98883620201672784, 3.467392232194206780 ) ) ;
#90305=ORIENTED_EDGE ( 'NONE', *, *, #93988, .F. ) ;
#90358=CARTESIAN_POINT ( 'NONE',  ( 4.898587196589412829E-16, -25.81250000409677270, -8.000000000000000000 ) ) ;
#90404=CARTESIAN_POINT ( 'NONE',  ( -7.743982712349856357, 33.46213014760736826, 2.020119794285908377 ) ) ;
#90443=CARTESIAN_POINT ( 'NONE',  ( -8.000000000000000000, -28.53125000409677270, -3.313708498984762496 ) ) ;
#90475=VECTOR ( 'NONE', #55517, 1000.000000000000000 ) ;
#90487=CARTESIAN_POINT ( 'NONE',  ( 8.000000000000000000, -10.90624999999999112, -3.313708498984761608 ) ) ;
#90497=DIRECTION ( 'NONE',  ( 0.000000000000000000, 0.000000000000000000, 1.000000000000000000 ) ) ;
#90516=CARTESIAN_POINT ( 'NONE',  ( -7.897196874019794421, 81.20872795832194413, -1.302055520192082705 ) ) ;
#90552=CARTESIAN_POINT ( 'NONE',  ( -5.082755093536326818, -28.71875000204838813, 5.082755093536325042 ) ) ;
#90578=EDGE_CURVE ( 'NONE', #67063, #3603, #75236, .T. ) ;
#90586=VERTEX_POINT ( 'NONE', #83996 ) ;
#90603=EDGE_CURVE ( 'NONE', #31791, #61442, #11148, .T. ) ;
#90613=CARTESIAN_POINT ( 'NONE',  ( 7.999999999999998224, -26.09374999999999289, 3.313708498984766493 ) ) ;
#90637=CARTESIAN_POINT ( 'NONE',  ( 5.082755093536325930, -12.96875000204838280, -5.082755093536325042 ) ) ;
#90638=CARTESIAN_POINT ( 'NONE',  ( -9.165151389911679658, 104.9999999999999858, -4.000000000000001776 ) ) ;
#90696=CARTESIAN_POINT ( 'NONE',  ( 7.188101187499999156, -10.62500000204838813, 2.977408999572654924 ) ) ;
#90699=CARTESIAN_POINT ( 'NONE',  ( 7.122964895856751077, -30.00000000000000355, -0.9654893961775683486 ) ) ;
#90705=CARTESIAN_POINT ( 'NONE',  ( -5.082755093536325042, -18.96875000204838457, -5.082755093536325930 ) ) ;
#90744=CARTESIAN_POINT ( 'NONE',  ( -7.188101187500000044, -23.28125000204838457, -8.802885111219163269E-16 ) ) ;
#90747=EDGE_CURVE ( 'NONE', #24651, #25439, #20674, .T. ) ;
#90754=CARTESIAN_POINT ( 'NONE',  ( 9.842984802582135373, 88.59069590475651523, 1.781981959250505732 ) ) ;
#90760=CARTESIAN_POINT ( 'NONE',  ( 7.986539162393897939, 26.02672828942547412, -0.5321833565149868273 ) ) ;
#90771=CARTESIAN_POINT ( 'NONE',  ( -4.912107334123172464, -8.720202445280490267, 6.401601164861591364 ) ) ;
#90775=AXIS2_PLACEMENT_3D ( 'NONE', #28904, #45579, #36459 ) ;
#90823=CARTESIAN_POINT ( 'NONE',  ( 8.000113193197767814, 89.00022638645860695, -0.2613481123984641719 ) ) ;
#90834=CARTESIAN_POINT ( 'NONE',  ( -7.188101187500000044, -10.90625000204838457, -8.802885111219163269E-16 ) ) ;
#90836=( BOUNDED_CURVE ( )  B_SPLINE_CURVE ( 2, ( #21115, #88988, #54461, #71201, #104632, #30237, #23214, #46410, #78757 ),
 .UNSPECIFIED., .F., .F. ) 
 B_SPLINE_CURVE_WITH_KNOTS ( ( 3, 2, 2, 2, 3 ),
 ( 0.3970588235294117974, 0.4044117647058824150, 0.4117647058823530326, 0.4191176470588236502, 0.4264705882352942123 ),
 .UNSPECIFIED. ) 
 CURVE ( )  GEOMETRIC_REPRESENTATION_ITEM ( )  RATIONAL_B_SPLINE_CURVE ( ( 0.9999999999999994449, 0.9238795325112872936, 1.000000000000000000, 0.9238795325112867385, 1.000000000000000000, 0.9238795325112867385, 1.000000000000000000, 0.9238795325112856283, 1.000000000000001110 ) ) 
 REPRESENTATION_ITEM ( '' )  );
#90866=CARTESIAN_POINT ( 'NONE',  ( -4.582575694955839829, 16.00000000000000000, 10.00000000000000000 ) ) ;
#90867=ORIENTED_EDGE ( 'NONE', *, *, #43042, .T. ) ;
#90869=CYLINDRICAL_SURFACE ( 'NONE', #67590, 4.000000000000000000 ) ;
#90891=CARTESIAN_POINT ( 'NONE',  ( -7.188101187500000044, -28.90625000204838813, -8.802885111219163269E-16 ) ) ;
#90900=CARTESIAN_POINT ( 'NONE',  ( -8.000000000000000000, -21.03125000409677625, -3.313708498984762496 ) ) ;
#90909=CARTESIAN_POINT ( 'NONE',  ( -2.838086098462165197, -29.99999999999999289, -7.435270884616921983 ) ) ;
#90983=FACE_BOUND ( 'NONE', #44943, .T. ) ;
#90999=CARTESIAN_POINT ( 'NONE',  ( 7.151217271224852290, 103.2125059955428554, -3.587901469523284259 ) ) ;
#91001=EDGE_CURVE ( 'NONE', #29277, #3543, #17556, .T. ) ;
#91015=ORIENTED_EDGE ( 'NONE', *, *, #25650, .F. ) ;
#91016=CARTESIAN_POINT ( 'NONE',  ( 9.797372177749755551, 108.4650949484756239, 2.014953862275849605 ) ) ;
#91050=CARTESIAN_POINT ( 'NONE',  ( 8.000000000000000000, -18.49999999999999289, 0.000000000000000000 ) ) ;
#91071=CARTESIAN_POINT ( 'NONE',  ( -7.619753052866896859, 81.82548497192826176, -2.447276542590445914 ) ) ;
#91102=CARTESIAN_POINT ( 'NONE',  ( 7.188101187500001821, -32.56250000204838813, -2.977408999572650483 ) ) ;
#91164=CARTESIAN_POINT ( 'NONE',  ( 7.999999999999998224, -23.09374999999999645, 3.313708498984766049 ) ) ;
#91165=CARTESIAN_POINT ( 'NONE',  ( -8.000000000000000000, -26.84374999999998934, -3.313708498984762496 ) ) ;
#91173=CARTESIAN_POINT ( 'NONE',  ( 0.000000000000000000, 115.0000000000000000, 0.000000000000000000 ) ) ;
#91185=CARTESIAN_POINT ( 'NONE',  ( 7.213352437320215138, 107.0183647300768257, -3.463014597543483841 ) ) ;
#91190=CARTESIAN_POINT ( 'NONE',  ( -2.977408999572650039, -11.18750000204838457, -7.188101187500001821 ) ) ;
#91241=ORIENTED_EDGE ( 'NONE', *, *, #96371, .T. ) ;
#91245=CARTESIAN_POINT ( 'NONE',  ( -1.320432766682874540E-15, -13.90625000204838457, 7.188101187500000044 ) ) ;
#91251=CARTESIAN_POINT ( 'NONE',  ( 2.977408999572650927, -17.75000000204838457, -7.188101187500001821 ) ) ;
#91288=CARTESIAN_POINT ( 'NONE',  ( 9.948513602187993854, 26.13022056656141245, 1.045942665286129003 ) ) ;
#91289=CARTESIAN_POINT ( 'NONE',  ( 7.188101187500000044, -21.03125000204838813, 0.000000000000000000 ) ) ;
#91301=CARTESIAN_POINT ( 'NONE',  ( -3.594033448928638741, -9.156975712238445197, 6.225088131883843801 ) ) ;
#91313=CARTESIAN_POINT ( 'NONE',  ( 5.082755093536325930, -30.96875000204838813, -5.082755093536325042 ) ) ;
#91346=DIRECTION ( 'NONE',  ( -0.000000000000000000, 1.000000000000000000, -0.000000000000000000 ) ) ;
#91371=CARTESIAN_POINT ( 'NONE',  ( -2.977408999572650039, -14.18750000204838280, -7.188101187500001821 ) ) ;
#91407=CARTESIAN_POINT ( 'NONE',  ( 7.744991119775238353, 81.53561214574871485, -2.016316005557097668 ) ) ;
#91413=CARTESIAN_POINT ( 'NONE',  ( 7.188101187500001821, -34.43750000204838813, -2.977408999572650483 ) ) ;
#91429=CARTESIAN_POINT ( 'NONE',  ( 7.188101187499999156, -22.25000000204839523, 2.977408999572654924 ) ) ;
#91432=EDGE_CURVE ( 'NONE', #70286, #27681, #18499, .T. ) ;
#91439=CARTESIAN_POINT ( 'NONE',  ( -5.656854249492381470, -22.25000000409676915, 5.656854249492379694 ) ) ;
#91443=CARTESIAN_POINT ( 'NONE',  ( 9.918325909156573417, 33.79235231707431808, 1.298699613733151681 ) ) ;
#91462=CARTESIAN_POINT ( 'NONE',  ( 0.000000000000000000, 16.00000000000000000, 0.000000000000000000 ) ) ;
#91500=CARTESIAN_POINT ( 'NONE',  ( 4.210530276627960866, 14.99999999999998934, 10.00000000000003908 ) ) ;
#91570=CARTESIAN_POINT ( 'NONE',  ( 0.000000000000000000, 15.00000000000000000, -10.00000000000000000 ) ) ;
#91621=CARTESIAN_POINT ( 'NONE',  ( 4.898587196589412829E-16, -28.62499999999999289, -8.000000000000000000 ) ) ;
#91623=VERTEX_POINT ( 'NONE', #70743 ) ;
#91628=CARTESIAN_POINT ( 'NONE',  ( 7.188101187500000044, -32.65625000204838813, 0.000000000000000000 ) ) ;
#91635=CARTESIAN_POINT ( 'NONE',  ( 5.656854249492380582, -27.31249999999999645, -5.656854249492379694 ) ) ;
#91660=ORIENTED_EDGE ( 'NONE', *, *, #86935, .F. ) ;
#91683=CARTESIAN_POINT ( 'NONE',  ( -3.313708498984765161, -27.96874999999999289, 7.999999999999998224 ) ) ;
#91689=ORIENTED_EDGE ( 'NONE', *, *, #75590, .F. ) ;
#91695=CARTESIAN_POINT ( 'NONE',  ( -5.656854249492379694, -33.12500000409677625, -5.656854249492380582 ) ) ;
#91696=CARTESIAN_POINT ( 'NONE',  ( 4.898587196589412829E-16, -27.31250000409677270, -8.000000000000000000 ) ) ;
#91708=CARTESIAN_POINT ( 'NONE',  ( -2.977408999572654480, -12.12500000204838990, 7.188101187499999156 ) ) ;
#91762=CARTESIAN_POINT ( 'NONE',  ( -7.188101187500002709, -9.687500002048384573, 2.977408999572647819 ) ) ;
#91769=CARTESIAN_POINT ( 'NONE',  ( -2.977408999572654480, -21.50000000204839168, 7.188101187499999156 ) ) ;
#91811=CARTESIAN_POINT ( 'NONE',  ( -7.188101187500001821, -21.87500000204838813, -2.977408999572651371 ) ) ;
#91813=CARTESIAN_POINT ( 'NONE',  ( -8.000000000000001776, -11.84375000409677092, 3.313708498984759387 ) ) ;
#91824=CARTESIAN_POINT ( 'NONE',  ( -7.188101187500000933, -9.500000002048388126, -2.977408999572651371 ) ) ;
#91833=CARTESIAN_POINT ( 'NONE',  ( 2.977408999572650927, -30.87500000204838813, -7.188101187500001821 ) ) ;
#91886=CARTESIAN_POINT ( 'NONE',  ( 4.401442555609581635E-16, -14.28125000204838457, -7.188101187500000044 ) ) ;
#91887=CARTESIAN_POINT ( 'NONE',  ( -10.00000000000000000, 15.00000000000000000, 10.00000000000000000 ) ) ;
#91923=DIRECTION ( 'NONE',  ( 0.000000000000000000, 0.000000000000000000, 1.000000000000000000 ) ) ;
#91943=CARTESIAN_POINT ( 'NONE',  ( -5.082755093536326818, -25.71875000204838813, 5.082755093536325042 ) ) ;
#91952=CARTESIAN_POINT ( 'NONE',  ( 3.313708498984762496, -23.46875000409677270, 7.999999999999998224 ) ) ;
#92007=EDGE_LOOP ( 'NONE', ( #95423, #82766, #105360, #66935 ) ) ;
#92011=CARTESIAN_POINT ( 'NONE',  ( 0.000000000000000000, 15.00000000000000000, 10.00000000000000000 ) ) ;
#92035=EDGE_LOOP ( 'NONE', ( #105275, #21510, #99673, #59832, #8741, #2803, #88169 ) ) ;
#92105=CARTESIAN_POINT ( 'NONE',  ( -7.934203308536660337, 81.13299659982199330, 1.057099537198550321 ) ) ;
#92145=AXIS2_PLACEMENT_3D ( 'NONE', #56326, #39659, #56865 ) ;
#92188=CARTESIAN_POINT ( 'NONE',  ( 5.656854249492378806, -27.68749999999999645, 5.656854249492381470 ) ) ;
#92205=CARTESIAN_POINT ( 'NONE',  ( 6.928203230275505220, 105.2688332450899935, -4.000000000000002665 ) ) ;
#92233=CARTESIAN_POINT ( 'NONE',  ( -1.469576158976823947E-15, -24.87499999999999289, 8.000000000000000000 ) ) ;
#92242=MECHANICAL_DESIGN_GEOMETRIC_PRESENTATION_REPRESENTATION('',(#81927),#80239);
#92243=ORIENTED_EDGE ( 'NONE', *, *, #12978, .F. ) ;
#92248=EDGE_CURVE ( 'NONE', #42289, #84434, #34341, .T. ) ;
#92275=CARTESIAN_POINT ( 'NONE',  ( 5.082755093536325930, -20.84375000204838813, -5.082755093536325042 ) ) ;
#92288=CARTESIAN_POINT ( 'NONE',  ( 3.313708498984685225, -13.71874999999998934, -8.000000000000076383 ) ) ;
#92292=ORIENTED_EDGE ( 'NONE', *, *, #53875, .T. ) ;
#92300=CARTESIAN_POINT ( 'NONE',  ( 9.607634652977997902, 15.83450757143046950, -2.797224791467303628 ) ) ;
#92319=CARTESIAN_POINT ( 'NONE',  ( 0.000000000000000000, -30.00000000000000000, 8.000000000000000000 ) ) ;
#92320=CARTESIAN_POINT ( 'NONE',  ( -2.977408999572650039, -17.56250000204838813, -7.188101187500001821 ) ) ;
#92345=CARTESIAN_POINT ( 'NONE',  ( -2.977408999572650039, -23.18750000204838813, -7.188101187500001821 ) ) ;
#92352=CARTESIAN_POINT ( 'NONE',  ( -10.00000000000000355, 30.00000000000000000, -4.000000000000000000 ) ) ;
#92396=EDGE_LOOP ( 'NONE', ( #22448, #46284, #27233, #9307 ) ) ;
#92398=CARTESIAN_POINT ( 'NONE',  ( -7.188101187500002709, -24.68750000204838813, 2.977408999572647819 ) ) ;
#92407=CARTESIAN_POINT ( 'NONE',  ( 2.977408999572650927, -15.87500000204838635, -7.188101187500001821 ) ) ;
#92436=ORIENTED_EDGE ( 'NONE', *, *, #95268, .T. ) ;
#92438=CARTESIAN_POINT ( 'NONE',  ( 6.943926999490792618, 84.46699007373855750, -3.973092371898546027 ) ) ;
#92467=CARTESIAN_POINT ( 'NONE',  ( -7.188101187500002709, -25.81250000204838457, 2.977408999572647819 ) ) ;
#92476=CARTESIAN_POINT ( 'NONE',  ( 5.656854249492378806, -24.87500000409677270, 5.656854249492381470 ) ) ;
#92485=CARTESIAN_POINT ( 'NONE',  ( 3.736676496572839845, -30.00000000000000000, -6.612488830499654746 ) ) ;
#92486=ORIENTED_EDGE ( 'NONE', *, *, #45470, .T. ) ;
#92536=ADVANCED_FACE ( 'NONE', ( #29963 ), #95738, .F. ) ;
#92569=EDGE_LOOP ( 'NONE', ( #2645, #69795, #63438 ) ) ;
#92608=ADVANCED_FACE ( 'NONE', ( #32619, #67088, #7237, #40145 ), #7768, .F. ) ;
#92613=CARTESIAN_POINT ( 'NONE',  ( 0.3539438260514400914, 15.11738935797732530, -9.999999999999998224 ) ) ;
#92615=ORIENTED_EDGE ( 'NONE', *, *, #35616, .T. ) ;
#92641=CARTESIAN_POINT ( 'NONE',  ( -9.537909130738276176, 107.6461483096339435, -3.010726932293859903 ) ) ;
#92708=CARTESIAN_POINT ( 'NONE',  ( -1.469576158976823947E-15, -29.56250000409677270, 8.000000000000000000 ) ) ;
#92730=CARTESIAN_POINT ( 'NONE',  ( 3.313708498984762052, -24.21874999999999289, -8.000000000000000000 ) ) ;
#92777=DIRECTION ( 'NONE',  ( 1.000000000000000000, 0.000000000000000000, 0.000000000000000000 ) ) ;
#92819=CARTESIAN_POINT ( 'NONE',  ( -1.320432766682874540E-15, -19.90625000204838457, 7.188101187500000044 ) ) ;
#92831=CARTESIAN_POINT ( 'NONE',  ( -6.943482370013980720, 85.52848370260727506, 3.973876482044367275 ) ) ;
#92840=CARTESIAN_POINT ( 'NONE',  ( 9.999999999999998224, 15.11603512202947108, -0.3498606326598576177 ) ) ;
#92855=CARTESIAN_POINT ( 'NONE',  ( 7.188101187500001821, -20.93750000204838457, -2.977408999572650483 ) ) ;
#92879=( BOUNDED_CURVE ( )  B_SPLINE_CURVE ( 2, ( #13002, #44334, #95025, #78807, #102570, #69155, #45928, #85877, #77228 ),
 .UNSPECIFIED., .F., .F. ) 
 B_SPLINE_CURVE_WITH_KNOTS ( ( 3, 2, 2, 2, 3 ),
 ( 0.2205882352941176960, 0.2279411764705882859, 0.2352941176470588758, 0.2426470588235294656, 0.2500000000000000555 ),
 .UNSPECIFIED. ) 
 CURVE ( )  GEOMETRIC_REPRESENTATION_ITEM ( )  RATIONAL_B_SPLINE_CURVE ( ( 0.9999999999999994449, 0.9238795325112872936, 1.000000000000000000, 0.9238795325112867385, 1.000000000000000000, 0.9238795325112867385, 1.000000000000000000, 0.9238795325112861834, 1.000000000000000666 ) ) 
 REPRESENTATION_ITEM ( '' )  );
#92885=CARTESIAN_POINT ( 'NONE',  ( -1.320432766682874540E-15, -27.03125000204838813, 7.188101187500000044 ) ) ;
#92887=CARTESIAN_POINT ( 'NONE',  ( 9.797174393178825657E-16, -30.00000000000000000, -8.000000000000000000 ) ) ;
#92913=CARTESIAN_POINT ( 'NONE',  ( 8.000000000000000000, -25.99999999999999645, 0.000000000000000000 ) ) ;
#92937=CARTESIAN_POINT ( 'NONE',  ( -2.977408999572654480, -24.50000000204839168, 7.188101187499999156 ) ) ;
#92948=CARTESIAN_POINT ( 'NONE',  ( -7.188101187500001821, -14.00000000204838457, -2.977408999572651371 ) ) ;
#92951=DIRECTION ( 'NONE',  ( 1.000000000000000000, 0.000000000000000000, 0.000000000000000000 ) ) ;
#92971=CARTESIAN_POINT ( 'NONE',  ( 0.000000000000000000, 115.0000000000000000, -10.00000000000000000 ) ) ;
#93008=CARTESIAN_POINT ( 'NONE',  ( -5.082755093536325042, -24.59375000204838813, -5.082755093536325930 ) ) ;
#93011=SURFACE_SIDE_STYLE ('',( #68205 ) ) ;
#93018=CARTESIAN_POINT ( 'NONE',  ( 4.898587196589412829E-16, -16.81250000409677270, -8.000000000000000000 ) ) ;
#93029=FILL_AREA_STYLE ('',( #3495 ) ) ;
#93035=VERTEX_POINT ( 'NONE', #54452 ) ;
#93076=ORIENTED_EDGE ( 'NONE', *, *, #19700, .F. ) ;
#93081=CARTESIAN_POINT ( 'NONE',  ( 2.701558353794677014, 15.00000000000000000, 9.999999999999998224 ) ) ;
#93100=DIRECTION ( 'NONE',  ( 0.000000000000000000, 0.000000000000000000, -1.000000000000000000 ) ) ;
#93123=DIRECTION ( 'NONE',  ( 1.734723475976807094E-16, 0.000000000000000000, 1.000000000000000000 ) ) ;
#93124=VERTEX_POINT ( 'NONE', #21620 ) ;
#93166=AXIS2_PLACEMENT_3D ( 'NONE', #37563, #86634, #61276 ) ;
#93190=CYLINDRICAL_SURFACE ( 'NONE', #39562, 8.000000000000000000 ) ;
#93197=LINE ( 'NONE', #100743, #37213 ) ;
#93225=CARTESIAN_POINT ( 'NONE',  ( -5.656854249492381470, -13.06249999999999467, 5.656854249492379694 ) ) ;
#93272=CARTESIAN_POINT ( 'NONE',  ( 3.313708498984762052, -18.21874999999999645, -8.000000000000000000 ) ) ;
#93295=CARTESIAN_POINT ( 'NONE',  ( 7.986468734911287726, 108.9731367972307936, 0.5341897780976140320 ) ) ;
#93303=FILL_AREA_STYLE ('',( #46341 ) ) ;
#93313=ORIENTED_EDGE ( 'NONE', *, *, #40221, .F. ) ;
#93322=CARTESIAN_POINT ( 'NONE',  ( -3.313708498984760276, -25.53124999999999645, -8.000000000000000000 ) ) ;
#93364=B_SPLINE_CURVE_WITH_KNOTS ( 'NONE', 3,
 ( #32423, #64253, #31882, #64766, #97641, #65292, #23807, #56653, #24337, #89576, #68495, #76558, #51754, #1596, #43670, #93295, #2669, #100308, #10234, #35620, #59339, #84669, #99781, #74431, #101385, #34558, #42072, #91185, #26469, #19451, #67432, #83584, #92205, #66896 ),
 .UNSPECIFIED., .F., .F.,
 ( 4, 2, 2, 2, 2, 2, 2, 2, 2, 2, 2, 2, 2, 2, 2, 2, 4 ),
 ( 0.01272238763756221476, 0.01351613129786393211, 0.01430987495816564946, 0.01510361861846736681, 0.01589736227876908589, 0.01669110593907080498, 0.01748484959937252059, 0.01827859325967423967, 0.01907233691997595529, 0.01986608058027767437, 0.02065982424057938999, 0.02145356790088110907, 0.02224731156118282815, 0.02304105522148454377, 0.02383479888178626285, 0.02462854254208798194, 0.02542228620238969755 ),
 .UNSPECIFIED. ) ;
#93366=CARTESIAN_POINT ( 'NONE',  ( -1.320432766682874540E-15, -13.90625000204838457, 7.188101187500000044 ) ) ;
#93373=CARTESIAN_POINT ( 'NONE',  ( -8.000000000000000000, -14.93750000409677092, -9.797174393178825657E-16 ) ) ;
#93409=CARTESIAN_POINT ( 'NONE',  ( -5.082755093536326818, -14.09375000204838457, 5.082755093536325042 ) ) ;
#93436=CARTESIAN_POINT ( 'NONE',  ( 2.977408999572651815, -28.43750000204839168, 7.188101187500000933 ) ) ;
#93451=CARTESIAN_POINT ( 'NONE',  ( 8.000000000000000000, -16.99999999999999289, 0.000000000000000000 ) ) ;
#93482=ORIENTED_EDGE ( 'NONE', *, *, #72350, .T. ) ;
#93488=CARTESIAN_POINT ( 'NONE',  ( 2.977408999572652260, -24.31250000204838813, 7.188101187500000044 ) ) ;
#93500=CARTESIAN_POINT ( 'NONE',  ( 2.977408999572651815, -30.31250000204838813, 7.188101187500000933 ) ) ;
#93502=( GEOMETRIC_REPRESENTATION_CONTEXT ( 3 ) GLOBAL_UNCERTAINTY_ASSIGNED_CONTEXT ( ( #47362 ) ) GLOBAL_UNIT_ASSIGNED_CONTEXT ( ( #81869, #74322, #42493 ) ) REPRESENTATION_CONTEXT ( 'NONE', 'WORKASPACE' ) );
#93533=CARTESIAN_POINT ( 'NONE',  ( 5.656854249492380582, -10.81249999999999289, -5.656854249492379694 ) ) ;
#93553=CARTESIAN_POINT ( 'NONE',  ( 2.977408999572650927, -26.37500000204838457, -7.188101187500000933 ) ) ;
#93562=CARTESIAN_POINT ( 'NONE',  ( 5.656854249492378806, -17.37500000409676915, 5.656854249492381470 ) ) ;
#93569=CARTESIAN_POINT ( 'NONE',  ( 6.245865719273044903, -30.00000000000000000, -3.919462879779509024 ) ) ;
#93621=CARTESIAN_POINT ( 'NONE',  ( 4.401442555609581635E-16, -29.28125000204838813, -7.188101187500000044 ) ) ;
#93676=ORIENTED_EDGE ( 'NONE', *, *, #8488, .F. ) ;
#93683=ORIENTED_EDGE ( 'NONE', *, *, #31857, .F. ) ;
#93718=CARTESIAN_POINT ( 'NONE',  ( -9.253817200599836923, 106.2999272991686297, -3.791916801615159649 ) ) ;
#93728=FACE_BOUND ( 'NONE', #7395, .T. ) ;
#93804=CARTESIAN_POINT ( 'NONE',  ( 8.000000000000000000, -21.49999999999999645, 0.000000000000000000 ) ) ;
#93876=CARTESIAN_POINT ( 'NONE',  ( 3.827754797006158505, 15.98931925350938243, -9.240220675753615609 ) ) ;
#93892=CARTESIAN_POINT ( 'NONE',  ( -7.188101187500002709, -15.68750000204838457, 2.977408999572648707 ) ) ;
#93895=AXIS2_PLACEMENT_3D ( 'NONE', #57981, #81710, #40743 ) ;
#93908=CARTESIAN_POINT ( 'NONE',  ( -7.743982712349856357, 88.46213014760739668, 2.020119794285906600 ) ) ;
#93934=CARTESIAN_POINT ( 'NONE',  ( 5.082755093536325930, -13.34375000204838457, -5.082755093536325042 ) ) ;
#93960=EDGE_CURVE ( 'NONE', #78182, #54822, #38473, .T. ) ;
#93965=CARTESIAN_POINT ( 'NONE',  ( -7.188101187500001821, -26.00000000204838457, -2.977408999572651371 ) ) ;
#93979=CARTESIAN_POINT ( 'NONE',  ( 9.253817200599836923, 103.7000727008313845, -3.791916801615160093 ) ) ;
#93984=MECHANICAL_DESIGN_GEOMETRIC_PRESENTATION_REPRESENTATION('',(#102608),#105981);
#93987=( BOUNDED_CURVE ( )  B_SPLINE_CURVE ( 2, ( #26213, #18633, #80540, #14740, #22356, #38525, #29905, #38014, #6121 ),
 .UNSPECIFIED., .F., .F. ) 
 B_SPLINE_CURVE_WITH_KNOTS ( ( 3, 2, 2, 2, 3 ),
 ( 0.5735294117647059542, 0.5808823529411766273, 0.5882352941176471894, 0.5955882352941177516, 0.6029411764705883137 ),
 .UNSPECIFIED. ) 
 CURVE ( )  GEOMETRIC_REPRESENTATION_ITEM ( )  RATIONAL_B_SPLINE_CURVE ( ( 0.9999999999999988898, 0.9238795325112878487, 1.000000000000000000, 0.9238795325112867385, 1.000000000000000000, 0.9238795325112867385, 1.000000000000000000, 0.9238795325112856283, 1.000000000000001110 ) ) 
 REPRESENTATION_ITEM ( '' )  );
#93988=EDGE_CURVE ( 'NONE', #12516, #32331, #40568, .T. ) ;
#93999=VERTEX_POINT ( 'NONE', #16288 ) ;
#94007=CARTESIAN_POINT ( 'NONE',  ( -2.977408999572650039, -26.56250000204838457, -7.188101187500000933 ) ) ;
#94018=CARTESIAN_POINT ( 'NONE',  ( -7.188101187500001821, -32.37500000204838813, -2.977408999572651371 ) ) ;
#94023=CARTESIAN_POINT ( 'NONE',  ( -7.744991119775240129, 108.4643878542513278, -2.016316005557099444 ) ) ;
#94034=DIRECTION ( 'NONE',  ( -0.000000000000000000, 1.000000000000000000, -0.000000000000000000 ) ) ;
#94036=CARTESIAN_POINT ( 'NONE',  ( 4.898587196589412829E-16, -10.81250000409677092, -8.000000000000000000 ) ) ;
#94057=CARTESIAN_POINT ( 'NONE',  ( 5.082755093536324154, -28.71875000204838813, 5.082755093536326818 ) ) ;
#94072=CARTESIAN_POINT ( 'NONE',  ( -2.977408999572654480, -19.62500000204838457, 7.188101187499999156 ) ) ;
#94075=CIRCLE ( 'NONE', #85458, 8.000000000000000000 ) ;
#94083=CARTESIAN_POINT ( 'NONE',  ( -5.656854249492379694, -16.62500000409677270, -5.656854249492380582 ) ) ;
#94089=CARTESIAN_POINT ( 'NONE',  ( -9.253817200599835147, 86.29992729916862970, -3.791916801615157873 ) ) ;
#94096=DIRECTION ( 'NONE',  ( -0.000000000000000000, 1.000000000000000000, -0.000000000000000000 ) ) ;
#94143=CARTESIAN_POINT ( 'NONE',  ( -7.188101187500002709, -24.31250000204838813, 2.977408999572648707 ) ) ;
#94144=ORIENTED_EDGE ( 'NONE', *, *, #65597, .T. ) ;
#94146=CARTESIAN_POINT ( 'NONE',  ( -0.3539438260514402579, 15.11738935797732886, 10.00000000000000000 ) ) ;
#94153=DIRECTION ( 'NONE',  ( 1.000000000000000000, -0.000000000000000000, -0.000000000000000000 ) ) ;
#94187=EDGE_LOOP ( 'NONE', ( #74991, #89544, #63128, #103861 ) ) ;
#94218=CARTESIAN_POINT ( 'NONE',  ( -7.551560007654696705, 101.9908964819301076, -2.648022159607842596 ) ) ;
#94241=CARTESIAN_POINT ( 'NONE',  ( -10.00000000000000000, 15.00000000000000000, 10.00000000000000000 ) ) ;
#94262=CARTESIAN_POINT ( 'NONE',  ( -5.656854249492379694, -24.12500000409677270, -5.656854249492380582 ) ) ;
#94306=DIRECTION ( 'NONE',  ( 0.9090909090909086165, 0.000000000000000000, 0.4165977904505319684 ) ) ;
#94310=( BOUNDED_CURVE ( )  B_SPLINE_CURVE ( 2, ( #61629, #2278, #27687, #94522, #93451, #2821, #52981, #20671, #53512 ),
 .UNSPECIFIED., .F., .F. ) 
 B_SPLINE_CURVE_WITH_KNOTS ( ( 3, 2, 2, 2, 3 ),
 ( 0.6911764705882353921, 0.6985294117647059542, 0.7058823529411766273, 0.7132352941176471894, 0.7205882352941177516 ),
 .UNSPECIFIED. ) 
 CURVE ( )  GEOMETRIC_REPRESENTATION_ITEM ( )  RATIONAL_B_SPLINE_CURVE ( ( 0.9999999999999988898, 0.9238795325112878487, 1.000000000000000000, 0.9238795325112867385, 1.000000000000000000, 0.9238795325112867385, 1.000000000000000000, 0.9238795325112856283, 1.000000000000001110 ) ) 
 REPRESENTATION_ITEM ( '' )  );
#94312=VERTEX_POINT ( 'NONE', #103353 ) ;
#94336=DIRECTION ( 'NONE',  ( -0.000000000000000000, 1.000000000000000000, -0.000000000000000000 ) ) ;
#94346=CARTESIAN_POINT ( 'NONE',  ( 8.000000000000000000, -19.99999999999999289, 0.000000000000000000 ) ) ;
#94400=CARTESIAN_POINT ( 'NONE',  ( -9.797372177749753774, 26.53490505152436185, 2.014953862275842944 ) ) ;
#94437=CARTESIAN_POINT ( 'NONE',  ( 4.401442555609581635E-16, -17.65625000204838813, -7.188101187500000044 ) ) ;
#94477=CARTESIAN_POINT ( 'NONE',  ( 7.188101187500000044, -13.53125000204838457, 0.000000000000000000 ) ) ;
#94508=CARTESIAN_POINT ( 'NONE',  ( 5.082755093536324154, -23.84375000204838457, 5.082755093536326818 ) ) ;
#94522=CARTESIAN_POINT ( 'NONE',  ( 7.999999999999998224, -17.09374999999999289, 3.313708498984766049 ) ) ;
#94526=CARTESIAN_POINT ( 'NONE',  ( 9.165151389911681434, 104.7368049370512040, 4.000000000000002665 ) ) ;
#94560=CARTESIAN_POINT ( 'NONE',  ( -1.320432766682874540E-15, -27.40625000204838813, 7.188101187500000044 ) ) ;
#94569=CARTESIAN_POINT ( 'NONE',  ( -7.188101187500001821, -9.500000002048386349, -2.977408999572651371 ) ) ;
#94586=VERTEX_POINT ( 'NONE', #55305 ) ;
#94611=CARTESIAN_POINT ( 'NONE',  ( 5.082755093536324154, -31.71875000204838457, 5.082755093536326818 ) ) ;
#94627=CARTESIAN_POINT ( 'NONE',  ( 7.188101187500000044, -20.65625000204838813, 0.000000000000000000 ) ) ;
#94636=CARTESIAN_POINT ( 'NONE',  ( 8.000000000000000000, -18.59375000409677270, -3.313708498984761608 ) ) ;
#94639=CARTESIAN_POINT ( 'NONE',  ( 9.403185743875125624, 15.24615751665866981, 3.409011323177099317 ) ) ;
#94661=LINE ( 'NONE', #95699, #646 ) ;
#94680=ORIENTED_EDGE ( 'NONE', *, *, #5600, .T. ) ;
#94698=CARTESIAN_POINT ( 'NONE',  ( 2.977408999572650927, -23.37500000204838813, -7.188101187500001821 ) ) ;
#94713=EDGE_CURVE ( 'NONE', #70179, #44397, #74746, .T. ) ;
#94746=CARTESIAN_POINT ( 'NONE',  ( 0.000000000000000000, 15.00000000000000000, -10.00000000000000000 ) ) ;
#94780=B_SPLINE_CURVE_WITH_KNOTS ( 'NONE', 3,
 ( #77074, #28559, #29625, #53337, #30681, #3731, #13915, #63568, #78133, #12330 ),
 .UNSPECIFIED., .F., .F.,
 ( 4, 2, 2, 2, 4 ),
 ( 0.000000000000000000, 0.001118707926289529489, 0.002237415852579058978, 0.003356123778868585431, 0.004474831705158112752 ),
 .UNSPECIFIED. ) ;
#94793=VERTEX_POINT ( 'NONE', #8085 ) ;
#94795=CARTESIAN_POINT ( 'NONE',  ( -9.698972129396508990, 108.1762971274194030, -2.445345647270322775 ) ) ;
#94807=DIRECTION ( 'NONE',  ( 0.000000000000000000, 1.000000000000000000, 0.000000000000000000 ) ) ;
#94823=AXIS2_PLACEMENT_3D ( 'NONE', #45938, #21173, #86942 ) ;
#94884=CARTESIAN_POINT ( 'NONE',  ( -8.000000000000000000, -19.34374999999999289, -3.313708498984762496 ) ) ;
#94891=ORIENTED_EDGE ( 'NONE', *, *, #103459, .F. ) ;
#94928=CARTESIAN_POINT ( 'NONE',  ( -10.00000000000000355, 85.00000000000000000, 0.000000000000000000 ) ) ;
#94947=ORIENTED_EDGE ( 'NONE', *, *, #59341, .T. ) ;
#94950=CARTESIAN_POINT ( 'NONE',  ( 9.797174393178825657E-16, -30.00000000000000000, -8.000000000000000000 ) ) ;
#94954=CARTESIAN_POINT ( 'NONE',  ( -9.333555687487613994, 103.2189730339102738, 3.591168747312690090 ) ) ;
#94970=CARTESIAN_POINT ( 'NONE',  ( 5.082755093536325930, -14.84375000204838457, -5.082755093536325042 ) ) ;
#95011=CARTESIAN_POINT ( 'NONE',  ( 7.188101187500000044, -15.03125000204838457, 0.000000000000000000 ) ) ;
#95025=CARTESIAN_POINT ( 'NONE',  ( 5.656854249492378806, -29.18749999999999645, 5.656854249492381470 ) ) ;
#95038=CARTESIAN_POINT ( 'NONE',  ( 7.188101187500000044, -17.65625000204838457, 0.000000000000000000 ) ) ;
#95079=STYLED_ITEM ( 'NONE', ( #31646 ), #104567 ) ;
#95087=CARTESIAN_POINT ( 'NONE',  ( -2.977408999572650039, -19.06250000204838102, -7.188101187500000933 ) ) ;
#95094=CARTESIAN_POINT ( 'NONE',  ( -5.082755093536326818, -32.09375000204838813, 5.082755093536325042 ) ) ;
#95100=CARTESIAN_POINT ( 'NONE',  ( -7.986452802927059835, 108.9730975769188461, 0.5332468218996380127 ) ) ;
#95113=CARTESIAN_POINT ( 'NONE',  ( 4.898587196589412829E-16, -22.81250000409677270, -8.000000000000000000 ) ) ;
#95135=CARTESIAN_POINT ( 'NONE',  ( -7.188101187500000044, -30.78125000204838813, -8.802885111219163269E-16 ) ) ;
#95147=CARTESIAN_POINT ( 'NONE',  ( -2.977408999572650039, -21.68750000204838813, -7.188101187500000933 ) ) ;
#95156=CARTESIAN_POINT ( 'NONE',  ( -3.313708498984765161, -11.65625000409677092, 7.999999999999998224 ) ) ;
#95158=CARTESIAN_POINT ( 'NONE',  ( 9.999999999999996447, 15.00000000000000000, 4.397168787612224072 ) ) ;
#95210=CARTESIAN_POINT ( 'NONE',  ( -10.00000000000000355, 15.00000000000000000, -10.00000000000000000 ) ) ;
#95217=CARTESIAN_POINT ( 'NONE',  ( -1.320432766682874540E-15, -27.03125000204838813, 7.188101187500000044 ) ) ;
#95219=CARTESIAN_POINT ( 'NONE',  ( 7.999999999999998224, -20.28125000409677625, 3.313708498984766049 ) ) ;
#95236=DIRECTION ( 'NONE',  ( -0.9090909090909090606, 0.000000000000000000, 0.4165977904505314133 ) ) ;
#95247=( BOUNDED_CURVE ( )  B_SPLINE_CURVE ( 2, ( #17032, #82817, #8916, #73645, #32157, #65036, #24084, #56925, #106549 ),
 .UNSPECIFIED., .F., .F. ) 
 B_SPLINE_CURVE_WITH_KNOTS ( ( 3, 2, 2, 2, 3 ),
 ( 0.6911764705882352811, 0.6985294117647058432, 0.7058823529411765163, 0.7132352941176470784, 0.7205882352941176405 ),
 .UNSPECIFIED. ) 
 CURVE ( )  GEOMETRIC_REPRESENTATION_ITEM ( )  RATIONAL_B_SPLINE_CURVE ( ( 1.000000000000000000, 0.9238795325112867385, 1.000000000000000000, 0.9238795325112867385, 1.000000000000000000, 0.9238795325112867385, 1.000000000000000000, 0.9238795325112867385, 1.000000000000000000 ) ) 
 REPRESENTATION_ITEM ( '' )  );
#95265=CARTESIAN_POINT ( 'NONE',  ( -2.450449656239130025, 15.75130202679986269, -9.701736001019305888 ) ) ;
#95268=EDGE_CURVE ( 'NONE', #62970, #1839, #70853, .T. ) ;
#95285=CARTESIAN_POINT ( 'NONE',  ( 9.701712097384767475, 15.75132464342601146, 2.450541714948253347 ) ) ;
#95339=DIRECTION ( 'NONE',  ( -1.734723475976807094E-16, -0.000000000000000000, -1.000000000000000000 ) ) ;
#95394=CARTESIAN_POINT ( 'NONE',  ( 7.999999999999998224, -18.59374999999998934, 3.313708498984766493 ) ) ;
#95397=ORIENTED_EDGE ( 'NONE', *, *, #11285, .F. ) ;
#95401=EDGE_LOOP ( 'NONE', ( #93482, #59473, #68277, #1400 ) ) ;
#95423=ORIENTED_EDGE ( 'NONE', *, *, #73497, .F. ) ;
#95441=CARTESIAN_POINT ( 'NONE',  ( -9.843481099141454749, 26.40795443846614532, -1.779148000612201574 ) ) ;
#95442=CARTESIAN_POINT ( 'NONE',  ( -1.469576158976823947E-15, -26.37499999999999645, 8.000000000000000000 ) ) ;
#95477=CARTESIAN_POINT ( 'NONE',  ( 7.188101187500000044, -16.53125000204838813, 0.000000000000000000 ) ) ;
#95483=EDGE_CURVE ( 'NONE', #29729, #93035, #20769, .T. ) ;
#95512=CARTESIAN_POINT ( 'NONE',  ( 7.414580834929598296, 32.64656280281481315, 3.010264818013836052 ) ) ;
#95515=CARTESIAN_POINT ( 'NONE',  ( -7.046357527897572304, 28.69384349398995937, -3.789683693877204718 ) ) ;
#95522=CARTESIAN_POINT ( 'NONE',  ( 5.082755093536325930, -11.84375000204838635, -5.082755093536325042 ) ) ;
#95548=CARTESIAN_POINT ( 'NONE',  ( -5.082755093536326818, -19.71875000204838457, 5.082755093536325042 ) ) ;
#95601=CARTESIAN_POINT ( 'NONE',  ( -7.188101187500000933, -20.37500000204838813, -2.977408999572651371 ) ) ;
#95609=CARTESIAN_POINT ( 'NONE',  ( -7.188101187500002709, -32.18750000204838813, 2.977408999572648707 ) ) ;
#95614=CARTESIAN_POINT ( 'NONE',  ( -6.928203230275507885, 105.0000000000000000, -4.000000000000001776 ) ) ;
#95655=CARTESIAN_POINT ( 'NONE',  ( 2.977408999572650927, -34.25000000204838813, -7.188101187500001821 ) ) ;
#95666=CARTESIAN_POINT ( 'NONE',  ( -5.082755093536326818, -19.71875000204838457, 5.082755093536325042 ) ) ;
#95672=CARTESIAN_POINT ( 'NONE',  ( -9.797372177749751998, 81.53490505152436185, 2.014953862275846497 ) ) ;
#95675=CARTESIAN_POINT ( 'NONE',  ( -5.656854249492381470, -11.75000000409677092, 5.656854249492379694 ) ) ;
#95678=EDGE_CURVE ( 'NONE', #66787, #4323, #78404, .T. ) ;
#95680=FILL_AREA_STYLE ('',( #30438 ) ) ;
#95686=CARTESIAN_POINT ( 'NONE',  ( -1.544939622599249551, 15.00000000000000000, 9.999999999999998224 ) ) ;
#95699=CARTESIAN_POINT ( 'NONE',  ( -10.00000000000000355, 105.0000000000000000, 4.000000000000001776 ) ) ;
#95738=CYLINDRICAL_SURFACE ( 'NONE', #98363, 4.000000000000000000 ) ;
#95739=CARTESIAN_POINT ( 'NONE',  ( 4.401442555609581635E-16, -23.28125000204838457, -7.188101187500000044 ) ) ;
#95743=CARTESIAN_POINT ( 'NONE',  ( -1.469576158976823947E-15, -25.06250000409677270, 8.000000000000000000 ) ) ;
#95813=CARTESIAN_POINT ( 'NONE',  ( 5.656854249492380582, -27.50000000409677270, -5.656854249492379694 ) ) ;
#95880=CARTESIAN_POINT ( 'NONE',  ( 0.000000000000000000, 115.0000000000000000, -8.000000000000000000 ) ) ;
#95904=LINE ( 'NONE', #14423, #61135 ) ;
#95918=TOROIDAL_SURFACE ( 'NONE', #49375, 11.00000000000000000, 1.000000000000000000 ) ;
#95923=CARTESIAN_POINT ( 'NONE',  ( -8.000000000000000000, -10.53125000409677092, -3.313708498984762496 ) ) ;
#95927=DIRECTION ( 'NONE',  ( -0.000000000000000000, 1.000000000000000000, -0.000000000000000000 ) ) ;
#95931=CARTESIAN_POINT ( 'NONE',  ( 4.898587196589412829E-16, -12.12499999999999289, -8.000000000000000000 ) ) ;
#95947=VECTOR ( 'NONE', #102760, 1000.000000000000000 ) ;
#95968=ADVANCED_FACE ( 'NONE', ( #79213 ), #30698, .T. ) ;
#95981=CARTESIAN_POINT ( 'NONE',  ( -9.948688207305192321, 26.12976850509815918, -1.044946705213435134 ) ) ;
#95996=CARTESIAN_POINT ( 'NONE',  ( -9.168149550320913832, 15.99999999372935022, -3.997425403568243496 ) ) ;
#96003=( NAMED_UNIT ( * ) PLANE_ANGLE_UNIT ( ) SI_UNIT ( $, .RADIAN. ) );
#96012=CARTESIAN_POINT ( 'NONE',  ( 0.000000000000000000, -30.00000000000000000, 0.000000000000000000 ) ) ;
#96017=LINE ( 'NONE', #87926, #90475 ) ;
#96053=CARTESIAN_POINT ( 'NONE',  ( -7.344361273354515163, 27.55439469411475173, -3.175733139645582792 ) ) ;
#96054=ORIENTED_EDGE ( 'NONE', *, *, #69423, .T. ) ;
#96059=CARTESIAN_POINT ( 'NONE',  ( 8.000000000000000000, -34.99999999999999289, 0.000000000000000000 ) ) ;
#96062=CARTESIAN_POINT ( 'NONE',  ( -7.619135598915500296, 101.8269463221532334, 2.449260492474796713 ) ) ;
#96083=CARTESIAN_POINT ( 'NONE',  ( -2.977408999572650039, -17.18750000204838813, -7.188101187500001821 ) ) ;
#96134=CARTESIAN_POINT ( 'NONE',  ( -5.082755093536326818, -17.09375000204838813, 5.082755093536325042 ) ) ;
#96136=CARTESIAN_POINT ( 'NONE',  ( -1.469576158976823947E-15, -11.56250000409677092, 8.000000000000000000 ) ) ;
#96140=ORIENTED_EDGE ( 'NONE', *, *, #64416, .T. ) ;
#96145=CARTESIAN_POINT ( 'NONE',  ( -7.188101187500002709, -26.18750000204838813, 2.977408999572648707 ) ) ;
#96192=CARTESIAN_POINT ( 'NONE',  ( 4.401442555609581635E-16, -34.15625000204838813, -7.188101187500000044 ) ) ;
#96195=EDGE_CURVE ( 'NONE', #48348, #71070, #53747, .T. ) ;
#96207=CARTESIAN_POINT ( 'NONE',  ( 4.401442555609581635E-16, -18.78125000204838457, -7.188101187500000044 ) ) ;
#96219=CARTESIAN_POINT ( 'NONE',  ( 8.000000000000000000, -9.687500004096769146, 0.000000000000000000 ) ) ;
#96227=FACE_OUTER_BOUND ( 'NONE', #77994, .T. ) ;
#96229=CARTESIAN_POINT ( 'NONE',  ( -9.645512969475854348, 33.01103150675724152, -2.645801731561393311 ) ) ;
#96232=CARTESIAN_POINT ( 'NONE',  ( -3.316968746324298500, 15.92795519102023860, 9.435590127032945418 ) ) ;
#96288=CARTESIAN_POINT ( 'NONE',  ( -7.188101187500002709, -22.81250000204838813, 2.977408999572648707 ) ) ;
#96350=CARTESIAN_POINT ( 'NONE',  ( -8.000000000000001776, -31.34375000409677270, 3.313708498984758943 ) ) ;
#96359=SURFACE_STYLE_USAGE ( .BOTH. , #31624 ) ;
#96371=EDGE_CURVE ( 'NONE', #54845, #15011, #29338, .T. ) ;
#96386=VERTEX_POINT ( 'NONE', #75506 ) ;
#96394=CARTESIAN_POINT ( 'NONE',  ( -4.931706463495239667, -29.99999999999998579, 5.709552341500299555 ) ) ;
#96414=CARTESIAN_POINT ( 'NONE',  ( -10.00000000000000355, 105.0000000000000000, -4.000000000000001776 ) ) ;
#96428=ORIENTED_EDGE ( 'NONE', *, *, #31487, .T. ) ;
#96430=EDGE_LOOP ( 'NONE', ( #60564, #32276, #73317, #48536 ) ) ;
#96434=EDGE_CURVE ( 'NONE', #54191, #30765, #12865, .T. ) ;
#96460=EDGE_CURVE ( 'NONE', #31698, #4323, #34963, .T. ) ;
#96468=CARTESIAN_POINT ( 'NONE',  ( -1.469576158976823947E-15, -14.37499999999999112, 8.000000000000000000 ) ) ;
#96470=VECTOR ( 'NONE', #1189, 1000.000000000000000 ) ;
#96513=EDGE_LOOP ( 'NONE', ( #35530, #27877, #33778 ) ) ;
#96514=CARTESIAN_POINT ( 'NONE',  ( 8.000000000000000000, -27.59375000409677270, -3.313708498984761164 ) ) ;
#96515=CARTESIAN_POINT ( 'NONE',  ( -9.907647895771706459, 15.45478884909084272, 1.400734872026643041 ) ) ;
#96548=CARTESIAN_POINT ( 'NONE',  ( -5.082755093536326818, -11.09375000204838457, 5.082755093536325042 ) ) ;
#96583=CARTESIAN_POINT ( 'NONE',  ( 7.999885325681426629, 33.99977065129937159, 0.2682325777720087623 ) ) ;
#96584=CARTESIAN_POINT ( 'NONE',  ( -7.999885325681428405, 26.00022934870063551, 0.2682325777720080962 ) ) ;
#96590=CARTESIAN_POINT ( 'NONE',  ( 8.000000000000000000, -33.49999999999999289, 0.000000000000000000 ) ) ;
#96614=CARTESIAN_POINT ( 'NONE',  ( 4.401442555609581635E-16, -21.78125000204838457, -7.188101187500000044 ) ) ;
#96662=CARTESIAN_POINT ( 'NONE',  ( -5.082755093536325042, -20.46875000204838813, -5.082755093536325930 ) ) ;
#96671=CARTESIAN_POINT ( 'NONE',  ( 7.188101187499999156, -25.62500000204838813, 2.977408999572654924 ) ) ;
#96709=ORIENTED_EDGE ( 'NONE', *, *, #49927, .F. ) ;
#96714=CARTESIAN_POINT ( 'NONE',  ( -1.320432766682874540E-15, -22.90625000204838457, 7.188101187500000044 ) ) ;
#96719=ADVANCED_FACE ( 'NONE', ( #35496 ), #68372, .F. ) ;
#96721=FACE_OUTER_BOUND ( 'NONE', #95401, .T. ) ;
#96731=CARTESIAN_POINT ( 'NONE',  ( 2.977408999572652260, -11.93750000204838635, 7.188101187500000044 ) ) ;
#96744=CARTESIAN_POINT ( 'NONE',  ( -3.313708498984760720, -12.21875000409676737, -8.000000000000000000 ) ) ;
#96749=SURFACE_STYLE_FILL_AREA ( #95680 ) ;
#96805=CARTESIAN_POINT ( 'NONE',  ( -2.977408999572654480, -21.12500000204838813, 7.188101187499999156 ) ) ;
#96808=CARTESIAN_POINT ( 'NONE',  ( 9.948561005166130400, 81.13009726251802078, -1.045755304005129505 ) ) ;
#96811=CARTESIAN_POINT ( 'NONE',  ( -5.656854249492379694, -13.62500000409676915, -5.656854249492380582 ) ) ;
#96815=LINE ( 'NONE', #105430, #14757 ) ;
#96834=( BOUNDED_CURVE ( )  B_SPLINE_CURVE ( 2, ( #32317, #24232, #89994, #81882, #8003, #40913, #73804, #84970, #43978 ),
 .UNSPECIFIED., .F., .F. ) 
 B_SPLINE_CURVE_WITH_KNOTS ( ( 3, 2, 2, 2, 3 ),
 ( 0.1960366238535917460, 0.1985294117647058709, 0.2058823529411764885, 0.2132352941176470784, 0.2205882352941176960 ),
 .UNSPECIFIED. ) 
 CURVE ( )  GEOMETRIC_REPRESENTATION_ITEM ( )  RATIONAL_B_SPLINE_CURVE ( ( 0.9658850645339884800, 0.9741937033643860433, 1.000000000000000000, 0.9238795325112867385, 1.000000000000000000, 0.9238795325112867385, 1.000000000000000000, 0.9238795325112861834, 1.000000000000000666 ) ) 
 REPRESENTATION_ITEM ( '' )  );
#96862=CARTESIAN_POINT ( 'NONE',  ( 7.188101187500000044, -28.15625000204838813, 0.000000000000000000 ) ) ;
#96867=CARTESIAN_POINT ( 'NONE',  ( -8.000000000000000000, -26.93750000409677625, -9.797174393178825657E-16 ) ) ;
#96884=EDGE_CURVE ( 'NONE', #94312, #699, #57380, .T. ) ;
#96888=CARTESIAN_POINT ( 'NONE',  ( -9.435590127033082197, 15.92795519102023860, 3.316968746323895267 ) ) ;
#96910=CARTESIAN_POINT ( 'NONE',  ( 0.000000000000000000, 115.0000000000000000, 0.000000000000000000 ) ) ;
#96987=CARTESIAN_POINT ( 'NONE',  ( 5.656854249492380582, -15.31249999999999289, -5.656854249492379694 ) ) ;
#97013=AXIS2_PLACEMENT_3D ( 'NONE', #53525, #86454, #104184 ) ;
#97031=EDGE_LOOP ( 'NONE', ( #21561, #94680, #65808, #92243 ) ) ;
#97040=CARTESIAN_POINT ( 'NONE',  ( -9.403185743875484448, 15.24615751665884389, -3.409011323176772912 ) ) ;
#97069=ORIENTED_EDGE ( 'NONE', *, *, #60368, .T. ) ;
#97070=ORIENTED_EDGE ( 'NONE', *, *, #42075, .F. ) ;
#97104=CARTESIAN_POINT ( 'NONE',  ( 5.082755093536325930, -10.34375000204838457, -5.082755093536325042 ) ) ;
#97128=CARTESIAN_POINT ( 'NONE',  ( -7.188101187500000044, -18.40625000204838457, -8.802885111219163269E-16 ) ) ;
#97147=CYLINDRICAL_SURFACE ( 'NONE', #51181, 8.000000000000000000 ) ;
#97173=CARTESIAN_POINT ( 'NONE',  ( 7.188101187500000933, -20.93750000204839168, -2.977408999572650483 ) ) ;
#97185=CARTESIAN_POINT ( 'NONE',  ( -2.977408999572650039, -29.56250000204838813, -7.188101187500001821 ) ) ;
#97219=AXIS2_PLACEMENT_3D ( 'NONE', #79033, #5153, #39122 ) ;
#97226=CARTESIAN_POINT ( 'NONE',  ( 7.188101187500001821, -22.43750000204838813, -2.977408999572650483 ) ) ;
#97243=CARTESIAN_POINT ( 'NONE',  ( 4.401442555609581635E-16, -14.28125000204838457, -7.188101187500000044 ) ) ;
#97244=CARTESIAN_POINT ( 'NONE',  ( 7.744991119775241017, 26.53561214574870064, -2.016316005557097224 ) ) ;
#97253=CARTESIAN_POINT ( 'NONE',  ( -8.000000000000000000, -19.24999999999999289, -9.797174393178825657E-16 ) ) ;
#97257=CARTESIAN_POINT ( 'NONE',  ( 8.000000000000000000, -14.09375000409676915, -3.313708498984761608 ) ) ;
#97261=CARTESIAN_POINT ( 'NONE',  ( -9.333079356992097786, 86.77833080074870509, 3.592383266237784589 ) ) ;
#97315=CARTESIAN_POINT ( 'NONE',  ( -2.977408999572650039, -20.18750000204838457, -7.188101187500001821 ) ) ;
#97318=CARTESIAN_POINT ( 'NONE',  ( 9.842473135306409660, 81.41068182886414206, 1.785129593756284772 ) ) ;
#97363=B_SPLINE_CURVE_WITH_KNOTS ( 'NONE', 3,
 ( #33340, #48419, #7961, #25252, #58111, #42461, #17673, #66749, #50020, #41932, #96062, #99635, #22194, #106118, #32271, #98045, #40872, #73761, #52146, #20384, #28446, #35479, #101767, #19839, #94218, #69419, #27933, #67814, #26864, #51614, #84534, #27403, #26338, #102300 ),
 .UNSPECIFIED., .F., .F.,
 ( 4, 2, 2, 2, 2, 2, 2, 2, 2, 2, 2, 2, 2, 2, 2, 2, 4 ),
 ( 0.01272238763756221823, 0.01351613129786393731, 0.01430987495816565813, 0.01510361861846737722, 0.01589736227876909630, 0.01669110593907081538, 0.01748484959937253447, 0.01827859325967425702, 0.01907233691997597264, 0.01986608058027769519, 0.02065982424057941080, 0.02145356790088112989, 0.02224731156118284550, 0.02304105522148456459, 0.02383479888178628020, 0.02462854254208799581, 0.02542228620238971143 ),
 .UNSPECIFIED. ) ;
#97373=CARTESIAN_POINT ( 'NONE',  ( -8.000000000000000000, -28.43750000409677270, -9.797174393178825657E-16 ) ) ;
#97378=CARTESIAN_POINT ( 'NONE',  ( 9.989690267985800176, 33.97444416594910876, -0.5238310916885827728 ) ) ;
#97381=ORIENTED_EDGE ( 'NONE', *, *, #41896, .F. ) ;
#97399=CARTESIAN_POINT ( 'NONE',  ( 5.656854249492378806, -12.68749999999999467, 5.656854249492381470 ) ) ;
#97407=ADVANCED_FACE ( 'NONE', ( #101619 ), #78924, .T. ) ;
#97427=CARTESIAN_POINT ( 'NONE',  ( 3.572352985695675276, 15.21714514899109894, 9.341953373613073097 ) ) ;
#97453=DIRECTION ( 'NONE',  ( -0.000000000000000000, -1.000000000000000000, -0.000000000000000000 ) ) ;
#97464=CARTESIAN_POINT ( 'NONE',  ( 7.344505440741524893, 102.5538107270129586, -3.175463080953002226 ) ) ;
#97485=CARTESIAN_POINT ( 'NONE',  ( -1.469576158976823947E-15, -10.06250000409677092, 8.000000000000000000 ) ) ;
#97488=CARTESIAN_POINT ( 'NONE',  ( 0.000000000000000000, -30.00000000000000000, 8.000000000000000000 ) ) ;
#97492=CARTESIAN_POINT ( 'NONE',  ( -8.000000000000000000, -13.34374999999999467, -3.313708498984762496 ) ) ;
#97517=CARTESIAN_POINT ( 'NONE',  ( 9.999999999999998224, 15.00000000000000000, -2.832769448823991188E-15 ) ) ;
#97557=SURFACE_STYLE_USAGE ( .BOTH. , #77690 ) ;
#97566=CARTESIAN_POINT ( 'NONE',  ( 3.313708498984743844, -27.78124999999999645, 8.000000000000017764 ) ) ;
#97621=CARTESIAN_POINT ( 'NONE',  ( -8.000000000000000000, -32.74999999999999289, -9.797174393178825657E-16 ) ) ;
#97629=AXIS2_PLACEMENT_3D ( 'NONE', #33667, #57903, #15866 ) ;
#97641=CARTESIAN_POINT ( 'NONE',  ( 7.045755811259133417, 106.3034160301355513, 3.790843699961855773 ) ) ;
#97645=CARTESIAN_POINT ( 'NONE',  ( -7.188101187500000044, -15.40625000204838635, -8.802885111219163269E-16 ) ) ;
#97672=VECTOR ( 'NONE', #81253, 1000.000000000000000 ) ;
#97700=CARTESIAN_POINT ( 'NONE',  ( -2.977408999572654480, -12.50000000204838813, 7.188101187499999156 ) ) ;
#97707=CARTESIAN_POINT ( 'NONE',  ( 5.082755093536324154, -28.71875000204838813, 5.082755093536326818 ) ) ;
#97710=CARTESIAN_POINT ( 'NONE',  ( -2.977408999572650039, -25.06250000204838457, -7.188101187500001821 ) ) ;
#97744=VERTEX_POINT ( 'NONE', #83976 ) ;
#97750=CARTESIAN_POINT ( 'NONE',  ( 2.977408999572650927, -26.75000000204838457, -7.188101187500001821 ) ) ;
#97766=CARTESIAN_POINT ( 'NONE',  ( -7.188101187500000933, -14.00000000204838457, -2.977408999572651371 ) ) ;
#97767=CARTESIAN_POINT ( 'NONE',  ( 7.046289519167717508, 28.69408180055621926, -3.789821819998816732 ) ) ;
#97781=CARTESIAN_POINT ( 'NONE',  ( 7.188101187499999156, -29.75000000204838813, 2.977408999572654924 ) ) ;
#97785=CARTESIAN_POINT ( 'NONE',  ( -9.536842176398147686, 87.64235369883989790, 3.014135744008184847 ) ) ;
#97848=CARTESIAN_POINT ( 'NONE',  ( 2.977408999572650927, -18.87500000204838457, -7.188101187500001821 ) ) ;
#97861=EDGE_CURVE ( 'NONE', #87634, #47033, #63448, .T. ) ;
#97913=CARTESIAN_POINT ( 'NONE',  ( 7.999999999999998224, -32.28125000409677625, 3.313708498984766493 ) ) ;
#97918=CARTESIAN_POINT ( 'NONE',  ( 9.165151389911679658, 30.00000000000000000, 4.000000000000000000 ) ) ;
#97934=B_SPLINE_CURVE_WITH_KNOTS ( 'NONE', 3,
 ( #33708, #67659, #92438, #100538, #1831, #35316, #49861, #50912, #42302, #58502, #51984, #91407, #68734, #84901, #34252, #75189, #82767, #59036, #2370, #101075, #84371, #27235, #10462, #83822, #67124, #34788, #50382, #99465, #75735, #17521, #26701, #76264, #83295, #68180 ),
 .UNSPECIFIED., .F., .F.,
 ( 4, 2, 2, 2, 2, 2, 2, 2, 2, 2, 2, 2, 2, 2, 2, 2, 4 ),
 ( 0.000000000000000000, 0.0007951492273476383141, 0.001590298454695276628, 0.002385447682042914942, 0.003180596909390553256, 0.003975746136738191570, 0.004770895364085829884, 0.005566044591433468199, 0.006361193818781106513, 0.007156343046128744827, 0.007951492273476383141, 0.008746641500824020588, 0.009541790728171659769, 0.01033693995551929895, 0.01113208918286693640, 0.01192723841021457384, 0.01272238763756221303 ),
 .UNSPECIFIED. ) ;
#97941=( LENGTH_UNIT ( ) NAMED_UNIT ( * ) SI_UNIT ( .MILLI., .METRE. ) );
#97954=ORIENTED_EDGE ( 'NONE', *, *, #42489, .F. ) ;
#97997=CARTESIAN_POINT ( 'NONE',  ( 0.000000000000000000, -30.00000000000000000, 0.000000000000000000 ) ) ;
#98008=CARTESIAN_POINT ( 'NONE',  ( 7.800703710507054467, 101.4140430734205722, 1.791736796405269505 ) ) ;
#98028=COLOUR_RGB ( '', 0.31764706, 0.68627451, 0.89019608) ;
#98041=CARTESIAN_POINT ( 'NONE',  ( -8.000000000000000000, -14.84374999999999112, -3.313708498984762496 ) ) ;
#98045=CARTESIAN_POINT ( 'NONE',  ( -7.986468734911285949, 101.0268632027691922, 0.5341897780976139209 ) ) ;
#98052=EDGE_CURVE ( 'NONE', #62602, #31698, #78400, .T. ) ;
#98066=CARTESIAN_POINT ( 'NONE',  ( 9.403185743875306812, 15.24615751665919916, -3.409011323176907027 ) ) ;
#98088=CARTESIAN_POINT ( 'NONE',  ( -9.246279647933185686, 16.00000000000000000, 3.826931552919418777 ) ) ;
#98103=CARTESIAN_POINT ( 'NONE',  ( -9.999999999999998224, 15.00000000000000000, 1.836970198721029589E-15 ) ) ;
#98105=CARTESIAN_POINT ( 'NONE',  ( 2.977408999572651815, -29.93750000204839523, 7.188101187500000933 ) ) ;
#98164=CARTESIAN_POINT ( 'NONE',  ( -8.000000000000000000, -34.24999999999999289, -9.797174393178825657E-16 ) ) ;
#98189=CARTESIAN_POINT ( 'NONE',  ( -7.188101187500002709, -12.31250000204838635, 2.977408999572648707 ) ) ;
#98204=VECTOR ( 'NONE', #84406, 1000.000000000000000 ) ;
#98234=EDGE_CURVE ( 'NONE', #57343, #99482, #92879, .T. ) ;
#98243=CARTESIAN_POINT ( 'NONE',  ( 2.977408999572652260, -15.31250000204838813, 7.188101187500000044 ) ) ;
#98250=CARTESIAN_POINT ( 'NONE',  ( 5.082755093536325930, -29.84375000204838813, -5.082755093536325042 ) ) ;
#98253=CARTESIAN_POINT ( 'NONE',  ( -5.082755093536325042, -29.46875000204838813, -5.082755093536325930 ) ) ;
#98295=CARTESIAN_POINT ( 'NONE',  ( -2.977408999572650039, -23.56250000204839168, -7.188101187500001821 ) ) ;
#98308=CARTESIAN_POINT ( 'NONE',  ( 9.333555687487612218, 86.78102696608972622, 3.591168747312686982 ) ) ;
#98313=CARTESIAN_POINT ( 'NONE',  ( -1.320432766682874540E-15, -12.03125000204838635, 7.188101187500000044 ) ) ;
#98314=CARTESIAN_POINT ( 'NONE',  ( 6.943482370013980720, 29.47151629739275691, 3.973876482044365499 ) ) ;
#98325=CARTESIAN_POINT ( 'NONE',  ( 4.401442555609581635E-16, -32.28125000204838813, -7.188101187500000044 ) ) ;
#98335=VECTOR ( 'NONE', #93123, 1000.000000000000000 ) ;
#98340=CARTESIAN_POINT ( 'NONE',  ( 5.656854249492378806, -9.875000004096769146, 5.656854249492381470 ) ) ;
#98356=LINE ( 'NONE', #16923, #16473 ) ;
#98363=AXIS2_PLACEMENT_3D ( 'NONE', #63916, #80594, #31557 ) ;
#98372=CARTESIAN_POINT ( 'NONE',  ( 6.928203230275509661, 85.26479267253573369, 3.999999999999999112 ) ) ;
#98377=CARTESIAN_POINT ( 'NONE',  ( 6.928203230275510549, 85.00000000000000000, 4.000000000000000000 ) ) ;
#98380=CARTESIAN_POINT ( 'NONE',  ( -7.188101187500000044, -21.40625000204838457, -8.802885111219163269E-16 ) ) ;
#98418=DIRECTION ( 'NONE',  ( -0.000000000000000000, 1.000000000000000000, -0.000000000000000000 ) ) ;
#98443=CARTESIAN_POINT ( 'NONE',  ( 7.999999999999998224, -26.28125000409677270, 3.313708498984766493 ) ) ;
#98450=CARTESIAN_POINT ( 'NONE',  ( -2.802461721337844658, 15.83563386295778308, -9.606080321247102205 ) ) ;
#98483=CARTESIAN_POINT ( 'NONE',  ( 4.898587196589412829E-16, -28.81250000409677270, -8.000000000000000000 ) ) ;
#98487=CARTESIAN_POINT ( 'NONE',  ( -7.893907107745417484, -29.99999999999998934, 0.07081340544336872656 ) ) ;
#98518=ADVANCED_FACE ( 'NONE', ( #65815 ), #35074, .T. ) ;
#98519=SURFACE_SIDE_STYLE ('',( #7911 ) ) ;
#98523=CARTESIAN_POINT ( 'NONE',  ( -3.313708498984760276, -28.71875000409677625, -8.000000000000000000 ) ) ;
#98534=CARTESIAN_POINT ( 'NONE',  ( 8.000086790516061086, 100.9998264189399322, 0.2639471549312805698 ) ) ;
#98542=CARTESIAN_POINT ( 'NONE',  ( 9.381593208289373820, 107.0143863811950666, -3.465401811657803144 ) ) ;
#98557=ORIENTED_EDGE ( 'NONE', *, *, #76286, .F. ) ;
#98594=AXIS2_PLACEMENT_3D ( 'NONE', #35857, #19148, #91923 ) ;
#98598=CARTESIAN_POINT ( 'NONE',  ( -7.551892080562057075, 81.99012297460615173, 2.647003822403972695 ) ) ;
#98628=CARTESIAN_POINT ( 'NONE',  ( -7.188101187500002709, -33.31250000204838813, 2.977408999572648707 ) ) ;
#98682=CARTESIAN_POINT ( 'NONE',  ( 5.656854249492380582, -28.81249999999999289, -5.656854249492379694 ) ) ;
#98705=CARTESIAN_POINT ( 'NONE',  ( 2.977408999572651815, -13.43750000204838457, 7.188101187500000933 ) ) ;
#98760=CARTESIAN_POINT ( 'NONE',  ( -2.977408999572650039, -14.56250000204838457, -7.188101187500000933 ) ) ;
#98764=CARTESIAN_POINT ( 'NONE',  ( 6.006401927973604060, -30.00000000000000355, 3.977000602544253027 ) ) ;
#98770=CARTESIAN_POINT ( 'NONE',  ( -5.082755093536325042, -20.46875000204838813, -5.082755093536325930 ) ) ;
#98812=CARTESIAN_POINT ( 'NONE',  ( -7.188101187500000044, -24.78125000204838813, -8.802885111219163269E-16 ) ) ;
#98825=CARTESIAN_POINT ( 'NONE',  ( 7.551437640244097693, 26.99127537477090399, -2.648272645923380519 ) ) ;
#98835=CARTESIAN_POINT ( 'NONE',  ( 7.188101187500001821, -34.06250000204839523, -2.977408999572650483 ) ) ;
#98843=CARTESIAN_POINT ( 'NONE',  ( -9.221249107921748234, 31.04821371498486471, 3.869340886054256856 ) ) ;
#98866=ADVANCED_FACE ( 'NONE', ( #25122 ), #106533, .T. ) ;
#98882=CARTESIAN_POINT ( 'NONE',  ( 6.928203230275510549, 85.00000000000000000, 4.000000000000000000 ) ) ;
#98894=CARTESIAN_POINT ( 'NONE',  ( 7.188101187500001821, -19.06250000204838813, -2.977408999572650483 ) ) ;
#98897=CARTESIAN_POINT ( 'NONE',  ( 9.253817200599835147, 83.70007270083139872, -3.791916801615157873 ) ) ;
#98949=CARTESIAN_POINT ( 'NONE',  ( 4.401442555609581635E-16, -29.28125000204838813, -7.188101187500000044 ) ) ;
#98959=CARTESIAN_POINT ( 'NONE',  ( -8.000000000000000000, -22.53125000409677980, -3.313708498984762496 ) ) ;
#98963=CARTESIAN_POINT ( 'NONE',  ( 9.165151389911679658, 30.26295510916337150, 3.999999999999999112 ) ) ;
#98990=CARTESIAN_POINT ( 'NONE',  ( 8.000000000000000000, -12.40624999999999289, -3.313708498984761164 ) ) ;
#99006=ORIENTED_EDGE ( 'NONE', *, *, #98234, .F. ) ;
#99041=CARTESIAN_POINT ( 'NONE',  ( -3.313708498984756723, -28.15625000409677270, 8.000000000000008882 ) ) ;
#99053=CARTESIAN_POINT ( 'NONE',  ( 7.046289519167718396, 103.6940818005561908, -3.789821819998814512 ) ) ;
#99088=CARTESIAN_POINT ( 'NONE',  ( -4.912105445019744998, -10.03270236560008932, 6.401603053965017054 ) ) ;
#99121=CARTESIAN_POINT ( 'NONE',  ( -7.151597709147946347, 83.21070734947782910, 3.587174531012138790 ) ) ;
#99158=CARTESIAN_POINT ( 'NONE',  ( 2.977408999572651815, -31.43750000204839168, 7.188101187500000933 ) ) ;
#99162=ADVANCED_FACE ( 'NONE', ( #54658 ), #89436, .F. ) ;
#99190=CARTESIAN_POINT ( 'NONE',  ( 5.656854249492378806, -29.37500000409677270, 5.656854249492381470 ) ) ;
#99215=CARTESIAN_POINT ( 'NONE',  ( 7.999999999999998224, -27.59374999999999289, 3.313708498984766493 ) ) ;
#99219=ORIENTED_EDGE ( 'NONE', *, *, #77049, .T. ) ;
#99237=CARTESIAN_POINT ( 'NONE',  ( 7.188101187499999156, -11.75000000204838813, 2.977408999572654924 ) ) ;
#99291=CARTESIAN_POINT ( 'NONE',  ( 4.401442555609581635E-16, -16.15625000204838457, -7.188101187500000044 ) ) ;
#99298=CARTESIAN_POINT ( 'NONE',  ( 7.188101187499999156, -18.12500000204838457, 2.977408999572654924 ) ) ;
#99337=CARTESIAN_POINT ( 'NONE',  ( -2.977408999572650039, -19.06250000204838813, -7.188101187500001821 ) ) ;
#99341=ORIENTED_EDGE ( 'NONE', *, *, #53875, .F. ) ;
#99350=DIRECTION ( 'NONE',  ( 0.000000000000000000, 0.000000000000000000, -1.000000000000000000 ) ) ;
#99361=CARTESIAN_POINT ( 'NONE',  ( -7.188101187500002709, -31.81250000204839168, 2.977408999572648707 ) ) ;
#99369=CARTESIAN_POINT ( 'NONE',  ( -9.253583916535177423, 31.29803908005034785, 3.792462592445554392 ) ) ;
#99412=CARTESIAN_POINT ( 'NONE',  ( 7.934203308536662114, 88.86700340017800670, 1.057099537198546324 ) ) ;
#99414=EDGE_LOOP ( 'NONE', ( #35725, #87542, #52112, #95397 ) ) ;
#99425=CARTESIAN_POINT ( 'NONE',  ( 7.188101187500001821, -11.56250000204838635, -2.977408999572650483 ) ) ;
#99428=CARTESIAN_POINT ( 'NONE',  ( 9.797174393178825657E-16, -30.00000000000000000, -8.000000000000000000 ) ) ;
#99465=CARTESIAN_POINT ( 'NONE',  ( 7.211357414135266986, 82.98853460065558352, 3.467230644691327690 ) ) ;
#99482=VERTEX_POINT ( 'NONE', #44895 ) ;
#99485=CARTESIAN_POINT ( 'NONE',  ( 2.977408999572652260, -23.93750000204838457, 7.188101187500000044 ) ) ;
#99488=VERTEX_POINT ( 'NONE', #52965 ) ;
#99498=CARTESIAN_POINT ( 'NONE',  ( -3.313708498984765161, -26.65625000409676915, 7.999999999999998224 ) ) ;
#99515=VECTOR ( 'NONE', #52870, 1000.000000000000000 ) ;
#99541=CARTESIAN_POINT ( 'NONE',  ( -6.928203230275510549, 29.99999999999999645, -4.000000000000000000 ) ) ;
#99560=CARTESIAN_POINT ( 'NONE',  ( 4.582575694955839829, 15.00000000000000000, 9.999999999999998224 ) ) ;
#99612=DIRECTION ( 'NONE',  ( -3.552713678800500929E-15, 0.000000000000000000, 1.000000000000000000 ) ) ;
#99631=CARTESIAN_POINT ( 'NONE',  ( -8.000000000000000000, -11.74999999999999289, -9.797174393178825657E-16 ) ) ;
#99633=ADVANCED_FACE ( 'NONE', ( #59886 ), #59347, .T. ) ;
#99635=CARTESIAN_POINT ( 'NONE',  ( -7.744168461338430731, 101.5374593828484109, 2.019395720771552938 ) ) ;
#99648=( BOUNDED_CURVE ( )  B_SPLINE_CURVE ( 2, ( #20848, #55259, #69876, #80072, #104902, #29967, #21885, #61808, #14271 ),
 .UNSPECIFIED., .F., .F. ) 
 B_SPLINE_CURVE_WITH_KNOTS ( ( 3, 2, 2, 2, 3 ),
 ( 0.4264705882352942123, 0.4338235294117648300, 0.4411764705882353921, 0.4485294117647060097, 0.4558823529411765718 ),
 .UNSPECIFIED. ) 
 CURVE ( )  GEOMETRIC_REPRESENTATION_ITEM ( )  RATIONAL_B_SPLINE_CURVE ( ( 0.9999999999999988898, 0.9238795325112878487, 1.000000000000000000, 0.9238795325112867385, 1.000000000000000000, 0.9238795325112867385, 1.000000000000000000, 0.9238795325112856283, 1.000000000000001110 ) ) 
 REPRESENTATION_ITEM ( '' )  );
#99669=CARTESIAN_POINT ( 'NONE',  ( -7.744329845603314944, 81.53711769846543689, -2.018701143083232452 ) ) ;
#99673=ORIENTED_EDGE ( 'NONE', *, *, #82549, .F. ) ;
#99675=VERTEX_POINT ( 'NONE', #90638 ) ;
#99702=CARTESIAN_POINT ( 'NONE',  ( 7.188101187500000044, -29.65625000204838813, 0.000000000000000000 ) ) ;
#99711=CARTESIAN_POINT ( 'NONE',  ( 4.898587196589412829E-16, -27.12499999999999645, -8.000000000000000000 ) ) ;
#99717=ADVANCED_FACE ( 'NONE', ( #54394 ), #100443, .F. ) ;
#99739=CARTESIAN_POINT ( 'NONE',  ( 8.000000000000000000, -29.18750000409677270, 0.000000000000000000 ) ) ;
#99760=CARTESIAN_POINT ( 'NONE',  ( -8.000000000000000000, -25.34374999999999645, -3.313708498984762496 ) ) ;
#99781=CARTESIAN_POINT ( 'NONE',  ( 7.744329845603314944, 108.4628823015345773, -2.018701143083236449 ) ) ;
#99785=CARTESIAN_POINT ( 'NONE',  ( -3.313708498984798467, -16.53124999999999289, -7.999999999999961808 ) ) ;
#99786=CARTESIAN_POINT ( 'NONE',  ( 2.977408999572650927, -14.37500000204838635, -7.188101187500001821 ) ) ;
#99827=AXIS2_PLACEMENT_3D ( 'NONE', #54796, #61875, #21944 ) ;
#99837=CARTESIAN_POINT ( 'NONE',  ( -7.188101187500000933, -15.87500000204838635, -2.977408999572651371 ) ) ;
#99845=CARTESIAN_POINT ( 'NONE',  ( 5.082755093536324154, -19.71875000204838457, 5.082755093536326818 ) ) ;
#99855=UNCERTAINTY_MEASURE_WITH_UNIT (LENGTH_MEASURE( 1.000000000000000082E-05 ), #5081, 'distance_accuracy_value', 'NONE');
#99874=CARTESIAN_POINT ( 'NONE',  ( 4.898587196589412829E-16, -25.81250000409677270, -8.000000000000000000 ) ) ;
#99889=CARTESIAN_POINT ( 'NONE',  ( -2.977408999572654480, -18.50000000204838457, 7.188101187499999156 ) ) ;
#99900=CARTESIAN_POINT ( 'NONE',  ( -7.188101187500002709, -9.312500002048382797, 2.977408999572647819 ) ) ;
#99913=CARTESIAN_POINT ( 'NONE',  ( 4.401442555609581635E-16, -33.78125000204838813, -7.188101187500000044 ) ) ;
#99972=CARTESIAN_POINT ( 'NONE',  ( 4.401442555609581635E-16, -15.78125000204838635, -7.188101187500000044 ) ) ;
#100009=CARTESIAN_POINT ( 'NONE',  ( 8.000000000000000000, -10.90624999999999467, -3.313708498984761164 ) ) ;
#100027=CARTESIAN_POINT ( 'NONE',  ( -7.188101187500000933, -24.50000000204839168, -2.977408999572651371 ) ) ;
#100036=EDGE_CURVE ( 'NONE', #81483, #43496, #47520, .T. ) ;
#100040=CARTESIAN_POINT ( 'NONE',  ( 5.656854249492380582, -21.50000000409676915, -5.656854249492379694 ) ) ;
#100047=CARTESIAN_POINT ( 'NONE',  ( -3.648665620917451502, 15.00000000000000178, -9.999999999999998224 ) ) ;
#100053=EDGE_CURVE ( 'NONE', #11237, #54191, #7234, .T. ) ;
#100058=AXIS2_PLACEMENT_3D ( 'NONE', #50346, #74624, #26142 ) ;
#100092=EDGE_LOOP ( 'NONE', ( #32461, #8400, #5439, #59922 ) ) ;
#100100=CARTESIAN_POINT ( 'NONE',  ( 1.224646799147354440E-15, 15.00000000000000000, 9.999999999999998224 ) ) ;
#100136=B_SPLINE_CURVE_WITH_KNOTS ( 'NONE', 3,
 ( #29683, #11858, #62555, #46364, #53400, #45314, #87363, #46878, #4309, #79253, #21071, #94400, #103014, #28625, #86321, #71159, #37245, #5379, #28095, #95981, #78709, #95441, #29170, #22108, #12913, #45837, #4845, #77679, #54420, #37778, #62045, #38298, #30194, #104054 ),
 .UNSPECIFIED., .F., .F.,
 ( 4, 2, 2, 2, 2, 2, 2, 2, 2, 2, 2, 2, 2, 2, 2, 2, 4 ),
 ( 0.01263889472610566986, 0.01342810546992894566, 0.01421731621375222319, 0.01500652695757550073, 0.01579573770139877653, 0.01658494844522205233, 0.01737415918904532813, 0.01816336993286860740, 0.01895258067669188320, 0.01974179142051515901, 0.02053100216433843828, 0.02132021290816171408, 0.02210942365198498988, 0.02289863439580826568, 0.02368784513963154148, 0.02447705588345482075, 0.02526626662727809655 ),
 .UNSPECIFIED. ) ;
#100167=CARTESIAN_POINT ( 'NONE',  ( -3.999976370155091665, -10.00072555073141167, 6.928216872919098712 ) ) ;
#100202=CARTESIAN_POINT ( 'NONE',  ( -6.928203230275510549, 85.00000000000000000, -4.000000000000000000 ) ) ;
#100207=( GEOMETRIC_REPRESENTATION_CONTEXT ( 3 ) GLOBAL_UNCERTAINTY_ASSIGNED_CONTEXT ( ( #59355 ) ) GLOBAL_UNIT_ASSIGNED_CONTEXT ( ( #38317, #96003, #86339 ) ) REPRESENTATION_CONTEXT ( 'NONE', 'WORKASPACE' ) );
#100268=B_SPLINE_CURVE_WITH_KNOTS ( 'NONE', 3,
 ( #69051, #20006, #52848, #85772 ),
 .UNSPECIFIED., .F., .F.,
 ( 4, 4 ),
 ( 0.000000000000000000, 0.001312499955570751390 ),
 .UNSPECIFIED. ) ;
#100288=CARTESIAN_POINT ( 'NONE',  ( -3.313708498984760720, -27.03124999999998934, -8.000000000000000000 ) ) ;
#100308=CARTESIAN_POINT ( 'NONE',  ( 8.000113193197767814, 109.0002263864586212, -0.2613481123984635612 ) ) ;
#100376=CARTESIAN_POINT ( 'NONE',  ( -7.188101187500000044, -21.78125000204838457, -8.802885111219163269E-16 ) ) ;
#100391=CARTESIAN_POINT ( 'NONE',  ( 3.313708498984800688, -14.28124999999998934, 7.999999999999960032 ) ) ;
#100393=CARTESIAN_POINT ( 'NONE',  ( -7.045965687440311598, 86.30392463786034796, 3.790395326974319357 ) ) ;
#100401=CARTESIAN_POINT ( 'NONE',  ( 9.852235012526417535, 15.56087475005694643, -1.749814335632526863 ) ) ;
#100419=CARTESIAN_POINT ( 'NONE',  ( 2.977408999572651815, -18.31250000204838457, 7.188101187500000933 ) ) ;
#100443=( BOUNDED_SURFACE ( )  B_SPLINE_SURFACE ( 3, 2, ( 
 ( #12889, #45813, #6928 ),
 ( #15553, #55986, #5862 ),
 ( #104563, #48444, #31764 ),
 ( #47385, #38787, #13952 ),
 ( #89980, #98066, #64645 ),
 ( #40898, #80815, #56529 ),
 ( #81335, #39850, #73240 ),
 ( #79756, #30170, #80277 ),
 ( #31250, #71656, #89459 ),
 ( #39325, #7445, #97517 ) ),
 .UNSPECIFIED., .F., .F., .F. ) 
 B_SPLINE_SURFACE_WITH_KNOTS ( ( 4, 2, 2, 2, 4 ),
 ( 3, 3 ),
 ( 0.002450517525418901676, 0.003060732775749469906, 0.003670948026080037702, 0.004891378526741174161, 0.007332239528063446213 ),
 ( 0.000000000000000000, 1.000000000000000000 ),
 .UNSPECIFIED. ) 
 GEOMETRIC_REPRESENTATION_ITEM ( )  RATIONAL_B_SPLINE_SURFACE ( (
 ( 1.000000000000000000, 0.7071067811865475727, 1.000000000000000000),
 ( 1.000000000000000000, 0.7344063550101603832, 1.000000000000000000),
 ( 1.000000000000000000, 0.7590375248711465073, 1.000000000000000000),
 ( 1.000000000000000000, 0.8038331608703648268, 1.000000000000000000),
 ( 1.000000000000000000, 0.8240352460866686712, 1.000000000000000000),
 ( 1.000000000000000000, 0.8791017378331671406, 1.000000000000000000),
 ( 1.000000000000000000, 0.9085032776981341041, 1.000000000000000000),
 ( 1.000000000000000000, 0.9784170511695907679, 1.000000000000000000),
 ( 1.000000000000000000, 0.9996598051697292986, 1.000000000000000000),
 ( 1.000000000000000000, 1.000000000000000000, 1.000000000000000000) ) ) 
 REPRESENTATION_ITEM ( '' )  SURFACE ( )  );
#100447=CARTESIAN_POINT ( 'NONE',  ( -5.082755093536326818, -27.21875000204838813, 5.082755093536325042 ) ) ;
#100451=ADVANCED_FACE ( 'NONE', ( #47034 ), #89107, .T. ) ;
#100463=CARTESIAN_POINT ( 'NONE',  ( -8.000000000000000000, -22.43750000409676915, -9.797174393178825657E-16 ) ) ;
#100495=CARTESIAN_POINT ( 'NONE',  ( 7.188101187499999156, -22.62500000204838813, 2.977408999572654924 ) ) ;
#100503=CARTESIAN_POINT ( 'NONE',  ( -7.188101187500000044, -13.90625000204838457, -8.802885111219163269E-16 ) ) ;
#100504=CARTESIAN_POINT ( 'NONE',  ( -5.656854249492381470, -17.75000000409676915, 5.656854249492379694 ) ) ;
#100538=CARTESIAN_POINT ( 'NONE',  ( 7.002619243997875387, 83.94992681986181537, -3.868708944012998252 ) ) ;
#100561=CARTESIAN_POINT ( 'NONE',  ( 7.188101187500000933, -26.56250000204838457, -2.977408999572650483 ) ) ;
#100569=CARTESIAN_POINT ( 'NONE',  ( 7.999999999999998224, -21.78125000409677980, 3.313708498984766493 ) ) ;
#100582=( BOUNDED_CURVE ( )  B_SPLINE_CURVE ( 2, ( #14657, #40546, #98250, #64310, #31947, #80991, #79935, #90162, #38971, #6045, #71844, #14133, #105807, #64828, #97707, #23872, #89637, #28248, #61670, #43857, #20710, #19099, #52470, #84852, #68690, #76748, #85391, #27184, #94560, #61118, #18547, #101030, #10420, #53548, #53017, #102087, #85942, #94007, #68136, #60075, #20168, #27727, #60600, #12012, #1788, #75689, #34745, #35810, #10935, #19637, #36350, #86479, #42797, #76215, #77829, #2322, #2856, #92398, #51411, #92937, #36870, #93488, #44945, #26653, #69738, #51939, #3407, #102631, #28788, #43334, #84323, #101569, #11471, #44399, #77296, #69220, #35266, #3938, #67617, #100495, #59530, #103689, #38446, #31426, #14650, #55116, #4463, #62202, #88046, #64301, #78343, #71312, #23320, #5523, #45993, #29833, #63774, #97173, #105280, #47027, #12535, #22797, #96662, #95601, #56159, #13598, #39500, #55632, #104206, #88569, #103168, #72374, #62710, #79929, #6566, #45471, #86994, #95087, #87517, #54578, #14126, #37404, #47560, #63242, #70265, #6038, #29311, #5001, #21741, #30350, #21219, #80455, #38963, #54049, #13064, #71837, #78872, #37932, #96134, #70793, #22268, #46511, #79408, #104743, #30895, #42130, #41609, #24398, #99291, #66407, #65353, #99837, #90155, #9222, #33535, #25467, #1111, #98243, #16260, #49690, #74492, #50226, #41, #16804, #83127, #98760, #41076, #58319, #48616, #105800, #8170, #64821, #91245, #17352, #81501, #82597, #15732, #15195, #75016, #72889, #80986, #73961, #34086, #66958, #31939, #56709, #89631, #97700, #567, #26009, #49145, #89101, #48086, #7102, #7621, #40017, #82048, #23864, #40539, #57768, #73421, #106316, #32480, #57237, #33013, #65880, #24914, #90696, #8701, #84197, #10293, #77168, #101445, #43730, #76620, #101963, #17881, #91762, #50735, #51814, #100894 ),
 .UNSPECIFIED., .F., .F. ) 
 B_SPLINE_CURVE_WITH_KNOTS ( ( 3, 2, 2, 2, 2, 2, 2, 2, 2, 2, 2, 2, 2, 2, 2, 2, 2, 2, 2, 2, 2, 2, 2, 2, 2, 2, 2, 2, 2, 2, 2, 2, 2, 2, 2, 2, 2, 2, 2, 2, 2, 2, 2, 2, 2, 2, 2, 2, 2, 2, 2, 2, 2, 2, 2, 2, 2, 2, 2, 2, 2, 2, 2, 2, 2, 2, 2, 2, 2, 2, 2, 2, 2, 2, 2, 2, 2, 2, 2, 2, 2, 2, 2, 2, 2, 2, 2, 2, 2, 2, 2, 2, 2, 2, 2, 2, 2, 2, 2, 2, 2, 2, 2, 2, 2, 2, 2, 2, 2, 2, 3 ),
 ( 0.1777496976123880690, 0.1838235294117647189, 0.1911764705882352811, 0.1985294117647058709, 0.2058823529411764608, 0.2132352941176470507, 0.2205882352941176405, 0.2279411764705882304, 0.2352941176470588203, 0.2426470588235294101, 0.2500000000000000000, 0.2573529411764705621, 0.2647058823529411797, 0.2720588235294117418, 0.2794117647058823595, 0.2867647058823529216, 0.2941176470588235392, 0.3014705882352941013, 0.3088235294117647189, 0.3161764705882352811, 0.3235294117647058987, 0.3308823529411764608, 0.3382352941176470784, 0.3455882352941176405, 0.3529411764705882582, 0.3602941176470588203, 0.3676470588235294379, 0.3750000000000000000, 0.3823529411764705621, 0.3897058823529412352, 0.3970588235294117418, 0.4044117647058823595, 0.4117647058823529216, 0.4191176470588234837, 0.4264705882352941013, 0.4338235294117647189, 0.4411764705882352811, 0.4485294117647058987, 0.4558823529411764608, 0.4632352941176470784, 0.4705882352941176405, 0.4779411764705882582, 0.4852941176470588203, 0.4926470588235294379, 0.5000000000000000000, 0.5073529411764705621, 0.5147058823529411242, 0.5220588235294117974, 0.5294117647058823595, 0.5367647058823529216, 0.5441176470588233727, 0.5514705882352941568, 0.5588235294117647189, 0.5661764705882352811, 0.5735294117647058432, 0.5808823529411765163, 0.5882352941176470784, 0.5955882352941176405, 0.6029411764705882026, 0.6102941176470588758, 0.6176470588235294379, 0.6250000000000000000, 0.6323529411764705621, 0.6397058823529411242, 0.6470588235294117974, 0.6544117647058823595, 0.6617647058823529216, 0.6691176470588233727, 0.6764705882352941568, 0.6838235294117647189, 0.6911764705882352811, 0.6985294117647058432, 0.7058823529411764053, 0.7132352941176469674, 0.7205882352941175295, 0.7279411764705880916, 0.7352941176470588758, 0.7426470588235294379, 0.7500000000000000000, 0.7573529411764705621, 0.7647058823529411242, 0.7720588235294116863, 0.7794117647058822484, 0.7867647058823528106, 0.7941176470588233727, 0.8014705882352941568, 0.8088235294117647189, 0.8161764705882352811, 0.8235294117647058432, 0.8308823529411764053, 0.8382352941176469674, 0.8455882352941175295, 0.8529411764705880916, 0.8602941176470588758, 0.8676470588235294379, 0.8750000000000000000, 0.8823529411764705621, 0.8897058823529411242, 0.8970588235294116863, 0.9044117647058822484, 0.9117647058823528106, 0.9191176470588233727, 0.9264705882352943789, 0.9338235294117647189, 0.9411764705882352811, 0.9485294117647058432, 0.9558823529411764053, 0.9632352941176471894, 0.9705882352941175295, 0.9779411764705880916, 0.9804062476879973342 ),
 .UNSPECIFIED. ) 
 CURVE ( )  GEOMETRIC_REPRESENTATION_ITEM ( )  RATIONAL_B_SPLINE_CURVE ( ( 0.9781234062028234533, 0.9371213634217746558, 1.000000000000000000, 0.9238795325112867385, 1.000000000000000000, 0.9238795325112867385, 1.000000000000000000, 0.9238795325112867385, 1.000000000000000000, 0.9238795325112867385, 1.000000000000000000, 0.9238795325112867385, 1.000000000000000000, 0.9238795325112867385, 1.000000000000000000, 0.9238795325112867385, 1.000000000000000000, 0.9238795325112867385, 1.000000000000000000, 0.9238795325112867385, 1.000000000000000000, 0.9238795325112867385, 1.000000000000000000, 0.9238795325112867385, 1.000000000000000000, 0.9238795325112867385, 1.000000000000000000, 0.9238795325112867385, 1.000000000000000000, 0.9238795325112867385, 1.000000000000000000, 0.9238795325112867385, 1.000000000000000000, 0.9238795325112867385, 1.000000000000000000, 0.9238795325112867385, 1.000000000000000000, 0.9238795325112867385, 1.000000000000000000, 0.9238795325112867385, 1.000000000000000000, 0.9238795325112867385, 1.000000000000000000, 0.9238795325112867385, 1.000000000000000000, 0.9238795325112867385, 1.000000000000000000, 0.9238795325112867385, 1.000000000000000000, 0.9238795325112867385, 1.000000000000000000, 0.9238795325112867385, 1.000000000000000000, 0.9238795325112867385, 1.000000000000000000, 0.9238795325112867385, 1.000000000000000000, 0.9238795325112867385, 1.000000000000000000, 0.9238795325112867385, 1.000000000000000000, 0.9238795325112867385, 1.000000000000000000, 0.9238795325112867385, 1.000000000000000000, 0.9238795325112867385, 1.000000000000000000, 0.9238795325112867385, 1.000000000000000000, 0.9238795325112867385, 1.000000000000000000, 0.9238795325112867385, 1.000000000000000000, 0.9238795325112867385, 1.000000000000000000, 0.9238795325112867385, 1.000000000000000000, 0.9238795325112867385, 1.000000000000000000, 0.9238795325112867385, 1.000000000000000000, 0.9238795325112867385, 1.000000000000000000, 0.9238795325112867385, 1.000000000000000000, 0.9238795325112867385, 1.000000000000000000, 0.9238795325112867385, 1.000000000000000000, 0.9238795325112867385, 1.000000000000000000, 0.9238795325112867385, 1.000000000000000000, 0.9238795325112867385, 1.000000000000000000, 0.9238795325112867385, 1.000000000000000000, 0.9238795325112867385, 1.000000000000000000, 0.9238795325112867385, 1.000000000000000000, 0.9238795325112867385, 1.000000000000000000, 0.9238795325112867385, 1.000000000000000000, 0.9238795325112867385, 1.000000000000000000, 0.9238795325112867385, 1.000000000000000000, 0.9238795325112867385, 1.000000000000000000, 0.9238795325112867385, 1.000000000000000000, 0.9238795325112867385, 1.000000000000000000, 0.9238795325112867385, 1.000000000000000000, 0.9238795325112867385, 1.000000000000000000, 0.9238795325112867385, 1.000000000000000000, 0.9238795325112867385, 1.000000000000000000, 0.9238795325112867385, 1.000000000000000000, 0.9238795325112867385, 1.000000000000000000, 0.9238795325112867385, 1.000000000000000000, 0.9238795325112867385, 1.000000000000000000, 0.9238795325112867385, 1.000000000000000000, 0.9238795325112867385, 1.000000000000000000, 0.9238795325112867385, 1.000000000000000000, 0.9238795325112867385, 1.000000000000000000, 0.9238795325112867385, 1.000000000000000000, 0.9238795325112867385, 1.000000000000000000, 0.9238795325112867385, 1.000000000000000000, 0.9238795325112867385, 1.000000000000000000, 0.9238795325112867385, 1.000000000000000000, 0.9238795325112867385, 1.000000000000000000, 0.9238795325112867385, 1.000000000000000000, 0.9238795325112867385, 1.000000000000000000, 0.9238795325112867385, 1.000000000000000000, 0.9238795325112867385, 1.000000000000000000, 0.9238795325112867385, 1.000000000000000000, 0.9238795325112867385, 1.000000000000000000, 0.9238795325112867385, 1.000000000000000000, 0.9238795325112867385, 1.000000000000000000, 0.9238795325112867385, 1.000000000000000000, 0.9238795325112867385, 1.000000000000000000, 0.9238795325112867385, 1.000000000000000000, 0.9238795325112867385, 1.000000000000000000, 0.9238795325112867385, 1.000000000000000000, 0.9238795325112867385, 1.000000000000000000, 0.9238795325112867385, 1.000000000000000000, 0.9238795325112867385, 1.000000000000000000, 0.9238795325112867385, 1.000000000000000000, 0.9238795325112867385, 1.000000000000000000, 0.9238795325112867385, 1.000000000000000000, 0.9238795325112867385, 1.000000000000000000, 0.9238795325112867385, 1.000000000000000000, 0.9238795325112867385, 1.000000000000000000, 0.9238795325112867385, 1.000000000000000000, 0.9238795325112867385, 1.000000000000000000, 0.9238795325112867385, 1.000000000000000000, 0.9238795325112867385, 1.000000000000000000, 0.9238795325112867385, 1.000000000000000000, 0.9238795325112867385, 1.000000000000000000, 0.9238795325112867385, 1.000000000000000000, 0.9238795325112867385, 1.000000000000000000, 0.9238795325112867385, 1.000000000000000000, 0.9238795325112867385, 1.000000000000000000, 0.9238795325112867385, 1.000000000000000000, 0.9238795325112867385, 1.000000000000000000, 0.9744806372091472380, 0.9660719911213342392 ) ) 
 REPRESENTATION_ITEM ( '' )  );
#100728=CARTESIAN_POINT ( 'NONE',  ( -9.253583916535172094, 106.2980390800503301, 3.792462592445557501 ) ) ;
#100739=CARTESIAN_POINT ( 'NONE',  ( -3.313708498984741180, -24.21875000409677625, -8.000000000000019540 ) ) ;
#100743=CARTESIAN_POINT ( 'NONE',  ( 9.797174393178825657E-16, -30.00000000000000000, -8.000000000000000000 ) ) ;
#100765=ORIENTED_EDGE ( 'NONE', *, *, #90603, .F. ) ;
#100803=AXIS2_PLACEMENT_3D ( 'NONE', #25958, #34565, #33480 ) ;
#100814=CARTESIAN_POINT ( 'NONE',  ( -5.656854249492381470, -26.56249999999999645, 5.656854249492379694 ) ) ;
#100881=LINE ( 'NONE', #18956, #77126 ) ;
#100892=ORIENTED_EDGE ( 'NONE', *, *, #56234, .F. ) ;
#100894=CARTESIAN_POINT ( 'NONE',  ( -3.594029361870008099, -9.531975552773349847, 6.225090491531444670 ) ) ;
#100895=CARTESIAN_POINT ( 'NONE',  ( 5.656854249492380582, -18.50000000409676915, -5.656854249492379694 ) ) ;
#100896=CARTESIAN_POINT ( 'NONE',  ( 3.212697619663445803, -30.00000000000000711, 6.447374205472699238 ) ) ;
#100902=CARTESIAN_POINT ( 'NONE',  ( 7.188101187500000044, -22.53125000204838457, 0.000000000000000000 ) ) ;
#100910=CARTESIAN_POINT ( 'NONE',  ( -1.469576158976823947E-15, -14.56250000409677092, 8.000000000000000000 ) ) ;
#100919=( GEOMETRIC_REPRESENTATION_CONTEXT ( 3 ) GLOBAL_UNCERTAINTY_ASSIGNED_CONTEXT ( ( #11361 ) ) GLOBAL_UNIT_ASSIGNED_CONTEXT ( ( #68845, #101196, #34370 ) ) REPRESENTATION_CONTEXT ( 'NONE', 'WORKASPACE' ) );
#100950=CARTESIAN_POINT ( 'NONE',  ( 9.380871178326122717, 27.98883620201673850, 3.467392232194197454 ) ) ;
#100951=CARTESIAN_POINT ( 'NONE',  ( -5.082755093536325042, -17.46875000204838813, -5.082755093536325930 ) ) ;
#100971=UNCERTAINTY_MEASURE_WITH_UNIT (LENGTH_MEASURE( 1.000000000000000082E-05 ), #35881, 'distance_accuracy_value', 'NONE');
#100978=CARTESIAN_POINT ( 'NONE',  ( -7.188101187500000044, -24.40625000204838813, -8.802885111219163269E-16 ) ) ;
#101030=CARTESIAN_POINT ( 'NONE',  ( 7.188101187499999156, -27.12500000204838457, 2.977408999572654924 ) ) ;
#101039=CARTESIAN_POINT ( 'NONE',  ( 7.188101187499999156, -11.75000000204838813, 2.977408999572654924 ) ) ;
#101057=CARTESIAN_POINT ( 'NONE',  ( -10.00000000000000355, 105.0000000000000000, 0.000000000000000000 ) ) ;
#101071=ORIENTED_EDGE ( 'NONE', *, *, #11285, .T. ) ;
#101075=CARTESIAN_POINT ( 'NONE',  ( 7.934883677559676940, 81.13160822062449995, 1.051380792122692531 ) ) ;
#101101=CARTESIAN_POINT ( 'NONE',  ( -7.188101187500000044, -24.40625000204838813, -8.802885111219163269E-16 ) ) ;
#101107=CARTESIAN_POINT ( 'NONE',  ( -9.221216839714871938, 83.95240251831026512, 3.869414262756993406 ) ) ;
#101109=CARTESIAN_POINT ( 'NONE',  ( -1.469576158976823947E-15, -17.56250000409676915, 8.000000000000000000 ) ) ;
#101136=DIRECTION ( 'NONE',  ( 0.000000000000000000, 1.000000000000000000, 0.000000000000000000 ) ) ;
#101161=FACE_OUTER_BOUND ( 'NONE', #45711, .T. ) ;
#101194=CYLINDRICAL_SURFACE ( 'NONE', #7758, 10.00000000000000000 ) ;
#101196=( NAMED_UNIT ( * ) PLANE_ANGLE_UNIT ( ) SI_UNIT ( $, .RADIAN. ) );
#101225=CARTESIAN_POINT ( 'NONE',  ( -4.165977904505308693, 16.00000000000000000, -9.090909090909089940 ) ) ;
#101227=CARTESIAN_POINT ( 'NONE',  ( -1.469576158976823947E-15, -11.56250000409677092, 8.000000000000000000 ) ) ;
#101238=( BOUNDED_CURVE ( )  B_SPLINE_CURVE ( 2, ( #19525, #103057, #27078, #29214, #93373, #84211, #3293, #2745, #100910 ),
 .UNSPECIFIED., .F., .F. ) 
 B_SPLINE_CURVE_WITH_KNOTS ( ( 3, 2, 2, 2, 3 ),
 ( 0.7205882352941176405, 0.7279411764705882026, 0.7352941176470588758, 0.7426470588235294379, 0.7500000000000000000 ),
 .UNSPECIFIED. ) 
 CURVE ( )  GEOMETRIC_REPRESENTATION_ITEM ( )  RATIONAL_B_SPLINE_CURVE ( ( 1.000000000000000000, 0.9238795325112867385, 1.000000000000000000, 0.9238795325112867385, 1.000000000000000000, 0.9238795325112867385, 1.000000000000000000, 0.9238795325112867385, 1.000000000000000000 ) ) 
 REPRESENTATION_ITEM ( '' )  );
#101273=CARTESIAN_POINT ( 'NONE',  ( 6.928203230275509661, 30.00000000000000000, 4.000000000000000000 ) ) ;
#101289=CIRCLE ( 'NONE', #85753, 0.9999999999999994449 ) ;
#101321=CARTESIAN_POINT ( 'NONE',  ( -3.313708498984837547, -13.53124999999998934, -7.999999999999923617 ) ) ;
#101340=EDGE_CURVE ( 'NONE', #50908, #20242, #44087, .T. ) ;
#101364=CARTESIAN_POINT ( 'NONE',  ( -1.469576158976823947E-15, -23.37499999999999289, 8.000000000000000000 ) ) ;
#101365=CARTESIAN_POINT ( 'NONE',  ( -8.000000000000000000, -20.74999999999999289, -9.797174393178825657E-16 ) ) ;
#101385=CARTESIAN_POINT ( 'NONE',  ( 7.551560007654694928, 108.0091035180699350, -2.648022159607841708 ) ) ;
#101407=DIRECTION ( 'NONE',  ( -0.000000000000000000, 1.000000000000000000, -0.000000000000000000 ) ) ;
#101435=CARTESIAN_POINT ( 'NONE',  ( -9.918512371096300129, 101.2071700772945064, -1.297150762882696817 ) ) ;
#101441=ORIENTED_EDGE ( 'NONE', *, *, #78040, .F. ) ;
#101445=CARTESIAN_POINT ( 'NONE',  ( 4.401442555609581635E-16, -10.15625000204838457, -7.188101187500000044 ) ) ;
#101453=CARTESIAN_POINT ( 'NONE',  ( 7.188101187500001821, -11.93750000204838457, -2.977408999572650483 ) ) ;
#101458=CARTESIAN_POINT ( 'NONE',  ( 9.165151389911679658, 105.0000000000000142, -4.000000000000001776 ) ) ;
#101467=CARTESIAN_POINT ( 'NONE',  ( -7.002641335706728754, 86.05087262680835636, 3.868676264653293284 ) ) ;
#101494=CARTESIAN_POINT ( 'NONE',  ( 2.977408999572650927, -20.75000000204839523, -7.188101187500001821 ) ) ;
#101503=DIRECTION ( 'NONE',  ( 0.000000000000000000, 0.000000000000000000, 1.000000000000000000 ) ) ;
#101519=CARTESIAN_POINT ( 'NONE',  ( 7.188101187499999156, -25.25000000204839523, 2.977408999572654924 ) ) ;
#101569=CARTESIAN_POINT ( 'NONE',  ( -7.188101187500000933, -23.37500000204838813, -2.977408999572651371 ) ) ;
#101579=CARTESIAN_POINT ( 'NONE',  ( -1.320432766682874540E-15, -33.40625000204838813, 7.188101187500000044 ) ) ;
#101585=CARTESIAN_POINT ( 'NONE',  ( -8.000000000000001776, -14.65624999999999467, 3.313708498984759387 ) ) ;
#101611=ADVANCED_FACE ( 'NONE', ( #101628 ), #18063, .F. ) ;
#101619=FACE_OUTER_BOUND ( 'NONE', #36150, .T. ) ;
#101628=FACE_OUTER_BOUND ( 'NONE', #17608, .T. ) ;
#101638=CARTESIAN_POINT ( 'NONE',  ( 7.188101187499999156, -23.75000000204838813, 2.977408999572654924 ) ) ;
#101648=CARTESIAN_POINT ( 'NONE',  ( 4.898587196589412829E-16, -19.81250000409677270, -8.000000000000000000 ) ) ;
#101704=CARTESIAN_POINT ( 'NONE',  ( -2.977408999572650039, -29.18750000204839523, -7.188101187500001821 ) ) ;
#101724=ORIENTED_EDGE ( 'NONE', *, *, #63984, .T. ) ;
#101735=ORIENTED_EDGE ( 'NONE', *, *, #77384, .F. ) ;
#101746=AXIS2_PLACEMENT_3D ( 'NONE', #84118, #43129, #2113 ) ;
#101767=CARTESIAN_POINT ( 'NONE',  ( -7.744329845603313167, 101.5371176984654085, -2.018701143083234228 ) ) ;
#101786=DIRECTION ( 'NONE',  ( -0.000000000000000000, 1.000000000000000000, -0.000000000000000000 ) ) ;
#101804=ORIENTED_EDGE ( 'NONE', *, *, #57500, .F. ) ;
#101808=CARTESIAN_POINT ( 'NONE',  ( -8.000000000000001776, -23.84375000409677270, 3.313708498984759387 ) ) ;
#101886=CARTESIAN_POINT ( 'NONE',  ( -8.000000000000001776, -23.65624999999999645, 3.313708498984758943 ) ) ;
#101894=ORIENTED_EDGE ( 'NONE', *, *, #89523, .T. ) ;
#101911=CARTESIAN_POINT ( 'NONE',  ( 5.082755093536325930, -9.968750002048384573, -5.082755093536325042 ) ) ;
#101925=VERTEX_POINT ( 'NONE', #12331 ) ;
#101932=CARTESIAN_POINT ( 'NONE',  ( -8.000000000000000000, -25.34374999999999645, -3.313708498984762496 ) ) ;
#101963=CARTESIAN_POINT ( 'NONE',  ( -7.188101187500000933, -9.875000002048388126, -2.977408999572651371 ) ) ;
#101964=CARTESIAN_POINT ( 'NONE',  ( 7.999999999999998224, -18.78125000409677270, 3.313708498984766049 ) ) ;
#101965=CARTESIAN_POINT ( 'NONE',  ( 4.404050688260422675, -29.99999999999999289, 5.685839403562723327 ) ) ;
#101970=CARTESIAN_POINT ( 'NONE',  ( -1.320432766682874540E-15, -16.90625000204838813, 7.188101187500000044 ) ) ;
#102011=CARTESIAN_POINT ( 'NONE',  ( 5.082755093536324154, -15.21875000204838457, 5.082755093536326818 ) ) ;
#102018=CARTESIAN_POINT ( 'NONE',  ( 10.00004721872059932, 89.00011804681153649, -0.2617599822266505338 ) ) ;
#102038=CARTESIAN_POINT ( 'NONE',  ( -7.188101187500002709, -27.31250000204838457, 2.977408999572648707 ) ) ;
#102058=CARTESIAN_POINT ( 'NONE',  ( 9.948513602187993854, 101.1302205665614053, 1.045942665286139439 ) ) ;
#102087=CARTESIAN_POINT ( 'NONE',  ( 2.977408999572650927, -26.75000000204838457, -7.188101187500000933 ) ) ;
#102098=CARTESIAN_POINT ( 'NONE',  ( -7.188101187500000044, -33.78125000204838813, -8.802885111219163269E-16 ) ) ;
#102104=CARTESIAN_POINT ( 'NONE',  ( -7.999912353029506207, 108.9998247060309069, -0.2691822806795004519 ) ) ;
#102143=CARTESIAN_POINT ( 'NONE',  ( -1.320432766682874540E-15, -28.90625000204838813, 7.188101187500000044 ) ) ;
#102159=CARTESIAN_POINT ( 'NONE',  ( 7.188101187499999156, -19.25000000204838457, 2.977408999572654924 ) ) ;
#102168=CARTESIAN_POINT ( 'NONE',  ( 5.656854249492380582, -18.50000000409676915, -5.656854249492379694 ) ) ;
#102170=FILL_AREA_STYLE ('',( #70345 ) ) ;
#102177=ORIENTED_EDGE ( 'NONE', *, *, #86141, .T. ) ;
#102181=CYLINDRICAL_SURFACE ( 'NONE', #10097, 8.000000000000000000 ) ;
#102232=CARTESIAN_POINT ( 'NONE',  ( -7.188101187500002709, -25.81250000204838457, 2.977408999572648707 ) ) ;
#102235=CARTESIAN_POINT ( 'NONE',  ( -2.797297131808754944, 15.83452282593334282, 9.607612890400021755 ) ) ;
#102238=CARTESIAN_POINT ( 'NONE',  ( -5.656854249492379694, -17.93749999999999645, -5.656854249492380582 ) ) ;
#102275=CARTESIAN_POINT ( 'NONE',  ( 4.898587196589412829E-16, -13.62499999999999112, -8.000000000000000000 ) ) ;
#102281=CARTESIAN_POINT ( 'NONE',  ( 5.656854249492380582, -11.00000000409677092, -5.656854249492379694 ) ) ;
#102300=CARTESIAN_POINT ( 'NONE',  ( -6.928203230275507885, 105.0000000000000000, -4.000000000000001776 ) ) ;
#102303=CARTESIAN_POINT ( 'NONE',  ( 9.852211596319799369, 15.56091200510340045, 1.749942564367552356 ) ) ;
#102349=EDGE_LOOP ( 'NONE', ( #83776, #75643, #101071, #3941 ) ) ;
#102371=PLANE ( 'NONE',  #5706 ) ;
#102417=CARTESIAN_POINT ( 'NONE',  ( -8.000000000000001776, -10.34375000409677092, 3.313708498984759387 ) ) ;
#102426=CARTESIAN_POINT ( 'NONE',  ( 3.313708498984762496, -20.28124999999999289, 7.999999999999998224 ) ) ;
#102439=DIRECTION ( 'NONE',  ( 0.000000000000000000, 1.000000000000000000, 0.000000000000000000 ) ) ;
#102449=CARTESIAN_POINT ( 'NONE',  ( -2.977408999572650039, -9.687500002048384573, -7.188101187500001821 ) ) ;
#102451=( LENGTH_UNIT ( ) NAMED_UNIT ( * ) SI_UNIT ( .MILLI., .METRE. ) );
#102469=VERTEX_POINT ( 'NONE', #7791 ) ;
#102470=EDGE_CURVE ( 'NONE', #78182, #28854, #27521, .T. ) ;
#102481=CARTESIAN_POINT ( 'NONE',  ( -8.000000000000000000, -26.74999999999999645, -9.797174393178825657E-16 ) ) ;
#102500=CARTESIAN_POINT ( 'NONE',  ( 4.034557488804384917, 15.07443463110268134, -9.151133496029480341 ) ) ;
#102511=ORIENTED_EDGE ( 'NONE', *, *, #52449, .F. ) ;
#102515=CARTESIAN_POINT ( 'NONE',  ( -2.977408999572650039, -14.56250000204838457, -7.188101187500001821 ) ) ;
#102529=CARTESIAN_POINT ( 'NONE',  ( -6.928203230275510549, 85.00000000000000000, 4.000000000000000000 ) ) ;
#102544=CARTESIAN_POINT ( 'NONE',  ( 7.213352437320216914, 32.01836473007681860, -3.463014597543476736 ) ) ;
#102552=CARTESIAN_POINT ( 'NONE',  ( 5.082755093536324154, -12.21875000204838635, 5.082755093536326818 ) ) ;
#102570=CARTESIAN_POINT ( 'NONE',  ( 8.000000000000000000, -28.99999999999999289, 0.000000000000000000 ) ) ;
#102581=CARTESIAN_POINT ( 'NONE',  ( 5.082755093536325930, -24.96875000204838813, -5.082755093536325042 ) ) ;
#102599=CARTESIAN_POINT ( 'NONE',  ( -3.313708498984746065, -22.15625000409677625, 8.000000000000017764 ) ) ;
#102600=CARTESIAN_POINT ( 'NONE',  ( 9.165151389911677882, 104.7326484439288237, -4.000000000000001776 ) ) ;
#102608=STYLED_ITEM ( 'NONE', ( #89723 ), #64886 ) ;
#102631=CARTESIAN_POINT ( 'NONE',  ( 2.977408999572650927, -23.75000000204838813, -7.188101187500000933 ) ) ;
#102642=CARTESIAN_POINT ( 'NONE',  ( -5.082755093536325042, -33.96875000204838813, -5.082755093536325930 ) ) ;
#102681=CARTESIAN_POINT ( 'NONE',  ( 5.082755093536324154, -33.21875000204838813, 5.082755093536326818 ) ) ;
#102696=CARTESIAN_POINT ( 'NONE',  ( 7.188101187500000933, -17.56250000204838457, -2.977408999572650483 ) ) ;
#102704=CARTESIAN_POINT ( 'NONE',  ( -5.656854249492381470, -16.25000000409677270, 5.656854249492379694 ) ) ;
#102707=SURFACE_STYLE_USAGE ( .BOTH. , #45548 ) ;
#102713=CARTESIAN_POINT ( 'NONE',  ( 0.8498388482167839042, -29.99999999999998934, -7.699168385716881780 ) ) ;
#102717=SURFACE_SIDE_STYLE ('',( #36435 ) ) ;
#102757=ORIENTED_EDGE ( 'NONE', *, *, #44800, .T. ) ;
#102760=DIRECTION ( 'NONE',  ( -1.000000000000000000, -0.000000000000000000, -0.000000000000000000 ) ) ;
#102767=CARTESIAN_POINT ( 'NONE',  ( 5.082755093536325930, -23.46875000204838457, -5.082755093536325042 ) ) ;
#102782=CYLINDRICAL_SURFACE ( 'NONE', #97219, 4.000000000000001776 ) ;
#102803=( BOUNDED_CURVE ( )  B_SPLINE_CURVE ( 2, ( #104901, #46647, #20847, #95219, #6177, #79547, #5659, #87131, #46134 ),
 .UNSPECIFIED., .F., .F. ) 
 B_SPLINE_CURVE_WITH_KNOTS ( ( 3, 2, 2, 2, 3 ),
 ( 0.5147058823529412352, 0.5220588235294119084, 0.5294117647058824705, 0.5367647058823529216, 0.5441176470588234837 ),
 .UNSPECIFIED. ) 
 CURVE ( )  GEOMETRIC_REPRESENTATION_ITEM ( )  RATIONAL_B_SPLINE_CURVE ( ( 0.9999999999999988898, 0.9238795325112878487, 1.000000000000000000, 0.9238795325112867385, 1.000000000000000000, 0.9238795325112867385, 1.000000000000000000, 0.9238795325112867385, 1.000000000000000000 ) ) 
 REPRESENTATION_ITEM ( '' )  );
#102846=DIRECTION ( 'NONE',  ( 0.000000000000000000, 0.000000000000000000, -1.000000000000000000 ) ) ;
#102852=EDGE_CURVE ( 'NONE', #14808, #40836, #60473, .T. ) ;
#102910=ORIENTED_EDGE ( 'NONE', *, *, #52011, .F. ) ;
#102934=CARTESIAN_POINT ( 'NONE',  ( 9.176803346051512378, 105.5294715579744178, 3.973598758023531019 ) ) ;
#102942=CARTESIAN_POINT ( 'NONE',  ( 9.999999999999996447, 15.00000000000000000, -10.00000000000000000 ) ) ;
#102960=CARTESIAN_POINT ( 'NONE',  ( 4.898587196589412829E-16, -19.62499999999999289, -8.000000000000000000 ) ) ;
#103014=CARTESIAN_POINT ( 'NONE',  ( -9.842984802582137149, 26.40930409524348477, 1.781981959250508618 ) ) ;
#103020=ORIENTED_EDGE ( 'NONE', *, *, #27648, .F. ) ;
#103035=CARTESIAN_POINT ( 'NONE',  ( 3.316968746324254536, 15.92795519102023860, -9.435590127032961405 ) ) ;
#103051=CARTESIAN_POINT ( 'NONE',  ( -7.188101187500000044, -17.28125000204838813, -8.802885111219163269E-16 ) ) ;
#103057=CARTESIAN_POINT ( 'NONE',  ( -3.313708498984760276, -15.21875000409677270, -8.000000000000000000 ) ) ;
#103091=CARTESIAN_POINT ( 'NONE',  ( -2.977408999572650039, -16.06250000204838457, -7.188101187500001821 ) ) ;
#103115=CARTESIAN_POINT ( 'NONE',  ( -1.320432766682874540E-15, -18.03125000204838457, 7.188101187500000044 ) ) ;
#103168=CARTESIAN_POINT ( 'NONE',  ( 5.082755093536324154, -19.71875000204838457, 5.082755093536326818 ) ) ;
#103176=CARTESIAN_POINT ( 'NONE',  ( -5.082755093536325042, -32.46875000204838813, -5.082755093536325930 ) ) ;
#103215=CARTESIAN_POINT ( 'NONE',  ( -7.188101187500001821, -33.87500000204838813, -2.977408999572651371 ) ) ;
#103221=VERTEX_POINT ( 'NONE', #106096 ) ;
#103230=CARTESIAN_POINT ( 'NONE',  ( 7.188101187500000044, -16.15625000204838457, 0.000000000000000000 ) ) ;
#103240=CARTESIAN_POINT ( 'NONE',  ( -3.313708498984760720, -15.21875000409677270, -8.000000000000000000 ) ) ;
#103291=AXIS2_PLACEMENT_3D ( 'NONE', #38074, #4610, #103308 ) ;
#103306=CARTESIAN_POINT ( 'NONE',  ( 2.977408999572651815, -25.43750000204838813, 7.188101187500000933 ) ) ;
#103308=DIRECTION ( 'NONE',  ( 0.000000000000000000, 0.000000000000000000, -1.000000000000000000 ) ) ;
#103353=CARTESIAN_POINT ( 'NONE',  ( -4.582575694955839829, 15.00000000000000000, 10.00000000000000000 ) ) ;
#103459=EDGE_CURVE ( 'NONE', #13028, #78182, #103528, .T. ) ;
#103473=CARTESIAN_POINT ( 'NONE',  ( -5.656854249492381470, -10.25000000409677092, 5.656854249492379694 ) ) ;
#103485=CARTESIAN_POINT ( 'NONE',  ( 3.313708498984762052, -21.21875000000000000, -8.000000000000000000 ) ) ;
#103528=CIRCLE ( 'NONE', #34669, 11.00000000000000000 ) ;
#103531=EDGE_LOOP ( 'NONE', ( #5427, #88693, #50570, #101441 ) ) ;
#103537=EDGE_CURVE ( 'NONE', #3603, #39461, #52845, .T. ) ;
#103554=FACE_OUTER_BOUND ( 'NONE', #96430, .T. ) ;
#103555=CARTESIAN_POINT ( 'NONE',  ( 3.836411046841841532, 15.00000000000000000, -9.999999999999998224 ) ) ;
#103569=CARTESIAN_POINT ( 'NONE',  ( -5.082755093536326818, -12.59375000204838635, 5.082755093536325042 ) ) ;
#103601=CARTESIAN_POINT ( 'NONE',  ( 6.928203230275509661, 30.00000000000000000, 4.000000000000000000 ) ) ;
#103602=CARTESIAN_POINT ( 'NONE',  ( -7.414580834929596520, 27.35343719718517974, 3.010264818013835608 ) ) ;
#103606=CARTESIAN_POINT ( 'NONE',  ( 5.656854249492380582, -21.31249999999999289, -5.656854249492379694 ) ) ;
#103609=CARTESIAN_POINT ( 'NONE',  ( -5.082755093536325042, -15.96875000204838635, -5.082755093536325930 ) ) ;
#103615=VERTEX_POINT ( 'NONE', #48272 ) ;
#103635=CARTESIAN_POINT ( 'NONE',  ( 4.401442555609581635E-16, -17.28125000204838813, -7.188101187500000044 ) ) ;
#103681=COLOUR_RGB ( '', 0.31764706, 0.68627451, 0.89019608) ;
#103684=ORIENTED_EDGE ( 'NONE', *, *, #64126, .F. ) ;
#103689=CARTESIAN_POINT ( 'NONE',  ( 7.188101187500000933, -22.43750000204838813, -2.977408999572650483 ) ) ;
#103697=CARTESIAN_POINT ( 'NONE',  ( -7.188101187500002709, -33.68750000204839523, 2.977408999572648707 ) ) ;
#103716=DIRECTION ( 'NONE',  ( 0.000000000000000000, 0.000000000000000000, 1.000000000000000000 ) ) ;
#103739=CARTESIAN_POINT ( 'NONE',  ( -2.977408999572650039, -29.56250000204838813, -7.188101187500001821 ) ) ;
#103752=CARTESIAN_POINT ( 'NONE',  ( 5.082755093536324154, -17.84375000204838457, 5.082755093536326818 ) ) ;
#103763=CARTESIAN_POINT ( 'NONE',  ( 3.313708498984762496, -9.968750004096770923, 7.999999999999998224 ) ) ;
#103776=DIRECTION ( 'NONE',  ( 0.000000000000000000, 1.000000000000000000, 0.000000000000000000 ) ) ;
#103798=VECTOR ( 'NONE', #81947, 1000.000000000000000 ) ;
#103820=CARTESIAN_POINT ( 'NONE',  ( -7.188101187500000044, -24.40625000204838813, -8.802885111219163269E-16 ) ) ;
#103861=ORIENTED_EDGE ( 'NONE', *, *, #86141, .F. ) ;
#103883=CARTESIAN_POINT ( 'NONE',  ( 5.656854249492380582, -29.00000000409677270, -5.656854249492379694 ) ) ;
#103928=CARTESIAN_POINT ( 'NONE',  ( 4.898587196589412829E-16, -21.31250000409676915, -8.000000000000000000 ) ) ;
#103998=CARTESIAN_POINT ( 'NONE',  ( 4.898587196589412829E-16, -16.81250000409677270, -8.000000000000000000 ) ) ;
#104002=CARTESIAN_POINT ( 'NONE',  ( 8.000000000000000000, -12.40624999999999289, -3.313708498984761608 ) ) ;
#104054=CARTESIAN_POINT ( 'NONE',  ( -9.165151389911681434, 30.00000000000000000, -4.000000000000000000 ) ) ;
#104068=CARTESIAN_POINT ( 'NONE',  ( -9.999999999999960920, 15.00000000000001066, -3.836411046841922801 ) ) ;
#104090=CARTESIAN_POINT ( 'NONE',  ( -3.594029361870008099, -9.531975552773351623, 6.225090491531445558 ) ) ;
#104125=CARTESIAN_POINT ( 'NONE',  ( -6.944371705245973025, 29.46100308575449134, -3.972324460300561633 ) ) ;
#104131=CARTESIAN_POINT ( 'NONE',  ( 7.188101187499999156, -12.12500000204838990, 2.977408999572654924 ) ) ;
#104157=CARTESIAN_POINT ( 'NONE',  ( 7.188101187500001821, -17.56250000204838457, -2.977408999572650483 ) ) ;
#104171=CARTESIAN_POINT ( 'NONE',  ( 3.313708498984722972, -21.40625000409676915, -8.000000000000040856 ) ) ;
#104184=DIRECTION ( 'NONE',  ( 0.000000000000000000, 0.000000000000000000, 1.000000000000000000 ) ) ;
#104206=CARTESIAN_POINT ( 'NONE',  ( -1.320432766682874540E-15, -19.90625000204838457, 7.188101187500000044 ) ) ;
#104216=CARTESIAN_POINT ( 'NONE',  ( -5.082755093536325042, -24.96875000204838813, -5.082755093536325930 ) ) ;
#104252=ORIENTED_EDGE ( 'NONE', *, *, #16074, .F. ) ;
#104259=CARTESIAN_POINT ( 'NONE',  ( 7.188101187500000044, -33.03125000204838813, 0.000000000000000000 ) ) ;
#104275=CARTESIAN_POINT ( 'NONE',  ( 7.188101187499999156, -17.75000000204838457, 2.977408999572654924 ) ) ;
#104282=CARTESIAN_POINT ( 'NONE',  ( -5.656854249492379694, -13.62500000409676915, -5.656854249492380582 ) ) ;
#104290=CARTESIAN_POINT ( 'NONE',  ( -9.165151389911684987, 30.26735155607116923, -4.000000000000001776 ) ) ;
#104293=CARTESIAN_POINT ( 'NONE',  ( -2.455962139888340889, 15.75268258782372754, 9.700350089084293970 ) ) ;
#104306=B_SPLINE_CURVE_WITH_KNOTS ( 'NONE', 3,
 ( #27934, #77504, #13272, #37613, #95285, #102303, #44075, #11682, #53749, #12219 ),
 .UNSPECIFIED., .F., .F.,
 ( 4, 2, 2, 2, 4 ),
 ( 0.000000000000000000, 0.001118707926289531874, 0.002237415852579063748, 0.003356123778868598875, 0.004474831705158133568 ),
 .UNSPECIFIED. ) ;
#104343=CARTESIAN_POINT ( 'NONE',  ( 2.977408999572651815, -26.93750000204838457, 7.188101187500000933 ) ) ;
#104379=ORIENTED_EDGE ( 'NONE', *, *, #1063, .T. ) ;
#104413=CARTESIAN_POINT ( 'NONE',  ( -8.000000000000000000, -30.03125000409677625, -3.313708498984762496 ) ) ;
#104433=CARTESIAN_POINT ( 'NONE',  ( -10.00000000000004086, 14.99999999999998934, 4.210530276627957313 ) ) ;
#104446=ADVANCED_FACE ( 'NONE', ( #45172, #63478, #21965, #22507 ), #87215, .F. ) ;
#104520=CARTESIAN_POINT ( 'NONE',  ( 5.656854249492380582, -24.50000000409677270, -5.656854249492379694 ) ) ;
#104521=CARTESIAN_POINT ( 'NONE',  ( 9.797174393178825657E-16, -30.00000000000000000, -8.000000000000000000 ) ) ;
#104535=CARTESIAN_POINT ( 'NONE',  ( -8.000000000000000000, -17.74999999999999645, -9.797174393178825657E-16 ) ) ;
#104547=DIRECTION ( 'NONE',  ( 0.000000000000000000, 1.000000000000000000, 0.000000000000000000 ) ) ;
#104563=CARTESIAN_POINT ( 'NONE',  ( 10.00000000000003730, 14.99999999999998934, -4.210530276627963531 ) ) ;
#104567=ADVANCED_FACE ( 'NONE', ( #74715 ), #60673, .F. ) ;
#104599=CARTESIAN_POINT ( 'NONE',  ( -9.216463528758735535, 15.13241195026071928, -3.884543032213800373 ) ) ;
#104628=( GEOMETRIC_REPRESENTATION_CONTEXT ( 3 ) GLOBAL_UNCERTAINTY_ASSIGNED_CONTEXT ( ( #53443 ) ) GLOBAL_UNIT_ASSIGNED_CONTEXT ( ( #89906, #40290, #56991 ) ) REPRESENTATION_CONTEXT ( 'NONE', 'WORKASPACE' ) );
#104632=CARTESIAN_POINT ( 'NONE',  ( 8.000000000000000000, -24.49999999999999289, 0.000000000000000000 ) ) ;
#104659=CARTESIAN_POINT ( 'NONE',  ( -6.944031699373470090, 29.46539345443872193, 3.972913591453822502 ) ) ;
#104666=CARTESIAN_POINT ( 'NONE',  ( 3.313708498984762496, -32.28125000000000000, 7.999999999999998224 ) ) ;
#104681=DIRECTION ( 'NONE',  ( 1.734723475976807094E-16, 0.000000000000000000, 1.000000000000000000 ) ) ;
#104691=CARTESIAN_POINT ( 'NONE',  ( 2.977408999572650927, -18.87500000204838457, -7.188101187500001821 ) ) ;
#104743=CARTESIAN_POINT ( 'NONE',  ( 7.188101187499999156, -16.62500000204838813, 2.977408999572654924 ) ) ;
#104753=CARTESIAN_POINT ( 'NONE',  ( 2.977408999572650927, -28.25000000204838813, -7.188101187500001821 ) ) ;
#104798=CARTESIAN_POINT ( 'NONE',  ( -2.977408999572654480, -23.00000000204839523, 7.188101187499999156 ) ) ;
#104813=CARTESIAN_POINT ( 'NONE',  ( 7.188101187500000933, -11.56250000204838635, -2.977408999572650483 ) ) ;
#104824=CARTESIAN_POINT ( 'NONE',  ( -9.999952458099484076, 81.00011885476135376, 0.2653554233229110659 ) ) ;
#104828=CARTESIAN_POINT ( 'NONE',  ( -5.656854249492381470, -14.75000000409677092, 5.656854249492379694 ) ) ;
#104836=CARTESIAN_POINT ( 'NONE',  ( -9.220915120640585272, 86.04454886432084493, -3.870126578504838655 ) ) ;
#104839=CARTESIAN_POINT ( 'NONE',  ( -9.843039827103243766, 33.59083502508334362, -1.781495459429555339 ) ) ;
#104842=( NAMED_UNIT ( * ) SI_UNIT ( $, .STERADIAN. ) SOLID_ANGLE_UNIT ( ) );
#104883=CIRCLE ( 'NONE', #25697, 10.00000000000000000 ) ;
#104899=CARTESIAN_POINT ( 'NONE',  ( -7.188101187500001821, -18.50000000204838457, -2.977408999572651371 ) ) ;
#104901=CARTESIAN_POINT ( 'NONE',  ( -1.469576158976823947E-15, -20.56250000409676915, 8.000000000000000000 ) ) ;
#104902=CARTESIAN_POINT ( 'NONE',  ( -8.000000000000000000, -23.74999999999999289, -9.797174393178825657E-16 ) ) ;
#104921=CARTESIAN_POINT ( 'NONE',  ( -8.000000000000000000, -19.43750000409677270, -9.797174393178825657E-16 ) ) ;
#104961=CARTESIAN_POINT ( 'NONE',  ( -8.000000000000001776, -32.84375000409677625, 3.313708498984758943 ) ) ;
#105081=LINE ( 'NONE', #97488, #85488 ) ;
#105085=CARTESIAN_POINT ( 'NONE',  ( -3.313708498984760720, -16.53124999999999289, -8.000000000000000000 ) ) ;
#105141=CARTESIAN_POINT ( 'NONE',  ( -9.151133496029672187, 15.07443463110270088, -4.034557488804598968 ) ) ;
#105145=CARTESIAN_POINT ( 'NONE',  ( 0.7408669144212451929, 15.11700796861005003, -9.999999999997889688 ) ) ;
#105168=EDGE_CURVE ( 'NONE', #10653, #67063, #7046, .T. ) ;
#105199=CARTESIAN_POINT ( 'NONE',  ( -7.551892080562055298, 26.99012297460616239, 2.647003822403974471 ) ) ;
#105206=CARTESIAN_POINT ( 'NONE',  ( -5.656854249492379694, -32.93749999999999289, -5.656854249492380582 ) ) ;
#105225=AXIS2_PLACEMENT_3D ( 'NONE', #56683, #38936, #47535 ) ;
#105232=CARTESIAN_POINT ( 'NONE',  ( 5.082755093536324154, -19.34375000204838457, 5.082755093536326818 ) ) ;
#105275=ORIENTED_EDGE ( 'NONE', *, *, #62580, .T. ) ;
#105280=CARTESIAN_POINT ( 'NONE',  ( 5.082755093536325930, -20.84375000204838813, -5.082755093536325042 ) ) ;
#105289=CARTESIAN_POINT ( 'NONE',  ( 7.188101187499999156, -28.62500000204838457, 2.977408999572654924 ) ) ;
#105324=VECTOR ( 'NONE', #48910, 1000.000000000000000 ) ;
#105332=CARTESIAN_POINT ( 'NONE',  ( 2.977408999572651815, -22.81250000204838813, 7.188101187500000933 ) ) ;
#105345=CARTESIAN_POINT ( 'NONE',  ( -5.082755093536325042, -12.59375000204838280, -5.082755093536325930 ) ) ;
#105360=ORIENTED_EDGE ( 'NONE', *, *, #31857, .T. ) ;
#105361=CARTESIAN_POINT ( 'NONE',  ( -8.000000000000000000, -13.53125000409676915, -3.313708498984762496 ) ) ;
#105364=CARTESIAN_POINT ( 'NONE',  ( -9.644834624769973885, 88.00890500205777300, 2.648308524638419925 ) ) ;
#105367=CARTESIAN_POINT ( 'NONE',  ( -9.220915120640583496, 31.04454886432083782, -3.870126578504839987 ) ) ;
#105371=CARTESIAN_POINT ( 'NONE',  ( -3.648665620917406649, 14.99999999999996625, 10.00000000000006750 ) ) ;
#105414=DIRECTION ( 'NONE',  ( -0.000000000000000000, 1.000000000000000000, -0.000000000000000000 ) ) ;
#105419=CARTESIAN_POINT ( 'NONE',  ( 4.401442555609581635E-16, -17.28125000204838813, -7.188101187500000044 ) ) ;
#105430=CARTESIAN_POINT ( 'NONE',  ( 0.000000000000000000, -30.00000000000000000, 8.000000000000000000 ) ) ;
#105450=EDGE_LOOP ( 'NONE', ( #22199, #34596, #39251 ) ) ;
#105479=CARTESIAN_POINT ( 'NONE',  ( -5.656854249492381470, -28.25000000409677270, 5.656854249492379694 ) ) ;
#105518=CARTESIAN_POINT ( 'NONE',  ( -7.344505440741525781, 32.44618927298703426, -3.175463080953007111 ) ) ;
#105535=SURFACE_STYLE_FILL_AREA ( #24127 ) ;
#105568=CARTESIAN_POINT ( 'NONE',  ( 7.744991119775237465, 101.5356121457486722, -2.016316005557098556 ) ) ;
#105577=CARTESIAN_POINT ( 'NONE',  ( 9.333555687487613994, 106.7810269660896836, 3.591168747312690090 ) ) ;
#105598=CARTESIAN_POINT ( 'NONE',  ( -5.656854249492379694, -13.43749999999999112, -5.656854249492380582 ) ) ;
#105613=( BOUNDED_SURFACE ( )  B_SPLINE_SURFACE ( 3, 2, ( 
 ( #88257, #47242, #50950 ),
 ( #67696, #66087, #25128 ),
 ( #57988, #40746, #73634 ),
 ( #26215, #82806, #7840 ),
 ( #100047, #74697, #9976 ),
 ( #65561, #57446, #98450 ),
 ( #42879, #59074, #66621 ),
 ( #106539, #24073, #9423 ),
 ( #74170, #32694, #24598 ),
 ( #42343, #50421, #25680 ) ),
 .UNSPECIFIED., .F., .F., .F. ) 
 B_SPLINE_SURFACE_WITH_KNOTS ( ( 4, 2, 2, 2, 4 ),
 ( 3, 3 ),
 ( 0.002450517525418896905, 0.003060732775749463834, 0.003670948026080030763, 0.004891378526741164620, 0.007332239528063431468 ),
 ( 0.000000000000000000, 1.000000000000000000 ),
 .UNSPECIFIED. ) 
 GEOMETRIC_REPRESENTATION_ITEM ( )  RATIONAL_B_SPLINE_SURFACE ( (
 ( 1.000000000000000000, 0.7071067811865481278, 1.000000000000000000),
 ( 1.000000000000000000, 0.7344063550101855853, 1.000000000000000000),
 ( 1.000000000000000000, 0.7590375248711127565, 1.000000000000000000),
 ( 1.000000000000000000, 0.8038331608703981335, 1.000000000000000000),
 ( 1.000000000000000000, 0.8240352460865911777, 1.000000000000000000),
 ( 1.000000000000000000, 0.8791017378333240151, 1.000000000000000000),
 ( 1.000000000000000000, 0.9085032776980892510, 1.000000000000000000),
 ( 1.000000000000000000, 0.9784170511696808070, 1.000000000000000000),
 ( 1.000000000000000000, 0.9996598051696607978, 1.000000000000000000),
 ( 1.000000000000000000, 1.000000000000000000, 1.000000000000000000) ) ) 
 REPRESENTATION_ITEM ( '' )  SURFACE ( )  );
#105667=CARTESIAN_POINT ( 'NONE',  ( 0.000000000000000000, 15.00000000000000000, -9.999999999999998224 ) ) ;
#105680=CARTESIAN_POINT ( 'NONE',  ( -7.188101187500002709, -9.687500002048384573, 2.977408999572648707 ) ) ;
#105721=CARTESIAN_POINT ( 'NONE',  ( -10.00000000000000000, 15.00000000000000000, 10.00000000000000000 ) ) ;
#105722=CARTESIAN_POINT ( 'NONE',  ( -8.000000000000001776, -32.65625000000000000, 3.313708498984758943 ) ) ;
#105750=CARTESIAN_POINT ( 'NONE',  ( 2.977408999572650927, -11.37500000204838813, -7.188101187500001821 ) ) ;
#105800=CARTESIAN_POINT ( 'NONE',  ( -7.188101187500002709, -14.18750000204838457, 2.977408999572647819 ) ) ;
#105807=CARTESIAN_POINT ( 'NONE',  ( -1.320432766682874540E-15, -28.90625000204838813, 7.188101187500000044 ) ) ;
#105810=CARTESIAN_POINT ( 'NONE',  ( -2.977408999572654480, -26.00000000204839168, 7.188101187499999156 ) ) ;
#105816=CARTESIAN_POINT ( 'NONE',  ( -7.343637806710344051, 107.4436312190061784, 3.177475076494675310 ) ) ;
#105846=CARTESIAN_POINT ( 'NONE',  ( 4.898587196589412829E-16, -13.81250000409676915, -8.000000000000000000 ) ) ;
#105848=CARTESIAN_POINT ( 'NONE',  ( 4.401442555609581635E-16, -26.65625000204838813, -7.188101187500000044 ) ) ;
#105864=CARTESIAN_POINT ( 'NONE',  ( -7.188101187500000044, -12.40625000204838635, -8.802885111219163269E-16 ) ) ;
#105875=CARTESIAN_POINT ( 'NONE',  ( -3.313708498984765161, -10.15625000409677092, 7.999999999999998224 ) ) ;
#105877=CARTESIAN_POINT ( 'NONE',  ( 9.910377230549926253, 15.23810023151367155, 1.510421413154057424 ) ) ;
#105881=CARTESIAN_POINT ( 'NONE',  ( -9.176645556628255207, 30.52739032406730502, 3.973966573947708802 ) ) ;
#105900=ORIENTED_EDGE ( 'NONE', *, *, #22127, .F. ) ;
#105932=CARTESIAN_POINT ( 'NONE',  ( -5.082755093536325042, -20.09375000204838457, -5.082755093536325930 ) ) ;
#105935=( BOUNDED_CURVE ( )  B_SPLINE_CURVE ( 2, ( #78254, #14032, #4907, #53458, #79836, #30255, #61566, #4367, #5942 ),
 .UNSPECIFIED., .F., .F. ) 
 B_SPLINE_CURVE_WITH_KNOTS ( ( 3, 2, 2, 2, 3 ),
 ( 0.2794117647058823040, 0.2867647058823528661, 0.2941176470588234837, 0.3014705882352940458, 0.3088235294117646634 ),
 .UNSPECIFIED. ) 
 CURVE ( )  GEOMETRIC_REPRESENTATION_ITEM ( )  RATIONAL_B_SPLINE_CURVE ( ( 1.000000000000000666, 0.9238795325112861834, 1.000000000000000000, 0.9238795325112867385, 1.000000000000000000, 0.9238795325112867385, 1.000000000000000000, 0.9238795325112872936, 0.9999999999999994449 ) ) 
 REPRESENTATION_ITEM ( '' )  );
#105936=CARTESIAN_POINT ( 'NONE',  ( 9.989435848181784650, 81.02619707471572497, -0.5278651953176017875 ) ) ;
#105953=CARTESIAN_POINT ( 'NONE',  ( -5.656854249492381470, -19.25000000409677270, 5.656854249492379694 ) ) ;
#105966=FACE_OUTER_BOUND ( 'NONE', #81526, .T. ) ;
#105981=( GEOMETRIC_REPRESENTATION_CONTEXT ( 3 ) GLOBAL_UNCERTAINTY_ASSIGNED_CONTEXT ( ( #60210 ) ) GLOBAL_UNIT_ASSIGNED_CONTEXT ( ( #39591, #14746, #104842 ) ) REPRESENTATION_CONTEXT ( 'NONE', 'WORKASPACE' ) );
#105993=CARTESIAN_POINT ( 'NONE',  ( 5.656854249492378806, -27.87500000409677270, 5.656854249492381470 ) ) ;
#106017=SURFACE_STYLE_FILL_AREA ( #88797 ) ;
#106058=MECHANICAL_DESIGN_GEOMETRIC_PRESENTATION_REPRESENTATION('',(#35449),#100919);
#106085=CARTESIAN_POINT ( 'NONE',  ( 7.619701877737480977, 101.8255784046723562, -2.447562251315980486 ) ) ;
#106096=CARTESIAN_POINT ( 'NONE',  ( -1.469576158976823947E-15, -17.56250000409676915, 8.000000000000000000 ) ) ;
#106114=CARTESIAN_POINT ( 'NONE',  ( -5.656854249492381470, -17.56249999999999645, 5.656854249492379694 ) ) ;
#106118=CARTESIAN_POINT ( 'NONE',  ( -7.896254658894421574, 101.2107081724580127, 1.307282859663298602 ) ) ;
#106178=CARTESIAN_POINT ( 'NONE',  ( -1.320432766682874540E-15, -31.53125000204838457, 7.188101187500000044 ) ) ;
#106190=STYLED_ITEM ( 'NONE', ( #88129 ), #6831 ) ;
#106241=CARTESIAN_POINT ( 'NONE',  ( 3.313708498984762052, -34.71875000000000000, -8.000000000000000000 ) ) ;
#106265=CARTESIAN_POINT ( 'NONE',  ( -5.082755093536325042, -12.59375000204838280, -5.082755093536325930 ) ) ;
#106316=CARTESIAN_POINT ( 'NONE',  ( -7.188101187500002709, -11.18750000204838457, 2.977408999572647819 ) ) ;
#106318=CARTESIAN_POINT ( 'NONE',  ( 7.070208275066456771, -30.00000000000001776, 1.379431653863122387 ) ) ;
#106324=CARTESIAN_POINT ( 'NONE',  ( 2.977408999572651815, -25.81250000204838813, 7.188101187500000933 ) ) ;
#106343=CARTESIAN_POINT ( 'NONE',  ( -7.986539162393901492, 88.97327171057456496, -0.5321833565149907130 ) ) ;
#106368=CARTESIAN_POINT ( 'NONE',  ( -1.469576158976823947E-15, -23.56250000409677270, 8.000000000000000000 ) ) ;
#106370=CARTESIAN_POINT ( 'NONE',  ( 2.977408999572650927, -25.25000000204839523, -7.188101187500001821 ) ) ;
#106383=CARTESIAN_POINT ( 'NONE',  ( 0.000000000000000000, 15.00000000000000000, -8.000000000000000000 ) ) ;
#106384=CARTESIAN_POINT ( 'NONE',  ( 5.082755093536325930, -14.46875000204838457, -5.082755093536325042 ) ) ;
#106390=VERTEX_POINT ( 'NONE', #3805 ) ;
#106394=CARTESIAN_POINT ( 'NONE',  ( -5.656854249492381470, -19.06249999999999289, 5.656854249492379694 ) ) ;
#106396=CIRCLE ( 'NONE', #68555, 11.00000000000000000 ) ;
#106398=CARTESIAN_POINT ( 'NONE',  ( -7.188101187500000044, -31.90625000204838813, -8.802885111219163269E-16 ) ) ;
#106412=ADVANCED_FACE ( 'NONE', ( #5396 ), #5330, .F. ) ;
#106452=CARTESIAN_POINT ( 'NONE',  ( 7.003653396366580353, 86.05706205559677358, -3.866846144092868531 ) ) ;
#106454=AXIS2_PLACEMENT_3D ( 'NONE', #36283, #60533, #101503 ) ;
#106462=CARTESIAN_POINT ( 'NONE',  ( -5.082755093536325042, -17.09375000204838813, -5.082755093536325930 ) ) ;
#106464=CARTESIAN_POINT ( 'NONE',  ( 9.798380800342661345, 81.53199345684495825, -2.010350564680322361 ) ) ;
#106521=CARTESIAN_POINT ( 'NONE',  ( 7.188101187500000044, -29.65625000204838813, 0.000000000000000000 ) ) ;
#106531=CARTESIAN_POINT ( 'NONE',  ( -5.656854249492381470, -23.75000000409677270, 5.656854249492379694 ) ) ;
#106533=CYLINDRICAL_SURFACE ( 'NONE', #93895, 8.000000000000000000 ) ;
#106539=CARTESIAN_POINT ( 'NONE',  ( -1.544939622599253326, 15.00000000000000000, -9.999999999999998224 ) ) ;
#106541=CARTESIAN_POINT ( 'NONE',  ( -3.999994092537668244, -10.00072617203139203, 6.928206640937045080 ) ) ;
#106549=CARTESIAN_POINT ( 'NONE',  ( 4.898587196589412829E-16, -15.31250000409677092, -8.000000000000000000 ) ) ;
#106557=SURFACE_SIDE_STYLE ('',( #106017 ) ) ;
#106566=( BOUNDED_CURVE ( )  B_SPLINE_CURVE ( 2, ( #87829, #22590, #55427, #78642, #71618, #13377, #104520, #4781, #21520 ),
 .UNSPECIFIED., .F., .F. ) 
 B_SPLINE_CURVE_WITH_KNOTS ( ( 3, 2, 2, 2, 3 ),
 ( 0.3382352941176470229, 0.3455882352941175850, 0.3529411764705882026, 0.3602941176470587648, 0.3676470588235293824 ),
 .UNSPECIFIED. ) 
 CURVE ( )  GEOMETRIC_REPRESENTATION_ITEM ( )  RATIONAL_B_SPLINE_CURVE ( ( 1.000000000000000666, 0.9238795325112861834, 1.000000000000000000, 0.9238795325112867385, 1.000000000000000000, 0.9238795325112867385, 1.000000000000000000, 0.9238795325112872936, 0.9999999999999994449 ) ) 
 REPRESENTATION_ITEM ( '' )  );
#106573=CARTESIAN_POINT ( 'NONE',  ( -7.801339272325197527, 33.58731471959700343, -1.788609912539670166 ) ) ;
#106582=CARTESIAN_POINT ( 'NONE',  ( -7.912393634621968097, -29.99999999999999645, -0.8598757053164162167 ) ) ;
#106611=SURFACE_STYLE_USAGE ( .BOTH. , #98519 ) ;
#106637=CARTESIAN_POINT ( 'NONE',  ( 9.842984802582135373, 108.5906959047565010, 1.781981959250507064 ) ) ;
#106703=CARTESIAN_POINT ( 'NONE',  ( -1.469576158976823947E-15, -17.37499999999999289, 8.000000000000000000 ) ) ;
#106722=CARTESIAN_POINT ( 'NONE',  ( -7.188101187500000044, -33.40625000204838813, -8.802885111219163269E-16 ) ) ;
#106780=CARTESIAN_POINT ( 'NONE',  ( 5.656854249492380582, -33.31249999999999289, -5.656854249492379694 ) ) ;
ENDSEC;
END-ISO-10303-21;
